ISO-10303-21;
HEADER;
FILE_DESCRIPTION (('STEP AP203'),
    '1' );
FILE_NAME ('Part1_handle1.step',
    '2026-10-06T15:07:10',
    ( '' ),
    ( '' ),
    'SwSTEP 2.0',
    'SolidWorks 2024',
    '' );
FILE_SCHEMA (( 'AUTOMOTIVE_DESIGN' ));
ENDSEC;

DATA;
#1=ADVANCED_FACE ( 'NONE', ( #10434 ), #18456, .F. ) ;
#11=VERTEX_POINT ( 'NONE', #9811 ) ;
#30=CARTESIAN_POINT ( 'NONE',  ( -3.423602242323041001, -10.69107769603132674, 1.500000000000237144 ) ) ;
#31=CARTESIAN_POINT ( 'NONE',  ( 2.717504505341735932, -0.4236608596156870021, 1.500000000000000000 ) ) ;
#32=CARTESIAN_POINT ( 'NONE',  ( 107.5624060836778426, -18.99272400518356463, -4.497198431447757550 ) ) ;
#36=AXIS2_PLACEMENT_3D ( 'NONE', #29138, #6225, #23788 ) ;
#42=DIRECTION ( 'NONE',  ( 0.000000000000000000, 1.000000000000000000, 0.000000000000000000 ) ) ;
#44=CARTESIAN_POINT ( 'NONE',  ( -2.880987360464337677, -0.6119841066606566127, -1.499999999999999334 ) ) ;
#50=ORIENTED_EDGE ( 'NONE', *, *, #20292, .T. ) ;
#54=VECTOR ( 'NONE', #11765, 999.9999999999998863 ) ;
#55=CARTESIAN_POINT ( 'NONE',  ( 2.117172266158220406, -1.242920418748501676, -0.9788672205888330202 ) ) ;
#56=CARTESIAN_POINT ( 'NONE',  ( 19.46884934643044929, -15.80146560116522991, 1.000000000000000000 ) ) ;
#57=EDGE_LOOP ( 'NONE', ( #2228, #29495, #10201, #20358 ) ) ;
#62=CARTESIAN_POINT ( 'NONE',  ( -2.655659815844460869, 0.1700350810717016214, 1.254089647469669000 ) ) ;
#63=DIRECTION ( 'NONE',  ( 0.000000000000000000, -0.000000000000000000, -1.000000000000000000 ) ) ;
#73=CARTESIAN_POINT ( 'NONE',  ( 0.8174907777731121872, -3.242754804592638429, -1.762319835267122992 ) ) ;
#74=CARTESIAN_POINT ( 'NONE',  ( 0.9232102171129921153, 0.000000000000000000, 4.522129901861157819 ) ) ;
#77=AXIS2_PLACEMENT_3D ( 'NONE', #24647, #7270, #1946 ) ;
#79=CARTESIAN_POINT ( 'NONE',  ( 0.6738579927983930906, -5.220872085256825557, 1.499999999999999556 ) ) ;
#96=AXIS2_PLACEMENT_3D ( 'NONE', #16937, #1925, #32505 ) ;
#103=ORIENTED_EDGE ( 'NONE', *, *, #2188, .F. ) ;
#107=CARTESIAN_POINT ( 'NONE',  ( 13.65718777918027271, -19.09288791508984318, -4.522129901861166701 ) ) ;
#113=CARTESIAN_POINT ( 'NONE',  ( 107.9870634758426746, -17.88307938695580646, -4.509668461024523012 ) ) ;
#117=LINE ( 'NONE', #10625, #6451 ) ;
#120=CARTESIAN_POINT ( 'NONE',  ( 21.54063306425963020, -21.75686058823632862, -1.475739251284730269 ) ) ;
#124=ORIENTED_EDGE ( 'NONE', *, *, #31376, .T. ) ;
#140=VERTEX_POINT ( 'NONE', #15060 ) ;
#143=AXIS2_PLACEMENT_3D ( 'NONE', #19996, #12938, #271 ) ;
#146=CARTESIAN_POINT ( 'NONE',  ( 0.4088345642745362385, -8.504920321588055998, 1.772058741665319292 ) ) ;
#147=CARTESIAN_POINT ( 'NONE',  ( 13.44509804309065615, -13.81913516398266495, 1.499999999999168887 ) ) ;
#152=ORIENTED_EDGE ( 'NONE', *, *, #16988, .F. ) ;
#161=EDGE_CURVE ( 'NONE', #26388, #31289, #10295, .T. ) ;
#163=ORIENTED_EDGE ( 'NONE', *, *, #25130, .F. ) ;
#170=CARTESIAN_POINT ( 'NONE',  ( 10.98818895950636509, -14.84697401622043600, -1.499999999999999556 ) ) ;
#172=CARTESIAN_POINT ( 'NONE',  ( 0.8174570305809125692, -9.170357625429589987, 1.500000000000000444 ) ) ;
#173=ORIENTED_EDGE ( 'NONE', *, *, #21181, .F. ) ;
#176=B_SPLINE_CURVE_WITH_KNOTS ( 'NONE', 3,
 ( #7908, #5090, #2742, #23440, #17780, #10075, #13097, #30687, #7762, #30496, #23136, #15414 ),
 .UNSPECIFIED., .F., .F.,
 ( 4, 2, 2, 2, 2, 4 ),
 ( -5.999999993276212224E-08, 0.0005421711927698825593, 0.0008132867891547902132, 0.001084402385539697759, 0.001626633578309510247, 0.002168864771079322736 ),
 .UNSPECIFIED. ) ;
#179=( GEOMETRIC_REPRESENTATION_CONTEXT ( 3 ) GLOBAL_UNCERTAINTY_ASSIGNED_CONTEXT ( ( #3915 ) ) GLOBAL_UNIT_ASSIGNED_CONTEXT ( ( #27348, #27672, #7131 ) ) REPRESENTATION_CONTEXT ( 'NONE', 'WORKASPACE' ) );
#187=EDGE_CURVE ( 'NONE', #21614, #30476, #10440, .T. ) ;
#201=EDGE_CURVE ( 'NONE', #32996, #24872, #8151, .T. ) ;
#220=CARTESIAN_POINT ( 'NONE',  ( 107.5617944031221640, -18.98359742639815551, 4.522129901861158707 ) ) ;
#222=CARTESIAN_POINT ( 'NONE',  ( 3.557967483062660641, -17.13335440830369194, 1.747754005074379169 ) ) ;
#227=FACE_OUTER_BOUND ( 'NONE', #31998, .T. ) ;
#249=CARTESIAN_POINT ( 'NONE',  ( 72.52374898135332160, -19.78015497550546442, -4.522129901861164925 ) ) ;
#251=ORIENTED_EDGE ( 'NONE', *, *, #16628, .F. ) ;
#254=CARTESIAN_POINT ( 'NONE',  ( -2.745055912661534592, -0.1926413909284909742, 1.404235515125175970 ) ) ;
#255=DIRECTION ( 'NONE',  ( 0.000000000000000000, -1.000000000000000000, 0.000000000000000000 ) ) ;
#257=EDGE_LOOP ( 'NONE', ( #26300, #26585, #23410, #1568 ) ) ;
#271=DIRECTION ( 'NONE',  ( 1.000000000000000000, 0.000000000000000000, 0.000000000000000000 ) ) ;
#274=CARTESIAN_POINT ( 'NONE',  ( 3.566513200368869096, -17.47573827932033197, 1.500000000000000000 ) ) ;
#291=CARTESIAN_POINT ( 'NONE',  ( 0.3285611067768016147, -13.34342412963018276, -4.522129901861166701 ) ) ;
#294=CARTESIAN_POINT ( 'NONE',  ( -3.765880891406458986, -9.390842214537469701, 1.743616753168593769 ) ) ;
#302=EDGE_CURVE ( 'NONE', #6546, #31289, #13105, .T. ) ;
#303=DIRECTION ( 'NONE',  ( -0.000000000000000000, -0.000000000000000000, -1.000000000000000000 ) ) ;
#310=CARTESIAN_POINT ( 'NONE',  ( 23.22564588060107482, -21.93932300456764040, 1.000000000000000000 ) ) ;
#319=CARTESIAN_POINT ( 'NONE',  ( 0.1303119166710321464, -6.187468044926815125, 1.772538222416039089 ) ) ;
#320=CARTESIAN_POINT ( 'NONE',  ( 8.690654616498143525, -10.89241706857682956, 1.499999999999998668 ) ) ;
#324=FACE_OUTER_BOUND ( 'NONE', #26610, .T. ) ;
#327=EDGE_CURVE ( 'NONE', #7729, #6546, #8223, .T. ) ;
#328=EDGE_CURVE ( 'NONE', #24580, #21614, #8416, .T. ) ;
#368=DIRECTION ( 'NONE',  ( -0.9816271834476639757, 0.000000000000000000, -0.1908089953765449709 ) ) ;
#370=DIRECTION ( 'NONE',  ( 1.000000000000000000, -2.473959037481237219E-13, 0.000000000000000000 ) ) ;
#373=CARTESIAN_POINT ( 'NONE',  ( -4.433196769082780264, -8.338993190668213984, 1.500000000000000000 ) ) ;
#375=CARTESIAN_POINT ( 'NONE',  ( 72.90878003214187686, -18.24052684336794883, 1.499999999999999556 ) ) ;
#387=EDGE_CURVE ( 'NONE', #22172, #21390, #18321, .T. ) ;
#393=CARTESIAN_POINT ( 'NONE',  ( -1.047937531484008478, -4.989690239015235562, -4.522129901861164925 ) ) ;
#395=CARTESIAN_POINT ( 'NONE',  ( 107.5537258199849617, -18.86684600943444678, 4.756303069492835434 ) ) ;
#406=CARTESIAN_POINT ( 'NONE',  ( 108.6155529559672885, -15.79924867777639186, -1.500000000000000000 ) ) ;
#411=CARTESIAN_POINT ( 'NONE',  ( 107.6641948605228123, -20.45809826282219746, -1.499999999999999556 ) ) ;
#416=CARTESIAN_POINT ( 'NONE',  ( 19.80237848050798988, -16.61788897934828668, 1.500000000000000666 ) ) ;
#428=DIRECTION ( 'NONE',  ( 0.000000000000000000, 1.000000000000000000, 0.000000000000000000 ) ) ;
#435=CARTESIAN_POINT ( 'NONE',  ( -0.9232102171129831225, 0.000000000000000000, -4.522129901861166701 ) ) ;
#438=CARTESIAN_POINT ( 'NONE',  ( 16.00007615138554584, -20.81650653636907222, 1.751028325053374912 ) ) ;
#451=CARTESIAN_POINT ( 'NONE',  ( -1.170068671574863162, -6.059534462705075342, -4.522129901861164925 ) ) ;
#458=CARTESIAN_POINT ( 'NONE',  ( -31.18783180709124636, -25.44850941282521006, 1.500000000000000000 ) ) ;
#460=ORIENTED_EDGE ( 'NONE', *, *, #1746, .F. ) ;
#463=CIRCLE ( 'NONE', #26112, 2.524999999999999467 ) ;
#466=CARTESIAN_POINT ( 'NONE',  ( 10.37705096095590385, -12.86926679082321989, 1.500000000000000000 ) ) ;
#474=CARTESIAN_POINT ( 'NONE',  ( -31.57659242536668032, -27.93932300454937590, -1.500000000000000000 ) ) ;
#477=CARTESIAN_POINT ( 'NONE',  ( -16.20597128428593336, -10.96966150227469328, -11.00000000000000000 ) ) ;
#478=DIRECTION ( 'NONE',  ( -0.9916316928897271898, 0.1290991311227692728, 0.000000000000000000 ) ) ;
#491=EDGE_CURVE ( 'NONE', #21250, #937, #1474, .T. ) ;
#498=DIRECTION ( 'NONE',  ( -1.000000000000000000, -0.000000000000000000, 3.469446951953613794E-15 ) ) ;
#503=CARTESIAN_POINT ( 'NONE',  ( 12.58808848377064749, -13.45617626434417424, -1.000000000000000000 ) ) ;
#517=DIRECTION ( 'NONE',  ( 0.000000000000000000, 0.000000000000000000, 1.000000000000000000 ) ) ;
#519=CARTESIAN_POINT ( 'NONE',  ( -4.280319716189089796, -6.512003988132526899, 1.499999999999839906 ) ) ;
#530=CIRCLE ( 'NONE', #8506, 10.46966150227469150 ) ;
#532=CARTESIAN_POINT ( 'NONE',  ( -2.800010172794354268, -0.4410551771863219783, -1.509141217649267563 ) ) ;
#540=CARTESIAN_POINT ( 'NONE',  ( 0.5859972064454607166, -5.135271408404159743, -0.9788672205888330202 ) ) ;
#541=CARTESIAN_POINT ( 'NONE',  ( 9.225170531479669478, -11.43511417576379152, 1.000000000000000222 ) ) ;
#542=CARTESIAN_POINT ( 'NONE',  ( 107.9485675974711825, -17.32874831497913704, 4.529272001225892907 ) ) ;
#548=ORIENTED_EDGE ( 'NONE', *, *, #612, .F. ) ;
#553=DIRECTION ( 'NONE',  ( -0.1908089953765452762, 2.336736254364082527E-17, 0.9816271834476639757 ) ) ;
#557=CARTESIAN_POINT ( 'NONE',  ( -17.45597128428593692, -25.43932300454937945, 11.00000000000000000 ) ) ;
#559=DIRECTION ( 'NONE',  ( 0.000000000000000000, 0.000000000000000000, 1.000000000000000000 ) ) ;
#560=CARTESIAN_POINT ( 'NONE',  ( 25.61042644976673444, -17.59778802277001475, -1.000000000000000000 ) ) ;
#563=VECTOR ( 'NONE', #4638, 1000.000000000000000 ) ;
#570=CARTESIAN_POINT ( 'NONE',  ( 74.44693909926891706, -23.04272217940160417, 0.9788672205877712029 ) ) ;
#579=ORIENTED_EDGE ( 'NONE', *, *, #5693, .F. ) ;
#593=VERTEX_POINT ( 'NONE', #13532 ) ;
#604=LINE ( 'NONE', #23341, #24218 ) ;
#612=EDGE_CURVE ( 'NONE', #16944, #1202, #29094, .T. ) ;
#626=CARTESIAN_POINT ( 'NONE',  ( 10.65647057407925935, -13.03481288881981470, 1.500000000000000000 ) ) ;
#629=AXIS2_PLACEMENT_3D ( 'NONE', #5301, #20695, #17660 ) ;
#635=VERTEX_POINT ( 'NONE', #15729 ) ;
#636=CARTESIAN_POINT ( 'NONE',  ( 1.073911348006138189, -2.620901292623725176, 1.760914277779327852 ) ) ;
#645=CARTESIAN_POINT ( 'NONE',  ( 107.6936962044510437, -18.97455700431297743, -4.522180800239018694 ) ) ;
#657=EDGE_CURVE ( 'NONE', #8978, #937, #27438, .T. ) ;
#661=VECTOR ( 'NONE', #32653, 1000.000000000000000 ) ;
#665=CARTESIAN_POINT ( 'NONE',  ( 108.1329823800173102, -19.98427530701518506, -1.262026545339949957 ) ) ;
#680=AXIS2_PLACEMENT_3D ( 'NONE', #6810, #29224, #6310 ) ;
#682=AXIS2_PLACEMENT_3D ( 'NONE', #9016, #19424, #19236 ) ;
#690=CARTESIAN_POINT ( 'NONE',  ( 0.000000000000000000, -0.5000000000000000000, -1.000000000000000000 ) ) ;
#695=CARTESIAN_POINT ( 'NONE',  ( 0.4213074008609886123, -4.489821273616160902, -1.766536014443793157 ) ) ;
#697=VERTEX_POINT ( 'NONE', #21084 ) ;
#701=CARTESIAN_POINT ( 'NONE',  ( 17.33093461831356663, -21.43932300456619799, 1.499999999999999112 ) ) ;
#705=ORIENTED_EDGE ( 'NONE', *, *, #743, .T. ) ;
#716=CARTESIAN_POINT ( 'NONE',  ( -2.910169157840587939, 0.01692106640608362356, -0.9265120394754853272 ) ) ;
#726=CARTESIAN_POINT ( 'NONE',  ( 107.4617763835125430, -17.53021834753707964, 4.828547747425045777 ) ) ;
#740=EDGE_CURVE ( 'NONE', #28886, #23895, #13196, .T. ) ;
#743=EDGE_CURVE ( 'NONE', #9413, #2672, #27116, .T. ) ;
#748=CARTESIAN_POINT ( 'NONE',  ( -0.9904391912309036261, -13.96299501477513694, -1.744689047112403024 ) ) ;
#751=CARTESIAN_POINT ( 'NONE',  ( 23.15368348410971677, -16.86203458189143944, -1.500000000001110223 ) ) ;
#752=CARTESIAN_POINT ( 'NONE',  ( 107.8942783567389796, -16.54699675389560909, -1.787313614190034539 ) ) ;
#755=CARTESIAN_POINT ( 'NONE',  ( 0.7529060732733400263, -8.134409449814636872, 1.500000000000000222 ) ) ;
#758=CARTESIAN_POINT ( 'NONE',  ( 3.295700863922491841, -0.1006852655820335979, 1.307585114970543527 ) ) ;
#771=ORIENTED_EDGE ( 'NONE', *, *, #7007, .F. ) ;
#772=CARTESIAN_POINT ( 'NONE',  ( 21.08401840680096129, -16.78474387324269657, -1.500000000000000000 ) ) ;
#776=DIRECTION ( 'NONE',  ( -0.1908089953765452762, 4.720536385445197917E-14, 0.9816271834476639757 ) ) ;
#781=DIRECTION ( 'NONE',  ( -1.000000000000000000, 0.000000000000000000, 0.000000000000000000 ) ) ;
#803=CARTESIAN_POINT ( 'NONE',  ( 0.000000000000000000, -25.93932300454937945, 11.50000000000000000 ) ) ;
#808=ORIENTED_EDGE ( 'NONE', *, *, #4569, .T. ) ;
#814=CARTESIAN_POINT ( 'NONE',  ( 8.323087564152990225, -11.23204384871645445, 1.500000000000000000 ) ) ;
#825=EDGE_LOOP ( 'NONE', ( #8438, #11419, #17829, #28728, #15049 ) ) ;
#829=CARTESIAN_POINT ( 'NONE',  ( 9.172108879787138846, -0.1070445578126106578, 1.318121098349317233 ) ) ;
#839=CARTESIAN_POINT ( 'NONE',  ( -31.57659242536668032, -21.43932300455408679, -1.500000000000000000 ) ) ;
#840=CARTESIAN_POINT ( 'NONE',  ( 0.7294883270165408717, -11.94795532514693548, 5.485967528433933538 ) ) ;
#841=ORIENTED_EDGE ( 'NONE', *, *, #657, .F. ) ;
#848=FACE_OUTER_BOUND ( 'NONE', #25602, .T. ) ;
#854=EDGE_CURVE ( 'NONE', #11874, #1933, #8468, .T. ) ;
#856=CARTESIAN_POINT ( 'NONE',  ( 8.285115449721931924, -10.40907249743529661, -1.000000000000000000 ) ) ;
#861=FACE_OUTER_BOUND ( 'NONE', #4593, .T. ) ;
#869=CARTESIAN_POINT ( 'NONE',  ( 15.95505479268522642, -20.93460661231094733, 1.499999999995777378 ) ) ;
#871=CARTESIAN_POINT ( 'NONE',  ( 21.59559372541029276, -17.25941758357585698, 1.753144073645959145 ) ) ;
#884=ADVANCED_FACE ( 'NONE', ( #20061 ), #30103, .T. ) ;
#885=CARTESIAN_POINT ( 'NONE',  ( 19.69555400981542803, -21.64588847999043253, 1.456500879219768452 ) ) ;
#890=CARTESIAN_POINT ( 'NONE',  ( 107.4977942790300460, -18.05374091625411026, 5.138025335311863451 ) ) ;
#892=CARTESIAN_POINT ( 'NONE',  ( -15.51216819290874227, 0.000000000000000000, 1.500000000000000000 ) ) ;
#899=LINE ( 'NONE', #26780, #12884 ) ;
#906=CARTESIAN_POINT ( 'NONE',  ( 107.9484595593237231, -17.32719259252710842, -4.525028783333800320 ) ) ;
#907=CARTESIAN_POINT ( 'NONE',  ( 24.80306213860341558, -17.49230408913766865, 1.499999999999999778 ) ) ;
#913=CARTESIAN_POINT ( 'NONE',  ( 2.712282326253089959, -0.4283266402567246223, 1.500000000000000444 ) ) ;
#923=CARTESIAN_POINT ( 'NONE',  ( -15.51216819290874227, -25.44850941282521006, 1.500000000000000000 ) ) ;
#926=VERTEX_POINT ( 'NONE', #32930 ) ;
#930=CARTESIAN_POINT ( 'NONE',  ( -2.889143798725324785, 0.000000000000000000, -0.9788672205760856615 ) ) ;
#937=VERTEX_POINT ( 'NONE', #28069 ) ;
#938=CARTESIAN_POINT ( 'NONE',  ( 21.97280264420809814, -21.86582870483968577, 1.264433483335436481 ) ) ;
#940=DIRECTION ( 'NONE',  ( -0.000000000000000000, -0.000000000000000000, 1.000000000000000000 ) ) ;
#942=CARTESIAN_POINT ( 'NONE',  ( 107.5608083496522767, -18.96961453642471795, 4.558424976626936242 ) ) ;
#944=CARTESIAN_POINT ( 'NONE',  ( -2.633834500755857455, -0.2542144740826015603, -1.655286495009812064 ) ) ;
#956=DIRECTION ( 'NONE',  ( 1.000000000000000000, -2.473959037481237219E-13, 0.000000000000000000 ) ) ;
#957=FACE_OUTER_BOUND ( 'NONE', #10051, .T. ) ;
#958=CARTESIAN_POINT ( 'NONE',  ( 8.996310305901880966, 0.3994363609773792789, 1.500000000000000000 ) ) ;
#962=CARTESIAN_POINT ( 'NONE',  ( 3.920534810732780873, -12.31833506282117519, 1.757815050190617567 ) ) ;
#966=CARTESIAN_POINT ( 'NONE',  ( 24.12394826718414365, -17.31889127434044440, -1.369171926258704541 ) ) ;
#973=CARTESIAN_POINT ( 'NONE',  ( 24.37017644007658390, -17.36705458136659175, -1.347230727354008728 ) ) ;
#984=CARTESIAN_POINT ( 'NONE',  ( -2.819379691724118508, -6.927609664242505794, 4.522129901861159595 ) ) ;
#985=ADVANCED_FACE ( 'NONE', ( #2503, #22875 ), #33078, .T. ) ;
#993=VERTEX_POINT ( 'NONE', #30766 ) ;
#1000=CARTESIAN_POINT ( 'NONE',  ( 24.26314457552869186, -17.18612746004505709, -0.9999999999999997780 ) ) ;
#1005=CARTESIAN_POINT ( 'NONE',  ( 0.9232102171129938917, 0.000000000000000000, -4.522129901861164925 ) ) ;
#1007=CARTESIAN_POINT ( 'NONE',  ( 19.06772426462030623, -16.20389337104299798, 1.500000000000000000 ) ) ;
#1008=FACE_OUTER_BOUND ( 'NONE', #32534, .T. ) ;
#1024=DIRECTION ( 'NONE',  ( -0.000000000000000000, -0.000000000000000000, 1.000000000000000000 ) ) ;
#1029=VERTEX_POINT ( 'NONE', #2843 ) ;
#1046=ORIENTED_EDGE ( 'NONE', *, *, #11544, .F. ) ;
#1050=CARTESIAN_POINT ( 'NONE',  ( 11.72844750001322822, -13.05523934058288837, -1.000000000000000000 ) ) ;
#1051=CARTESIAN_POINT ( 'NONE',  ( 107.4502834832519937, -17.36344364793921713, -4.530928846047229896 ) ) ;
#1058=B_SPLINE_CURVE_WITH_KNOTS ( 'NONE', 3,
 ( #9443, #29853, #6935, #14138, #17134, #8946, #24338, #1450, #32034, #9104, #27343, #4464, #12281, #4950, #10454, #33029 ),
 .UNSPECIFIED., .F., .F.,
 ( 4, 2, 2, 2, 2, 2, 2, 4 ),
 ( 0.005048008663721728281, 0.006023483056901835289, 0.006511220253491893997, 0.006755088851786918147, 0.006877023150934431089, 0.006937990300508186693, 0.006968473875295064929, 0.006998957450081943164 ),
 .UNSPECIFIED. ) ;
#1064=CARTESIAN_POINT ( 'NONE',  ( 17.33093461831347781, -21.43932300456618378, 1.500000000000000000 ) ) ;
#1067=CARTESIAN_POINT ( 'NONE',  ( 19.72835230534338891, -21.42792461751427169, 1.670332045613381222 ) ) ;
#1072=ORIENTED_EDGE ( 'NONE', *, *, #24945, .T. ) ;
#1076=CARTESIAN_POINT ( 'NONE',  ( 25.52557118915443723, -17.56218954043521308, -1.000000000000000444 ) ) ;
#1080=ORIENTED_EDGE ( 'NONE', *, *, #6143, .T. ) ;
#1084=AXIS2_PLACEMENT_3D ( 'NONE', #25186, #12492, #22701 ) ;
#1091=EDGE_CURVE ( 'NONE', #926, #21122, #3685, .T. ) ;
#1095=CARTESIAN_POINT ( 'NONE',  ( 108.0601430345486307, -18.93540685241356769, 4.558616106265892753 ) ) ;
#1099=LINE ( 'NONE', #9089, #14117 ) ;
#1106=AXIS2_PLACEMENT_3D ( 'NONE', #13582, #15922, #8262 ) ;
#1115=CARTESIAN_POINT ( 'NONE',  ( 7.637044423814637994, -3.948987408041380487, 1.000000000000000000 ) ) ;
#1117=CARTESIAN_POINT ( 'NONE',  ( 19.06772426461969516, -16.20389337104281680, -1.500000000000000666 ) ) ;
#1119=CARTESIAN_POINT ( 'NONE',  ( 0.5495841022003185028, -7.012970908023616445, 1.500000000000000000 ) ) ;
#1133=DIRECTION ( 'NONE',  ( 0.000000000000000000, -1.000000000000000000, 0.000000000000000000 ) ) ;
#1139=VERTEX_POINT ( 'NONE', #9301 ) ;
#1140=CARTESIAN_POINT ( 'NONE',  ( 21.08401840680153327, -16.78474387323987926, -1.949999999999999512 ) ) ;
#1146=CARTESIAN_POINT ( 'NONE',  ( 6.399351475474185591, -16.64279405589157079, 5.485967528433935314 ) ) ;
#1169=CARTESIAN_POINT ( 'NONE',  ( -3.222375984151267581, 0.000000000000000000, -1.000000000000000000 ) ) ;
#1179=ORIENTED_EDGE ( 'NONE', *, *, #17111, .F. ) ;
#1184=CARTESIAN_POINT ( 'NONE',  ( 10.25014922901193692, -19.98138187138910737, 1.499999999999999112 ) ) ;
#1195=CARTESIAN_POINT ( 'NONE',  ( -4.147447373149248051, -6.154642429219350674, -1.745243162019930239 ) ) ;
#1198=AXIS2_PLACEMENT_3D ( 'NONE', #27477, #14755, #22445 ) ;
#1202=VERTEX_POINT ( 'NONE', #25175 ) ;
#1207=CARTESIAN_POINT ( 'NONE',  ( 20.72551590764672724, -21.66366526924204194, 1.459983613673395908 ) ) ;
#1212=EDGE_LOOP ( 'NONE', ( #12042, #3122, #11676, #30079, #26435, #23259 ) ) ;
#1228=CARTESIAN_POINT ( 'NONE',  ( -2.940577200613229358, -11.38371329336536242, -1.743664497973003158 ) ) ;
#1232=CARTESIAN_POINT ( 'NONE',  ( 6.669411210323004546, -6.378078458904371750, -1.500000000000000000 ) ) ;
#1236=CIRCLE ( 'NONE', #3911, 6.000000000000001776 ) ;
#1248=DIRECTION ( 'NONE',  ( 0.000000000000000000, -0.000000000000000000, -1.000000000000000000 ) ) ;
#1252=VECTOR ( 'NONE', #5654, 1000.000000000000114 ) ;
#1257=DIRECTION ( 'NONE',  ( -0.4030398059120889331, -0.9151824489413822317, 5.627812144739313658E-15 ) ) ;
#1263=CARTESIAN_POINT ( 'NONE',  ( 24.57728726453494517, -17.46986644506281650, -1.411007141442706114 ) ) ;
#1265=VECTOR ( 'NONE', #16366, 1000.000000000000000 ) ;
#1273=CARTESIAN_POINT ( 'NONE',  ( 6.448894291894883501, -17.04229596238074507, 4.522129901861158707 ) ) ;
#1281=CARTESIAN_POINT ( 'NONE',  ( 108.0612880515141683, -18.95189481187503588, 4.515510177595837504 ) ) ;
#1283=CARTESIAN_POINT ( 'NONE',  ( 42.88108885377458535, -22.62752020922543750, -4.522129901861166701 ) ) ;
#1285=DIRECTION ( 'NONE',  ( -0.000000000000000000, -0.000000000000000000, 1.000000000000000000 ) ) ;
#1288=EDGE_CURVE ( 'NONE', #10646, #9547, #31984, .T. ) ;
#1296=EDGE_LOOP ( 'NONE', ( #7344, #2499, #27989 ) ) ;
#1300=CYLINDRICAL_SURFACE ( 'NONE', #11941, 0.5000000000000007772 ) ;
#1302=VERTEX_POINT ( 'NONE', #30546 ) ;
#1303=CARTESIAN_POINT ( 'NONE',  ( -17.45597128428593336, -28.43932300454937590, 11.00000000000000000 ) ) ;
#1304=EDGE_CURVE ( 'NONE', #7488, #29208, #32077, .T. ) ;
#1305=( BOUNDED_SURFACE ( )  B_SPLINE_SURFACE ( 3, 2, ( 
 ( #24739, #12041, #29607 ),
 ( #17027, #27233, #4350 ),
 ( #11383, #4530, #8343 ),
 ( #665, #23875, #13513 ) ),
 .UNSPECIFIED., .F., .F., .F. ) 
 B_SPLINE_SURFACE_WITH_KNOTS ( ( 4, 4 ),
 ( 3, 3 ),
 ( 0.003700663664647922940, 0.007131426728608055571 ),
 ( 0.000000000000000000, 1.000000000000000000 ),
 .UNSPECIFIED. ) 
 GEOMETRIC_REPRESENTATION_ITEM ( )  RATIONAL_B_SPLINE_SURFACE ( (
 ( 1.000000000000000000, 0.7067603058644310599, 1.000000000000000000),
 ( 1.000000000000000000, 0.7067606020011648615, 1.000000000000000000),
 ( 1.000000000000000000, 0.7067612639882160375, 1.000000000000000000),
 ( 1.000000000000000000, 0.7067623105831786212, 1.000000000000000000) ) ) 
 REPRESENTATION_ITEM ( '' )  SURFACE ( )  );
#1308=CARTESIAN_POINT ( 'NONE',  ( 1.872983491663670286, -10.12226979866639809, 1.499999999999999556 ) ) ;
#1316=LINE ( 'NONE', #8818, #3838 ) ;
#1330=CIRCLE ( 'NONE', #28556, 0.5000000000000004441 ) ;
#1332=PLANE ( 'NONE',  #680 ) ;
#1333=CARTESIAN_POINT ( 'NONE',  ( -2.092582746845476738, -9.051626392537004406, 5.485967528433935314 ) ) ;
#1353=ORIENTED_EDGE ( 'NONE', *, *, #11804, .F. ) ;
#1364=CARTESIAN_POINT ( 'NONE',  ( -14.62340757463330654, -21.93932300455827900, -1.000000000000000000 ) ) ;
#1365=EDGE_LOOP ( 'NONE', ( #10471, #2774, #2252, #29150 ) ) ;
#1369=CARTESIAN_POINT ( 'NONE',  ( 25.47590243882417482, -17.55751406896973421, 1.147657757683672619 ) ) ;
#1371=FACE_OUTER_BOUND ( 'NONE', #4290, .T. ) ;
#1386=FACE_OUTER_BOUND ( 'NONE', #22890, .T. ) ;
#1391=CARTESIAN_POINT ( 'NONE',  ( 107.6641398346956890, -20.45810202417174750, -1.499999999999999556 ) ) ;
#1392=CARTESIAN_POINT ( 'NONE',  ( 107.3753443242040362, -16.28466752050562505, 2.316915192227371190 ) ) ;
#1393=ORIENTED_EDGE ( 'NONE', *, *, #16236, .F. ) ;
#1398=CARTESIAN_POINT ( 'NONE',  ( 13.25896750271661517, -14.28336940137728739, -1.500000000000000000 ) ) ;
#1399=CARTESIAN_POINT ( 'NONE',  ( 108.0017345319158295, -18.09433894470946314, -4.637781146201932714 ) ) ;
#1404=LINE ( 'NONE', #29654, #8270 ) ;
#1415=CARTESIAN_POINT ( 'NONE',  ( 21.21813830868036632, -21.75718202030900983, -1.395944860339461968 ) ) ;
#1417=CARTESIAN_POINT ( 'NONE',  ( 4.129790720829305428, -11.96909370240749482, -1.499999999999999556 ) ) ;
#1420=CARTESIAN_POINT ( 'NONE',  ( 25.43628654896174623, -17.54453578616395149, -1.000000000000000222 ) ) ;
#1428=CARTESIAN_POINT ( 'NONE',  ( 3.554613218822866294, -15.76807188677689631, 4.522129901861158707 ) ) ;
#1432=CARTESIAN_POINT ( 'NONE',  ( 24.80306213860490061, -17.49230408913781787, -1.500000000000000000 ) ) ;
#1437=CARTESIAN_POINT ( 'NONE',  ( -2.819379691724354764, -6.927609664243463250, -4.522129901861166701 ) ) ;
#1450=CARTESIAN_POINT ( 'NONE',  ( 23.05582502382718602, -21.92970400627778460, -1.098154049131486509 ) ) ;
#1452=CARTESIAN_POINT ( 'NONE',  ( 7.154313483739771939, -6.723190066291747868, 1.000000000000000000 ) ) ;
#1454=CARTESIAN_POINT ( 'NONE',  ( 7.085399849431443187, -9.284427924817668654, -1.500000000000000444 ) ) ;
#1456=CARTESIAN_POINT ( 'NONE',  ( 3.073984382316905961, -11.22322413323466606, 1.500000000000000444 ) ) ;
#1467=B_SPLINE_CURVE_WITH_KNOTS ( 'NONE', 3,
 ( #3439, #26801, #31836, #31989, #23803, #13598, #8905, #6391, #16591, #16778 ),
 .UNSPECIFIED., .F., .F.,
 ( 4, 3, 3, 4 ),
 ( 1.734723475976807094E-18, 0.001000000000055348759, 0.002000000000112648647, 0.003363950672716857146 ),
 .UNSPECIFIED. ) ;
#1469=CARTESIAN_POINT ( 'NONE',  ( -2.617344628312510135, 0.000000000000000000, 1.468739241856748867 ) ) ;
#1474=LINE ( 'NONE', #19360, #22064 ) ;
#1476=CARTESIAN_POINT ( 'NONE',  ( 6.448894291894883501, -17.04229596238074151, -4.522129901861166701 ) ) ;
#1481=CARTESIAN_POINT ( 'NONE',  ( 24.73879325185242095, -17.41122989233535634, -1.266732818455850618 ) ) ;
#1498=CARTESIAN_POINT ( 'NONE',  ( 7.433516504560094162, -4.668991481927904807, -1.000000000000000000 ) ) ;
#1506=CARTESIAN_POINT ( 'NONE',  ( 2.821167764927612343, -11.54352467686084616, -1.759796262541038159 ) ) ;
#1515=CARTESIAN_POINT ( 'NONE',  ( -15.00903914005711925, -21.93932300455818307, 1.032046942684759161 ) ) ;
#1518=CARTESIAN_POINT ( 'NONE',  ( 21.03177542174608661, -17.18603084754167298, 1.753176640694532162 ) ) ;
#1523=CARTESIAN_POINT ( 'NONE',  ( -4.184206142744113066, -5.072448364080297090, -1.499999999999959366 ) ) ;
#1537=DIRECTION ( 'NONE',  ( 0.9975973382524639943, 0.06927878976713691683, -8.540109289633579845E-19 ) ) ;
#1541=DIRECTION ( 'NONE',  ( -0.7071067811865467956, 8.659560562354925463E-17, 0.7071067811865483499 ) ) ;
#1544=CARTESIAN_POINT ( 'NONE',  ( 0.2309143942741746225, -15.52425963734929404, -1.499999999999999778 ) ) ;
#1549=CARTESIAN_POINT ( 'NONE',  ( 7.650166298460330694, -9.403575860117920016, -1.500000000000286438 ) ) ;
#1550=CARTESIAN_POINT ( 'NONE',  ( 107.9747431708452012, -17.70567005987862785, -5.016769268009813487 ) ) ;
#1560=CARTESIAN_POINT ( 'NONE',  ( -23.35000000000000142, -10.96966150227469505, -1.499999999999999556 ) ) ;
#1563=CARTESIAN_POINT ( 'NONE',  ( 2.802272078496797825, -0.3634031030573144361, -1.485394228827264351 ) ) ;
#1568=ORIENTED_EDGE ( 'NONE', *, *, #19353, .F. ) ;
#1583=B_SPLINE_CURVE_WITH_KNOTS ( 'NONE', 3,
 ( #26620, #5892, #8410, #28794, #13404, #6077, #23791, #21280, #19102, #18772, #3724, #20963, #31333, #748, #31479, #26478, #21616, #31183, #1228, #3243, #8265, #11421, #16081, #18457, #6376, #26311, #3424, #8561, #29290, #26784, #28977, #3577 ),
 .UNSPECIFIED., .F., .F.,
 ( 4, 2, 2, 2, 2, 2, 2, 2, 2, 2, 2, 2, 2, 2, 2, 4 ),
 ( 0.09044956997018868683, 0.09470617999383536267, 0.09896279001748202464, 0.1032194000411287005, 0.1074760100647753763, 0.1085401625706870349, 0.1096043150765987073, 0.1117326200884220522, 0.1127967725943337107, 0.1138609251002453970, 0.1149250776061570556, 0.1159892301120687419, 0.1181175351238920868, 0.1191816876298037453, 0.1202458401357154177, 0.1245024501593621075 ),
 .UNSPECIFIED. ) ;
#1587=CIRCLE ( 'NONE', #29865, 0.5000000000000004441 ) ;
#1588=CARTESIAN_POINT ( 'NONE',  ( 3.551765900376503193, -15.35947713381494673, -5.485967528433938867 ) ) ;
#1596=EDGE_LOOP ( 'NONE', ( #5955, #19738, #3255, #12058 ) ) ;
#1603=CARTESIAN_POINT ( 'NONE',  ( 8.690022415558827262, -0.1784382875756478082, 1.500000000000000000 ) ) ;
#1609=CARTESIAN_POINT ( 'NONE',  ( 0.2309801563857631079, -6.520475440346420903, 1.500000000000070388 ) ) ;
#1613=CARTESIAN_POINT ( 'NONE',  ( 9.266707753004491011, -0.05004968855533440536, -1.221243012139963779 ) ) ;
#1616=CARTESIAN_POINT ( 'NONE',  ( 24.37248106195859876, -17.41561295274971499, -1.432003413859580965 ) ) ;
#1620=EDGE_CURVE ( 'NONE', #32817, #4832, #29019, .T. ) ;
#1624=CARTESIAN_POINT ( 'NONE',  ( 23.14329945973239333, -21.92788238883852259, -1.164089052066207941 ) ) ;
#1632=CARTESIAN_POINT ( 'NONE',  ( 17.97422212135272446, -19.86246923125032282, -4.522129901861166701 ) ) ;
#1652=ORIENTED_EDGE ( 'NONE', *, *, #5719, .T. ) ;
#1663=EDGE_CURVE ( 'NONE', #12973, #12534, #8780, .T. ) ;
#1668=CARTESIAN_POINT ( 'NONE',  ( 3.920802734502714770, -12.31850478943684557, -1.757814695358448365 ) ) ;
#1678=ORIENTED_EDGE ( 'NONE', *, *, #14870, .T. ) ;
#1680=AXIS2_PLACEMENT_3D ( 'NONE', #18385, #3337, #5674 ) ;
#1682=AXIS2_PLACEMENT_3D ( 'NONE', #2754, #7773, #559 ) ;
#1685=ADVANCED_FACE ( 'NONE', ( #30646 ), #28442, .T. ) ;
#1687=FACE_OUTER_BOUND ( 'NONE', #21236, .T. ) ;
#1695=CARTESIAN_POINT ( 'NONE',  ( 21.19329141388212534, -21.80292992253753326, 1.345625751490156174 ) ) ;
#1700=ORIENTED_EDGE ( 'NONE', *, *, #28290, .T. ) ;
#1705=VERTEX_POINT ( 'NONE', #15735 ) ;
#1707=ADVANCED_FACE ( 'NONE', ( #7532 ), #3073, .T. ) ;
#1710=ORIENTED_EDGE ( 'NONE', *, *, #26107, .F. ) ;
#1711=TOROIDAL_SURFACE ( 'NONE', #15052, 6.500000000000002665, 0.5000000000000000000 ) ;
#1720=CARTESIAN_POINT ( 'NONE',  ( 9.037136197878623989, -11.91234824294515704, -1.500000000000000000 ) ) ;
#1721=CARTESIAN_POINT ( 'NONE',  ( 108.0346010918886890, -18.56760923201772329, -5.018359539779770451 ) ) ;
#1729=AXIS2_PLACEMENT_3D ( 'NONE', #29887, #1985, #18577 ) ;
#1734=AXIS2_PLACEMENT_3D ( 'NONE', #23832, #3135, #10802 ) ;
#1740=CARTESIAN_POINT ( 'NONE',  ( -55.59999999999999432, -10.96966150227468972, 1.500000000000000000 ) ) ;
#1746=EDGE_CURVE ( 'NONE', #15957, #28480, #32106, .T. ) ;
#1748=ORIENTED_EDGE ( 'NONE', *, *, #7674, .T. ) ;
#1752=CARTESIAN_POINT ( 'NONE',  ( 17.39502519979081185, -21.04076415203811479, -1.751145182513948573 ) ) ;
#1761=CARTESIAN_POINT ( 'NONE',  ( -1.218076164763124636, -14.00532792343563848, -1.500000000000000000 ) ) ;
#1770=CARTESIAN_POINT ( 'NONE',  ( -2.408800074497261079, -5.498703686517334432, -5.485967528433938867 ) ) ;
#1779=AXIS2_PLACEMENT_3D ( 'NONE', #14596, #14098, #9407 ) ;
#1796=CARTESIAN_POINT ( 'NONE',  ( 18.46877649744746819, -16.82957494019613520, 1.753327325565563921 ) ) ;
#1798=CARTESIAN_POINT ( 'NONE',  ( 107.3476768466457401, -15.88628154573096651, 1.500000000000000000 ) ) ;
#1801=CARTESIAN_POINT ( 'NONE',  ( -4.181783187175765804, -9.389479943443376442, 1.500000000000000000 ) ) ;
#1803=AXIS2_PLACEMENT_3D ( 'NONE', #12447, #22662, #7414 ) ;
#1811=CARTESIAN_POINT ( 'NONE',  ( -3.222375984151269357, 0.000000000000000000, 1.000000000000000000 ) ) ;
#1812=CARTESIAN_POINT ( 'NONE',  ( 23.22050010672911569, -21.93619796768840047, -1.062839084286906211 ) ) ;
#1824=PRODUCT_DEFINITION_FORMATION_WITH_SPECIFIED_SOURCE ( 'ANY', '', #4694, .NOT_KNOWN. ) ;
#1826=CARTESIAN_POINT ( 'NONE',  ( 25.38257154049698272, -17.53428803818666992, -1.078154016645389790 ) ) ;
#1840=CARTESIAN_POINT ( 'NONE',  ( 2.342933509396896152, -0.1895978275999587181, 1.757325986342921587 ) ) ;
#1858=CARTESIAN_POINT ( 'NONE',  ( 1.563235467773296250, -10.39397044182024921, -1.763951029879659460 ) ) ;
#1869=ADVANCED_FACE ( 'NONE', ( #861 ), #16027, .T. ) ;
#1872=EDGE_CURVE ( 'NONE', #30338, #9983, #20082, .T. ) ;
#1875=CARTESIAN_POINT ( 'NONE',  ( 2.226843223301624430, -16.57429286563273862, -1.499999999999679146 ) ) ;
#1897=EDGE_CURVE ( 'NONE', #10078, #7472, #22848, .T. ) ;
#1902=CARTESIAN_POINT ( 'NONE',  ( 23.22564588060097890, -22.38932300456763969, 1.000000000000000000 ) ) ;
#1904=FACE_OUTER_BOUND ( 'NONE', #28144, .T. ) ;
#1906=CARTESIAN_POINT ( 'NONE',  ( 107.9489733406790037, -17.33459091623378256, -4.544509996648006478 ) ) ;
#1907=EDGE_LOOP ( 'NONE', ( #20317, #8545, #22276, #29830 ) ) ;
#1923=CARTESIAN_POINT ( 'NONE',  ( 2.913020537602763582, 0.09936728819754167552, -1.050862340634153291 ) ) ;
#1925=DIRECTION ( 'NONE',  ( 0.000000000000000000, -1.000000000000000000, 0.000000000000000000 ) ) ;
#1931=ORIENTED_EDGE ( 'NONE', *, *, #14870, .F. ) ;
#1933=VERTEX_POINT ( 'NONE', #32095 ) ;
#1937=ORIENTED_EDGE ( 'NONE', *, *, #28996, .F. ) ;
#1941=CARTESIAN_POINT ( 'NONE',  ( 108.0981717737594749, -19.48301123669095247, 2.289311975388307108 ) ) ;
#1942=CARTESIAN_POINT ( 'NONE',  ( -1.921189184902703406, -10.44034746380417289, -4.522129901861166701 ) ) ;
#1946=DIRECTION ( 'NONE',  ( -1.000000000000000000, 0.000000000000000000, 0.000000000000000000 ) ) ;
#1947=CARTESIAN_POINT ( 'NONE',  ( -1.824298235657122902, -2.866444442092977329, 5.485967528433935314 ) ) ;
#1962=CARTESIAN_POINT ( 'NONE',  ( 12.13210218395027162, -15.56661508947843764, 1.754034462302825892 ) ) ;
#1972=CARTESIAN_POINT ( 'NONE',  ( 23.25968158267518149, -21.94039639562157618, -1.058068363327190564 ) ) ;
#1983=CARTESIAN_POINT ( 'NONE',  ( 24.54848581754903236, -17.37474206563366508, -1.294224261558855060 ) ) ;
#1984=CARTESIAN_POINT ( 'NONE',  ( -23.35000000000000142, -10.96966150227469505, -11.50000000000000000 ) ) ;
#1985=DIRECTION ( 'NONE',  ( -0.9873162094019954926, 0.1587661886299326364, 1.242416025591495175E-13 ) ) ;
#2008=CARTESIAN_POINT ( 'NONE',  ( 0.2521526662550623299, -7.034850097465708885, -1.499999999999965139 ) ) ;
#2025=CARTESIAN_POINT ( 'NONE',  ( 3.379177507580384709, -17.49396809222194094, -1.499999999999999112 ) ) ;
#2035=DIRECTION ( 'NONE',  ( -0.1908089953765452484, 0.000000000000000000, 0.9816271834476638647 ) ) ;
#2045=CARTESIAN_POINT ( 'NONE',  ( 10.18192333485687406, -19.96327110613152556, -1.499999999999998890 ) ) ;
#2052=CARTESIAN_POINT ( 'NONE',  ( 108.0105747311263258, -18.22163561417639954, -4.627746478616681536 ) ) ;
#2061=CARTESIAN_POINT ( 'NONE',  ( -3.135269660805079628, -0.5000000000000013323, -1.500000000000000000 ) ) ;
#2083=FACE_OUTER_BOUND ( 'NONE', #20688, .T. ) ;
#2090=CARTESIAN_POINT ( 'NONE',  ( 107.9808716746043160, -17.79391898944944117, -4.343976358951705308 ) ) ;
#2091=DIRECTION ( 'NONE',  ( -0.000000000000000000, -0.000000000000000000, -1.000000000000000000 ) ) ;
#2098=EDGE_LOOP ( 'NONE', ( #27076, #14372 ) ) ;
#2104=DIRECTION ( 'NONE',  ( 1.000000000000000000, 0.000000000000000000, 0.000000000000000000 ) ) ;
#2107=CARTESIAN_POINT ( 'NONE',  ( 9.015741301869967472, -14.64812015776037235, 1.754831107654766909 ) ) ;
#2118=CARTESIAN_POINT ( 'NONE',  ( 107.4811544939907293, -15.87715700148073239, -1.499966567242897009 ) ) ;
#2126=CARTESIAN_POINT ( 'NONE',  ( -1.921189184902703406, -10.44034746380417289, -4.522129901861166701 ) ) ;
#2127=CARTESIAN_POINT ( 'NONE',  ( -14.63259398290947289, -21.93932300455829676, -0.9045955023117272509 ) ) ;
#2134=CIRCLE ( 'NONE', #16517, 0.5000000000000000000 ) ;
#2137=ORIENTED_EDGE ( 'NONE', *, *, #17572, .F. ) ;
#2142=CARTESIAN_POINT ( 'NONE',  ( 0.1913146712875998523, -7.518111206453180984, 1.774246272807403768 ) ) ;
#2150=EDGE_CURVE ( 'NONE', #10646, #11, #7704, .T. ) ;
#2161=CARTESIAN_POINT ( 'NONE',  ( 0.2669967855539195911, -7.206639073886805136, -1.500000000000035083 ) ) ;
#2162=CARTESIAN_POINT ( 'NONE',  ( -1.047937531484010476, -4.989690239014954010, 4.522129901861157819 ) ) ;
#2165=CARTESIAN_POINT ( 'NONE',  ( 0.000000000000000000, -0.5000000000000000000, 1.000000000000000000 ) ) ;
#2179=CARTESIAN_POINT ( 'NONE',  ( -3.000167615074412097, -11.27277999132675923, -1.743644601730333532 ) ) ;
#2181=CIRCLE ( 'NONE', #20865, 4.499999999999997335 ) ;
#2184=CARTESIAN_POINT ( 'NONE',  ( 107.9497830788478296, -17.34625094442536408, 4.563380564801009065 ) ) ;
#2188=EDGE_CURVE ( 'NONE', #28886, #9056, #31197, .T. ) ;
#2203=DIRECTION ( 'NONE',  ( 1.000000000000000000, 0.000000000000000000, 0.000000000000000000 ) ) ;
#2211=CARTESIAN_POINT ( 'NONE',  ( 9.283830569141848343, -0.1241467202047346063, -1.000000000000000000 ) ) ;
#2212=CARTESIAN_POINT ( 'NONE',  ( 107.6641398346956890, -20.45810202417174750, -1.499999999999999556 ) ) ;
#2218=ADVANCED_FACE ( 'NONE', ( #11149 ), #13498, .F. ) ;
#2228=ORIENTED_EDGE ( 'NONE', *, *, #31560, .F. ) ;
#2237=ORIENTED_EDGE ( 'NONE', *, *, #13779, .T. ) ;
#2239=CARTESIAN_POINT ( 'NONE',  ( 1.998430852895130228, -1.623920106752339221, -1.500000000000000444 ) ) ;
#2249=ORIENTED_EDGE ( 'NONE', *, *, #27712, .T. ) ;
#2251=EDGE_CURVE ( 'NONE', #7955, #11449, #29580, .T. ) ;
#2252=ORIENTED_EDGE ( 'NONE', *, *, #26390, .F. ) ;
#2254=CARTESIAN_POINT ( 'NONE',  ( 41.06247019076344884, -19.55897407381494091, 1.500000000000000000 ) ) ;
#2265=CARTESIAN_POINT ( 'NONE',  ( 25.06773407388143582, -17.47416606015757878, 1.197364706238863263 ) ) ;
#2283=DIRECTION ( 'NONE',  ( -0.000000000000000000, -0.000000000000000000, 1.000000000000000000 ) ) ;
#2285=CARTESIAN_POINT ( 'NONE',  ( 107.9601777634633635, -17.49593181718839574, 4.828277428366157586 ) ) ;
#2288=CARTESIAN_POINT ( 'NONE',  ( 9.144569539486429477, -14.26359586708033156, 1.499999999999999112 ) ) ;
#2292=CARTESIAN_POINT ( 'NONE',  ( 10.18185458677248967, -19.96325353452428786, 1.499999999999999778 ) ) ;
#2298=CARTESIAN_POINT ( 'NONE',  ( 107.6149215477164205, -15.92400613423469302, -1.487010776595593331 ) ) ;
#2299=CARTESIAN_POINT ( 'NONE',  ( 21.43024762280364470, -21.75451284338814162, -1.453503648288084760 ) ) ;
#2301=EDGE_CURVE ( 'NONE', #5840, #28620, #26805, .T. ) ;
#2302=VERTEX_POINT ( 'NONE', #11644 ) ;
#2305=B_SPLINE_CURVE_WITH_KNOTS ( 'NONE', 3,
 ( #18952, #8893, #26314, #16574, #4067, #21446, #5893, #11422, #26621, #23940, #8746, #21768, #8411 ),
 .UNSPECIFIED., .F., .F.,
 ( 4, 3, 3, 3, 4 ),
 ( 1.301042606982605513E-18, 0.0005988814224540803992, 0.001512661714883095426, 0.002883332157778191723, 0.003274339315335596419 ),
 .UNSPECIFIED. ) ;
#2309=B_SPLINE_CURVE_WITH_KNOTS ( 'NONE', 3,
 ( #13115, #20655, #20803, #15791 ),
 .UNSPECIFIED., .F., .F.,
 ( 4, 4 ),
 ( 0.000000000000000000, 2.202191994273081657E-08 ),
 .UNSPECIFIED. ) ;
#2319=CARTESIAN_POINT ( 'NONE',  ( 22.65740490676230579, -21.90673157959312434, 1.180310388834064028 ) ) ;
#2328=ADVANCED_FACE ( 'NONE', ( #9307 ), #24354, .T. ) ;
#2330=CARTESIAN_POINT ( 'NONE',  ( 2.482257818914018088, 0.000000000000000000, -1.712210361609936005 ) ) ;
#2331=CARTESIAN_POINT ( 'NONE',  ( 2.410813113191278223, -0.09135288944859165650, 1.740945950647664331 ) ) ;
#2338=AXIS2_PLACEMENT_3D ( 'NONE', #11838, #22363, #29393 ) ;
#2344=CARTESIAN_POINT ( 'NONE',  ( 72.90878003214282899, -18.24052684336788488, -1.499999999999999556 ) ) ;
#2347=ORIENTED_EDGE ( 'NONE', *, *, #10593, .F. ) ;
#2352=CARTESIAN_POINT ( 'NONE',  ( 21.03177542174492487, -17.18603084754148469, -1.753176640694678712 ) ) ;
#2353=CARTESIAN_POINT ( 'NONE',  ( 3.527557386959605967, -11.88551672347146848, 0.9788672205888330202 ) ) ;
#2363=AXIS2_PLACEMENT_3D ( 'NONE', #27858, #7809, #30226 ) ;
#2371=CARTESIAN_POINT ( 'NONE',  ( -0.1324184762035490182, -14.88641855047732143, -1.499999999999879874 ) ) ;
#2395=CARTESIAN_POINT ( 'NONE',  ( 6.220890055303850197, -15.20372210278348035, 4.522129901861156931 ) ) ;
#2402=EDGE_CURVE ( 'NONE', #7529, #22183, #5682, .T. ) ;
#2405=DIRECTION ( 'NONE',  ( -0.000000000000000000, 0.000000000000000000, 1.000000000000000000 ) ) ;
#2407=DIRECTION ( 'NONE',  ( 0.000000000000000000, 0.000000000000000000, 1.000000000000000000 ) ) ;
#2416=CARTESIAN_POINT ( 'NONE',  ( -2.617344628312510135, 0.000000000000000000, 1.468739241856748867 ) ) ;
#2418=CARTESIAN_POINT ( 'NONE',  ( 108.6155529559672885, -15.79924867777639186, -1.500000000000000444 ) ) ;
#2420=CARTESIAN_POINT ( 'NONE',  ( 14.14625720941031339, -14.08932802803050066, 0.9999999999999995559 ) ) ;
#2424=VERTEX_POINT ( 'NONE', #12641 ) ;
#2425=CARTESIAN_POINT ( 'NONE',  ( -2.861038829132344752, 0.01832029024769343817, 1.013940918434999672 ) ) ;
#2431=ORIENTED_EDGE ( 'NONE', *, *, #23196, .F. ) ;
#2433=CARTESIAN_POINT ( 'NONE',  ( 12.65465643788354200, -15.70291107026620914, -1.500000000000000000 ) ) ;
#2435=CARTESIAN_POINT ( 'NONE',  ( 3.403631140498738272, -11.97511429332634947, -1.758598531020624467 ) ) ;
#2437=CARTESIAN_POINT ( 'NONE',  ( 22.92640216610100623, -21.90430348730661692, -1.195188340063571886 ) ) ;
#2442=CARTESIAN_POINT ( 'NONE',  ( 25.10129074172987274, -17.52164282029619358, 1.281897516810119209 ) ) ;
#2443=EDGE_CURVE ( 'NONE', #22183, #13510, #28012, .T. ) ;
#2444=ADVANCED_FACE ( 'NONE', ( #4633 ), #10309, .T. ) ;
#2458=EDGE_CURVE ( 'NONE', #24580, #4070, #22014, .T. ) ;
#2464=ORIENTED_EDGE ( 'NONE', *, *, #14920, .F. ) ;
#2469=EDGE_LOOP ( 'NONE', ( #16835, #18940, #12887, #30734 ) ) ;
#2471=LINE ( 'NONE', #23340, #24041 ) ;
#2473=CARTESIAN_POINT ( 'NONE',  ( 21.38384797955244565, -21.75816543643470169, -1.434735962053344416 ) ) ;
#2476=DIRECTION ( 'NONE',  ( 1.000000000000000000, 0.000000000000000000, 0.000000000000000000 ) ) ;
#2485=CARTESIAN_POINT ( 'NONE',  ( 22.49117028854453793, -21.89694127986719963, 1.202706146049940639 ) ) ;
#2492=CARTESIAN_POINT ( 'NONE',  ( 8.184049377293504790, -14.35829901518298435, 1.755177411681289712 ) ) ;
#2495=CARTESIAN_POINT ( 'NONE',  ( -31.59999999999999787, -25.93932300454937945, 1.500000000000000000 ) ) ;
#2496=EDGE_CURVE ( 'NONE', #17041, #12973, #604, .T. ) ;
#2499=ORIENTED_EDGE ( 'NONE', *, *, #29364, .T. ) ;
#2503=FACE_BOUND ( 'NONE', #5219, .T. ) ;
#2506=EDGE_LOOP ( 'NONE', ( #21648, #5634, #16217 ) ) ;
#2511=CARTESIAN_POINT ( 'NONE',  ( 14.73499698773293787, -15.74765953506444838, -1.500000000000000000 ) ) ;
#2512=CARTESIAN_POINT ( 'NONE',  ( 12.57238041616097313, -15.42470150510370530, 0.9788672205888330202 ) ) ;
#2516=DIRECTION ( 'NONE',  ( -0.000000000000000000, 0.000000000000000000, 1.000000000000000000 ) ) ;
#2520=VERTEX_POINT ( 'NONE', #18150 ) ;
#2526=CARTESIAN_POINT ( 'NONE',  ( -1.397888388080156474, -14.12209114206489957, -1.500000000000000444 ) ) ;
#2543=CARTESIAN_POINT ( 'NONE',  ( -2.962992063741595405, -11.77309494928644185, -1.500000000000000000 ) ) ;
#2549=ORIENTED_EDGE ( 'NONE', *, *, #10611, .F. ) ;
#2553=CARTESIAN_POINT ( 'NONE',  ( -4.524743775585262640, -7.612468530177983972, 1.499999999999999556 ) ) ;
#2556=ORIENTED_EDGE ( 'NONE', *, *, #26972, .F. ) ;
#2562=CARTESIAN_POINT ( 'NONE',  ( 17.99869063402067226, -21.49583829453746731, -1.499999999999980904 ) ) ;
#2568=( BOUNDED_CURVE ( )  B_SPLINE_CURVE ( 3, ( #12890, #26105, #8235, #5571 ),
 .UNSPECIFIED., .F., .F. ) 
 B_SPLINE_CURVE_WITH_KNOTS ( ( 4, 4 ),
 ( 4.520402762665447050, 4.712388980384689674 ),
 .UNSPECIFIED. ) 
 CURVE ( )  GEOMETRIC_REPRESENTATION_ITEM ( )  RATIONAL_B_SPLINE_CURVE ( ( 1.000000000000000000, 0.9969307989114568613, 0.9969307989114568613, 1.000000000000000000 ) ) 
 REPRESENTATION_ITEM ( '' )  );
#2571=CARTESIAN_POINT ( 'NONE',  ( 0.8032528114568866506, -4.297275870435939282, -0.9788672205888330202 ) ) ;
#2573=CARTESIAN_POINT ( 'NONE',  ( 11.84970817546995114, -13.11509834239990013, 1.000000000000000222 ) ) ;
#2575=EDGE_CURVE ( 'NONE', #31833, #21433, #15960, .T. ) ;
#2580=CARTESIAN_POINT ( 'NONE',  ( -3.086647630617488147, -0.4418915582519432617, 1.500000000000000222 ) ) ;
#2589=CARTESIAN_POINT ( 'NONE',  ( 22.54151439274422941, -21.86162235810806109, -1.385141676428145452 ) ) ;
#2591=CARTESIAN_POINT ( 'NONE',  ( 107.8922813183675089, -16.51823989814691629, 1.728346180483987027 ) ) ;
#2593=CARTESIAN_POINT ( 'NONE',  ( 15.98687768421490674, -15.99250810535818701, 1.500000000000000444 ) ) ;
#2595=CARTESIAN_POINT ( 'NONE',  ( -0.1366093623685602776, -14.96249823008941604, 1.500000000000000000 ) ) ;
#2605=CARTESIAN_POINT ( 'NONE',  ( 20.08514749461435400, -21.49093168682445310, -1.640482353827673601 ) ) ;
#2609=EDGE_CURVE ( 'NONE', #9843, #9922, #463, .T. ) ;
#2613=CARTESIAN_POINT ( 'NONE',  ( 111.3844470440328251, -20.20075132222358505, -1.499999999999999556 ) ) ;
#2617=CARTESIAN_POINT ( 'NONE',  ( 14.60942776824126632, -20.56080517165843347, 1.750898333654289596 ) ) ;
#2619=CARTESIAN_POINT ( 'NONE',  ( 108.0105480239282372, -18.22125103716771832, -4.637810049791077915 ) ) ;
#2625=CARTESIAN_POINT ( 'NONE',  ( 107.6641398346957033, -20.45810202417174750, 1.500000000000000000 ) ) ;
#2628=VERTEX_POINT ( 'NONE', #21172 ) ;
#2630=DIRECTION ( 'NONE',  ( -0.1908089953765452762, 0.000000000000000000, 0.9816271834476639757 ) ) ;
#2632=DIRECTION ( 'NONE',  ( 0.000000000000000000, 0.000000000000000000, -1.000000000000000000 ) ) ;
#2636=CARTESIAN_POINT ( 'NONE',  ( -17.45597128428593336, -25.93932300454937945, 11.00000000000000000 ) ) ;
#2643=CARTESIAN_POINT ( 'NONE',  ( 1.942333353379948502, -0.8689713362383969519, 1.758041117768017747 ) ) ;
#2644=CARTESIAN_POINT ( 'NONE',  ( 10.63777811968352971, -12.44241537618772320, 1.500000000000427658 ) ) ;
#2656=ORIENTED_EDGE ( 'NONE', *, *, #17503, .F. ) ;
#2663=CARTESIAN_POINT ( 'NONE',  ( 13.13178786249840435, -17.31629153505178920, 4.522129901861157819 ) ) ;
#2666=CYLINDRICAL_SURFACE ( 'NONE', #24057, 0.5000000000000000000 ) ;
#2667=AXIS2_PLACEMENT_3D ( 'NONE', #9755, #255, #63 ) ;
#2669=LINE ( 'NONE', #17534, #13389 ) ;
#2671=CARTESIAN_POINT ( 'NONE',  ( 24.43445557112933386, -17.40480440763387904, 1.396984404749296971 ) ) ;
#2672=VERTEX_POINT ( 'NONE', #3614 ) ;
#2683=CARTESIAN_POINT ( 'NONE',  ( 107.8460215217088773, -15.85211033425178861, 1.499787059522396770 ) ) ;
#2691=ORIENTED_EDGE ( 'NONE', *, *, #302, .T. ) ;
#2699=CARTESIAN_POINT ( 'NONE',  ( 3.566513200368869096, -17.47573827932033197, 1.500000000000000000 ) ) ;
#2707=CARTESIAN_POINT ( 'NONE',  ( -3.817309019801226722, -10.46513237797910989, 1.499999999999999112 ) ) ;
#2711=CARTESIAN_POINT ( 'NONE',  ( 108.0290687835694854, -18.48794536861594295, -4.329972080810385648 ) ) ;
#2716=AXIS2_PLACEMENT_3D ( 'NONE', #26094, #3053, #368 ) ;
#2723=VECTOR ( 'NONE', #5734, 1000.000000000000000 ) ;
#2725=CARTESIAN_POINT ( 'NONE',  ( 22.52203367452178995, -21.86037836540916146, 1.500000000000000000 ) ) ;
#2726=CARTESIAN_POINT ( 'NONE',  ( 108.0291781248179177, -18.48951985539285658, 4.325670280512381005 ) ) ;
#2727=CARTESIAN_POINT ( 'NONE',  ( 107.4934131274682869, -17.99000828170487765, -5.121421805061605603 ) ) ;
#2729=EDGE_CURVE ( 'NONE', #25210, #29208, #21496, .T. ) ;
#2730=DIRECTION ( 'NONE',  ( 0.000000000000000000, 0.000000000000000000, -1.000000000000000000 ) ) ;
#2736=ORIENTED_EDGE ( 'NONE', *, *, #15816, .F. ) ;
#2742=CARTESIAN_POINT ( 'NONE',  ( 107.5502113151021177, -18.81587173190781215, 4.846782049358179911 ) ) ;
#2749=CIRCLE ( 'NONE', #31025, 0.5000000000000004441 ) ;
#2750=CARTESIAN_POINT ( 'NONE',  ( 1.278428506419904798, -2.392608122357158251, -1.500000000000000000 ) ) ;
#2753=CARTESIAN_POINT ( 'NONE',  ( 6.920196482735073928, -13.86306298490376143, -1.755640868487531758 ) ) ;
#2754=CARTESIAN_POINT ( 'NONE',  ( -29.24402871571405882, -25.93932300454937945, 11.00000000000000000 ) ) ;
#2756=LINE ( 'NONE', #17345, #21356 ) ;
#2760=CARTESIAN_POINT ( 'NONE',  ( 0.6375389515528632201, -7.656606984113278003, 1.500000000000000444 ) ) ;
#2764=CARTESIAN_POINT ( 'NONE',  ( 14.21659522551787624, -20.98447794503849906, 0.9788672205877712029 ) ) ;
#2773=DIRECTION ( 'NONE',  ( -6.938893903907222067E-15, 0.000000000000000000, 1.000000000000000000 ) ) ;
#2774=ORIENTED_EDGE ( 'NONE', *, *, #2188, .T. ) ;
#2780=CARTESIAN_POINT ( 'NONE',  ( 18.68429645396945560, -21.55436976724162790, -1.490931396286244937 ) ) ;
#2789=CARTESIAN_POINT ( 'NONE',  ( -3.348806739241649399, -1.982316163823921507, 1.747785182639436830 ) ) ;
#2802=DIRECTION ( 'NONE',  ( -1.000000000000000000, 0.000000000000000000, 0.000000000000000000 ) ) ;
#2803=AXIS2_PLACEMENT_3D ( 'NONE', #29453, #11561, #23781 ) ;
#2811=EDGE_CURVE ( 'NONE', #1705, #6111, #17079, .T. ) ;
#2822=ORIENTED_EDGE ( 'NONE', *, *, #24401, .T. ) ;
#2828=VECTOR ( 'NONE', #517, 1000.000000000000000 ) ;
#2831=CARTESIAN_POINT ( 'NONE',  ( 6.329657586300834637, -13.60801132437365801, 1.755870824322850465 ) ) ;
#2832=CARTESIAN_POINT ( 'NONE',  ( 19.32480846800364915, -16.28061487828867016, 1.500000000000000000 ) ) ;
#2843=CARTESIAN_POINT ( 'NONE',  ( 21.36097421961354925, -21.76718868951427055, 1.410897148389129052 ) ) ;
#2848=CIRCLE ( 'NONE', #16148, 7.634842307437897269 ) ;
#2853=CARTESIAN_POINT ( 'NONE',  ( -55.59999999999999432, -10.96966150227468972, 7.500000000000000000 ) ) ;
#2856=CARTESIAN_POINT ( 'NONE',  ( 12.16192611266111712, -15.44737063921108700, -1.499999999999999778 ) ) ;
#2865=AXIS2_PLACEMENT_3D ( 'NONE', #14796, #7619, #2104 ) ;
#2866=ORIENTED_EDGE ( 'NONE', *, *, #23981, .F. ) ;
#2874=CARTESIAN_POINT ( 'NONE',  ( 17.39502519979085449, -21.04076415203812189, -1.751145182513948573 ) ) ;
#2878=AXIS2_PLACEMENT_3D ( 'NONE', #8627, #18170, #10644 ) ;
#2906=CARTESIAN_POINT ( 'NONE',  ( -1.112475574502160613, -13.84051535357300011, 1.744598623382826785 ) ) ;
#2911=ORIENTED_EDGE ( 'NONE', *, *, #161, .F. ) ;
#2922=ORIENTED_EDGE ( 'NONE', *, *, #491, .F. ) ;
#2928=CARTESIAN_POINT ( 'NONE',  ( -2.976978444279338110, -0.1588929671266211263, -1.367460996489382685 ) ) ;
#2929=CARTESIAN_POINT ( 'NONE',  ( 71.67787245194618606, -18.34520463695562498, -1.500000000000000444 ) ) ;
#2931=CARTESIAN_POINT ( 'NONE',  ( 107.4498065544417500, -17.35655240063459104, 4.512182935183896682 ) ) ;
#2941=ORIENTED_EDGE ( 'NONE', *, *, #24401, .F. ) ;
#2948=CARTESIAN_POINT ( 'NONE',  ( 0.2098061928526393227, -5.473028564773644966, -1.769944308764095586 ) ) ;
#2950=CARTESIAN_POINT ( 'NONE',  ( -50.60000000000000142, -10.96966150227468972, 7.500000000000000000 ) ) ;
#2959=CARTESIAN_POINT ( 'NONE',  ( 3.393608999705025386, -0.06500480712391917826, 1.255126411524221997 ) ) ;
#2975=CARTESIAN_POINT ( 'NONE',  ( -2.223027892448373066, -2.927336879246196677, -4.522129901861166701 ) ) ;
#2978=CARTESIAN_POINT ( 'NONE',  ( -50.59999999999987352, -21.43932300454937945, 1.000000000000000000 ) ) ;
#2984=CARTESIAN_POINT ( 'NONE',  ( 108.1144640473778082, -19.71761592378730299, 1.808523936579597535 ) ) ;
#2989=ORIENTED_EDGE ( 'NONE', *, *, #3881, .F. ) ;
#2995=CARTESIAN_POINT ( 'NONE',  ( 23.22564588060106772, -21.93932300456763329, 1.010482627728501948 ) ) ;
#2999=ORIENTED_EDGE ( 'NONE', *, *, #26390, .T. ) ;
#3005=CARTESIAN_POINT ( 'NONE',  ( 13.85437446117657068, -14.51384729146047547, 1.500000000000000000 ) ) ;
#3013=EDGE_CURVE ( 'NONE', #29829, #20134, #17612, .T. ) ;
#3019=CARTESIAN_POINT ( 'NONE',  ( 9.350000000000001421, 0.000000000000000000, 1.000000000000000000 ) ) ;
#3025=VERTEX_POINT ( 'NONE', #23154 ) ;
#3032=DIRECTION ( 'NONE',  ( 1.000000000000000000, 0.000000000000000000, 0.000000000000000000 ) ) ;
#3041=DIRECTION ( 'NONE',  ( -0.000000000000000000, 0.000000000000000000, 1.000000000000000000 ) ) ;
#3045=EDGE_LOOP ( 'NONE', ( #10017, #26499, #8500, #2922 ) ) ;
#3049=CARTESIAN_POINT ( 'NONE',  ( 41.56220206658399263, -20.97620094567151838, -4.522129901861164925 ) ) ;
#3053=DIRECTION ( 'NONE',  ( 0.1908089953765454150, 4.257129299459132156E-16, -0.9816271834476638647 ) ) ;
#3054=ORIENTED_EDGE ( 'NONE', *, *, #1620, .T. ) ;
#3057=CARTESIAN_POINT ( 'NONE',  ( 2.087651665455726224, -16.81471312933366136, 1.500000000000000444 ) ) ;
#3059=CARTESIAN_POINT ( 'NONE',  ( 3.093679806470314819, -0.1913619822784919933, 1.398088436977038107 ) ) ;
#3062=EDGE_CURVE ( 'NONE', #16944, #30215, #25692, .T. ) ;
#3064=B_SPLINE_CURVE_WITH_KNOTS ( 'NONE', 3,
 ( #6470, #26888, #29885, #1826, #12008, #6968, #32567, #19534, #14315, #1481, #1983, #24512 ),
 .UNSPECIFIED., .F., .F.,
 ( 4, 2, 2, 2, 2, 4 ),
 ( 8.673617379884035472E-19, 7.411273891762962317E-05, 0.0001482254778352583790, 0.0002964509556705158906, 0.0005929019113410210476, 0.001185803822682031470 ),
 .UNSPECIFIED. ) ;
#3068=ADVANCED_FACE ( 'NONE', ( #26138 ), #5532, .T. ) ;
#3073=B_SPLINE_SURFACE_WITH_KNOTS ( 'NONE', 1, 3, ( 
 ( #5552, #12560, #25434, #30453, #17740, #20428, #12712, #25588, #1761, #2543, #17916, #11956, #28107, #30806, #27759, #5205 ),
 ( #27947, #19639, #10390, #23262, #7874, #15381, #2699, #5054, #22152, #25271, #10040, #6911, #17107, #12870, #20750, #22764 ) ),
 .UNSPECIFIED., .F., .F., .F.,
 ( 2, 2 ),
 ( 4, 2, 2, 2, 2, 2, 2, 4 ),
 ( 0.000000000000000000, 1.000000000000000000 ),
 ( 0.000000000000000000, 0.5000000000000000000, 0.6250000000000000000, 0.7500000000000000000, 0.8125000000000000000, 0.8750000000000000000, 0.9375000000000000000, 1.000000000000000000 ),
 .UNSPECIFIED. ) ;
#3075=ORIENTED_EDGE ( 'NONE', *, *, #26835, .F. ) ;
#3078=CARTESIAN_POINT ( 'NONE',  ( 0.4474568012433098874, -7.410208993127078259, -0.9788672205888330202 ) ) ;
#3079=CARTESIAN_POINT ( 'NONE',  ( 25.43628654896178176, -17.54453578616395149, 1.000000000000000000 ) ) ;
#3080=CARTESIAN_POINT ( 'NONE',  ( 107.9510094122608734, -17.36390984048267327, 4.614126556756068531 ) ) ;
#3081=EDGE_LOOP ( 'NONE', ( #17559, #1353, #25116, #19800 ) ) ;
#3093=ORIENTED_EDGE ( 'NONE', *, *, #7486, .F. ) ;
#3101=CARTESIAN_POINT ( 'NONE',  ( 0.6161739807942353542, -5.543681800203635213, 1.499999999999999778 ) ) ;
#3105=CARTESIAN_POINT ( 'NONE',  ( 2.632061376486628301, -0.4999999999999992784, 1.500000000000000444 ) ) ;
#3114=CARTESIAN_POINT ( 'NONE',  ( 19.72213158284597867, -21.49998897973801704, -1.523512165874404189 ) ) ;
#3119=DIRECTION ( 'NONE',  ( 1.000000000000000000, 0.000000000000000000, 0.000000000000000000 ) ) ;
#3122=ORIENTED_EDGE ( 'NONE', *, *, #22115, .F. ) ;
#3123=ORIENTED_EDGE ( 'NONE', *, *, #1288, .T. ) ;
#3124=DIRECTION ( 'NONE',  ( 0.000000000000000000, 0.000000000000000000, 1.000000000000000000 ) ) ;
#3135=DIRECTION ( 'NONE',  ( -0.000000000000000000, -0.000000000000000000, -1.000000000000000000 ) ) ;
#3138=CARTESIAN_POINT ( 'NONE',  ( -15.57671159194236488, -25.43932300454937590, 1.499999999999999556 ) ) ;
#3145=DIRECTION ( 'NONE',  ( 2.473959037481232675E-13, 1.000000000000000000, 0.000000000000000000 ) ) ;
#3147=CARTESIAN_POINT ( 'NONE',  ( 12.29359088965425784, -13.32350402072020934, 1.000000000000000000 ) ) ;
#3152=ORIENTED_EDGE ( 'NONE', *, *, #16195, .T. ) ;
#3159=VERTEX_POINT ( 'NONE', #14890 ) ;
#3162=CARTESIAN_POINT ( 'NONE',  ( 8.694260012178471442, -0.3977034846782490640, 1.500000000000001554 ) ) ;
#3175=( BOUNDED_SURFACE ( )  B_SPLINE_SURFACE ( 3, 3, ( 
 ( #26185, #23979, #11122, #18830, #23345, #6123, #28843, #26659, #21500, #31713, #15823, #451, #10631, #20836, #31050, #13292 ),
 ( #8305, #18498, #15964, #4257, #14273, #3952, #24468, #32374, #27328, #6767, #3769, #31865, #27153, #14624, #8934, #19314 ),
 ( #30016, #19140, #12117, #9587, #16957, #24159, #1588, #14430, #9087, #21658, #4447, #24824, #1770, #11773, #21978, #22312 ),
 ( #16624, #17310, #1283, #14126, #32523, #16806, #13939, #19806, #11464, #1942, #11965, #1437, #32204, #24641, #7107, #29331 ) ),
 .UNSPECIFIED., .F., .F., .F. ) 
 B_SPLINE_SURFACE_WITH_KNOTS ( ( 4, 4 ),
 ( 4, 2, 2, 2, 2, 2, 2, 4 ),
 ( 0.000000000000000000, 1.000000000000000000 ),
 ( 0.000000000000000000, 0.5000000000000000000, 0.6250000000000000000, 0.7500000000000000000, 0.8125000000000000000, 0.8750000000000000000, 0.9375000000000000000, 1.000000000000000000 ),
 .UNSPECIFIED. ) 
 GEOMETRIC_REPRESENTATION_ITEM ( )  RATIONAL_B_SPLINE_SURFACE ( (
 ( 1.000000000000000000, 1.000000000000000000, 1.000000000000000000, 1.000000000000000000, 1.000000000000000000, 1.000000000000000000, 1.000000000000000000, 1.000000000000000000, 1.000000000000000000, 1.000000000000000000, 1.000000000000000000, 1.000000000000000000, 1.000000000000000000, 1.000000000000000000, 1.000000000000000000, 1.000000000000000000),
 ( 0.5895302151065233698, 0.5895302151065233698, 0.5895302151065233698, 0.5895302151065233698, 0.5895302151065233698, 0.5895302151065233698, 0.5895302151065233698, 0.5895302151065233698, 0.5895302151065233698, 0.5895302151065233698, 0.5895302151065233698, 0.5895302151065233698, 0.5895302151065233698, 0.5895302151065233698, 0.5895302151065233698, 0.5895302151065233698),
 ( 0.5895302151065233698, 0.5895302151065233698, 0.5895302151065233698, 0.5895302151065233698, 0.5895302151065233698, 0.5895302151065233698, 0.5895302151065233698, 0.5895302151065233698, 0.5895302151065233698, 0.5895302151065233698, 0.5895302151065233698, 0.5895302151065233698, 0.5895302151065233698, 0.5895302151065233698, 0.5895302151065233698, 0.5895302151065233698),
 ( 1.000000000000000000, 1.000000000000000000, 1.000000000000000000, 1.000000000000000000, 1.000000000000000000, 1.000000000000000000, 1.000000000000000000, 1.000000000000000000, 1.000000000000000000, 1.000000000000000000, 1.000000000000000000, 1.000000000000000000, 1.000000000000000000, 1.000000000000000000, 1.000000000000000000, 1.000000000000000000) ) ) 
 REPRESENTATION_ITEM ( '' )  SURFACE ( )  );
#3179=ORIENTED_EDGE ( 'NONE', *, *, #4664, .T. ) ;
#3187=DIRECTION ( 'NONE',  ( 1.000000000000000000, 0.000000000000000000, 0.000000000000000000 ) ) ;
#3194=CARTESIAN_POINT ( 'NONE',  ( 0.1517578099452217555, -1.375880305419572514, -4.522129901861164925 ) ) ;
#3203=CARTESIAN_POINT ( 'NONE',  ( 10.32244514579517691, -19.71146457077206193, 1.499999999999365841 ) ) ;
#3205=CARTESIAN_POINT ( 'NONE',  ( 3.744708216408842549, 0.000000000000000000, 1.000000000000000000 ) ) ;
#3222=CARTESIAN_POINT ( 'NONE',  ( -2.994413461838833612, -0.08301688964435380291, -1.285747183615637113 ) ) ;
#3223=EDGE_CURVE ( 'NONE', #22549, #12204, #18529, .T. ) ;
#3226=CARTESIAN_POINT ( 'NONE',  ( 108.0017901292596747, -18.09513953262979058, 4.637902566605376364 ) ) ;
#3229=EDGE_LOOP ( 'NONE', ( #24727, #26646, #9576, #31466, #15506 ) ) ;
#3232=VERTEX_POINT ( 'NONE', #5854 ) ;
#3243=CARTESIAN_POINT ( 'NONE',  ( -3.262261974584276913, -10.74317314725658434, -1.743566385593488199 ) ) ;
#3254=CARTESIAN_POINT ( 'NONE',  ( 2.949938889207334825, 0.4708014538555421735, 1.389575531037028799 ) ) ;
#3255=ORIENTED_EDGE ( 'NONE', *, *, #6907, .F. ) ;
#3266=CARTESIAN_POINT ( 'NONE',  ( 20.05745782660422094, -21.55152848446452296, -1.510982242221070804 ) ) ;
#3268=CARTESIAN_POINT ( 'NONE',  ( 1.135243775848452819, -9.027721268913223795, -1.499999999999999112 ) ) ;
#3278=EDGE_CURVE ( 'NONE', #29313, #7400, #16923, .T. ) ;
#3291=CIRCLE ( 'NONE', #22510, 5.500000000000001776 ) ;
#3293=CARTESIAN_POINT ( 'NONE',  ( -2.617344628312510135, 0.000000000000000000, -1.468739241856748867 ) ) ;
#3299=CARTESIAN_POINT ( 'NONE',  ( 23.19969958429632229, -21.93395823966979563, 1.123858831411095105 ) ) ;
#3310=CARTESIAN_POINT ( 'NONE',  ( 24.24156412054449206, -17.70199322286843113, 1.500000000000000000 ) ) ;
#3316=ORIENTED_EDGE ( 'NONE', *, *, #8723, .F. ) ;
#3327=ORIENTED_EDGE ( 'NONE', *, *, #3278, .F. ) ;
#3336=CARTESIAN_POINT ( 'NONE',  ( 108.1288400433390393, -19.92462668933126579, -1.384270303710054328 ) ) ;
#3337=DIRECTION ( 'NONE',  ( 0.4030398059120877119, 0.9151824489413827868, -3.863824945872021474E-15 ) ) ;
#3342=AXIS2_PLACEMENT_3D ( 'NONE', #19941, #27610, #9715 ) ;
#3346=CARTESIAN_POINT ( 'NONE',  ( -1.293118168543983204, -1.473601950426632889, 5.485967528433935314 ) ) ;
#3347=ORIENTED_EDGE ( 'NONE', *, *, #27986, .F. ) ;
#3367=CARTESIAN_POINT ( 'NONE',  ( 12.02900455932878820, -13.20152970908862500, -1.000000000000000000 ) ) ;
#3374=CARTESIAN_POINT ( 'NONE',  ( 7.868768533615232208, -10.68327055928662617, 1.500000000000000000 ) ) ;
#3376=CARTESIAN_POINT ( 'NONE',  ( 1.743661372318740632, -1.493834480585329194, -1.500000000000000222 ) ) ;
#3387=CIRCLE ( 'NONE', #7113, 0.4499999999999990119 ) ;
#3394=DIRECTION ( 'NONE',  ( 0.000000000000000000, 0.000000000000000000, -1.000000000000000000 ) ) ;
#3395=CARTESIAN_POINT ( 'NONE',  ( -3.018833153846783635, -0.05660549560294792643, -1.240144350321688238 ) ) ;
#3401=CARTESIAN_POINT ( 'NONE',  ( 18.00753636102977850, -21.49658694929768998, 1.499999999999999112 ) ) ;
#3402=CARTESIAN_POINT ( 'NONE',  ( -3.086632255569896177, -0.4418731834524158852, -1.500000000000000444 ) ) ;
#3405=CARTESIAN_POINT ( 'NONE',  ( 107.4526705878834179, -17.39807245566085570, 4.614338180291445823 ) ) ;
#3418=CIRCLE ( 'NONE', #23596, 0.5000000000000004441 ) ;
#3420=EDGE_CURVE ( 'NONE', #14502, #6959, #18993, .T. ) ;
#3424=CARTESIAN_POINT ( 'NONE',  ( -4.148668979644773103, -6.185511544332382705, -1.745226750906151425 ) ) ;
#3427=CARTESIAN_POINT ( 'NONE',  ( 20.69346795568988995, -16.15118080712828430, -1.000000000000000444 ) ) ;
#3428=CARTESIAN_POINT ( 'NONE',  ( 107.4498027076793960, -17.35649700946218132, -4.512031564368074399 ) ) ;
#3430=CARTESIAN_POINT ( 'NONE',  ( 107.5617944031221640, -18.98359742639815551, -4.522129901861166701 ) ) ;
#3432=DIRECTION ( 'NONE',  ( -1.000000000000000000, 0.000000000000000000, 0.000000000000000000 ) ) ;
#3434=CARTESIAN_POINT ( 'NONE',  ( 2.363212477606361439, -0.1552069907123549142, 1.757289734063312014 ) ) ;
#3437=EDGE_CURVE ( 'NONE', #17869, #26510, #14664, .T. ) ;
#3439=CARTESIAN_POINT ( 'NONE',  ( 107.3476768466458253, -15.88628154573095586, -1.500000000000000000 ) ) ;
#3445=ADVANCED_FACE ( 'NONE', ( #24861 ), #10688, .T. ) ;
#3449=CARTESIAN_POINT ( 'NONE',  ( 0.5441516179539818143, -6.195371308637259489, -1.500000000000000000 ) ) ;
#3459=ORIENTED_EDGE ( 'NONE', *, *, #10593, .T. ) ;
#3470=CARTESIAN_POINT ( 'NONE',  ( 108.0617485914592208, -18.95852647251686562, 4.497382052644061545 ) ) ;
#3489=CARTESIAN_POINT ( 'NONE',  ( 8.396671913538202858, -0.7629006742129739171, 1.500000000000000000 ) ) ;
#3493=CARTESIAN_POINT ( 'NONE',  ( 1.562973067601286070, -10.39368793503460431, 1.763952067544157343 ) ) ;
#3496=EDGE_CURVE ( 'NONE', #1139, #23130, #4978, .T. ) ;
#3497=EDGE_CURVE ( 'NONE', #13341, #7400, #12985, .T. ) ;
#3501=EDGE_LOOP ( 'NONE', ( #27745, #25053, #22650, #10923, #25083, #32399 ) ) ;
#3504=EDGE_CURVE ( 'NONE', #7400, #6370, #15513, .T. ) ;
#3514=CARTESIAN_POINT ( 'NONE',  ( 107.5617944031221640, -18.98359742639815551, 4.522129901861158707 ) ) ;
#3517=CARTESIAN_POINT ( 'NONE',  ( -0.9232102171129876744, 0.000000000000000000, 4.522129901861159595 ) ) ;
#3518=CARTESIAN_POINT ( 'NONE',  ( 25.11445742118086599, -17.48309506032569516, 1.186364133453378322 ) ) ;
#3528=ORIENTED_EDGE ( 'NONE', *, *, #1897, .T. ) ;
#3531=ADVANCED_FACE ( 'NONE', ( #30381, #23006 ), #12306, .F. ) ;
#3539=CARTESIAN_POINT ( 'NONE',  ( 8.970430173841169363, -11.86789775953564785, 1.499999999999999778 ) ) ;
#3545=CARTESIAN_POINT ( 'NONE',  ( 17.39502519978892892, -21.04076415203781636, 1.751145182513948129 ) ) ;
#3551=ADVANCED_FACE ( 'NONE', ( #22523, #7452, #17654 ), #15473, .T. ) ;
#3554=DIRECTION ( 'NONE',  ( -0.000000000000000000, -0.000000000000000000, 1.000000000000000000 ) ) ;
#3567=DIRECTION ( 'NONE',  ( 0.000000000000000000, 0.000000000000000000, 1.000000000000000000 ) ) ;
#3569=CARTESIAN_POINT ( 'NONE',  ( -2.600000000000000089, 0.000000000000000000, 1.000000000000000000 ) ) ;
#3577=CARTESIAN_POINT ( 'NONE',  ( -2.767073886773233848, -0.6621507858625382825, -1.748408842879326075 ) ) ;
#3579=CARTESIAN_POINT ( 'NONE',  ( 7.502484982175676720, -10.19046547981761996, -1.500000000000000000 ) ) ;
#3584=CARTESIAN_POINT ( 'NONE',  ( 2.386646147131364248, -0.3554301312245136679, 1.500000000000000000 ) ) ;
#3585=ORIENTED_EDGE ( 'NONE', *, *, #2301, .T. ) ;
#3588=FACE_OUTER_BOUND ( 'NONE', #26645, .T. ) ;
#3591=B_SPLINE_CURVE_WITH_KNOTS ( 'NONE', 3,
 ( #23285, #28773, #15402, #25611, #2725, #23121 ),
 .UNSPECIFIED., .F., .F.,
 ( 4, 2, 4 ),
 ( 0.01682075285868001036, 0.5000000000000000000, 0.5131349204668873565 ),
 .UNSPECIFIED. ) ;
#3593=CARTESIAN_POINT ( 'NONE',  ( 20.06012370291101732, -21.48645126995936039, 1.642756992391390947 ) ) ;
#3598=ORIENTED_EDGE ( 'NONE', *, *, #17572, .T. ) ;
#3601=CARTESIAN_POINT ( 'NONE',  ( 25.34157222223566919, -17.52646456585300072, -1.103933258152206776 ) ) ;
#3602=B_SPLINE_SURFACE_WITH_KNOTS ( 'NONE', 1, 3, ( 
 ( #12924, #7916, #2254, #25634, #10258, #25823, #12443, #30849, #17793, #22657, #13103, #20296, #17451, #23304, #27649, #15110 ),
 ( #406, #5249, #15424, #28303, #2433, #17605, #14924, #22955, #15273, #25476, #32861, #20484, #12602, #2750, #10082, #22805 ) ),
 .UNSPECIFIED., .F., .F., .F.,
 ( 2, 2 ),
 ( 4, 2, 2, 2, 2, 2, 2, 4 ),
 ( 0.000000000000000000, 1.000000000000000000 ),
 ( 0.000000000000000000, 0.5000000000000000000, 0.6250000000000000000, 0.7500000000000000000, 0.8125000000000000000, 0.8750000000000000000, 0.9375000000000000000, 1.000000000000000000 ),
 .UNSPECIFIED. ) ;
#3604=EDGE_LOOP ( 'NONE', ( #12021, #24451, #5651, #251 ) ) ;
#3614=CARTESIAN_POINT ( 'NONE',  ( 9.350000000000001421, 0.000000000000000000, -1.000000000000000000 ) ) ;
#3616=CARTESIAN_POINT ( 'NONE',  ( 108.0606459309291267, -18.94264843518903163, 4.540289307709638678 ) ) ;
#3633=CARTESIAN_POINT ( 'NONE',  ( 6.976285486575339867, -4.435383624114959566, 1.500000000000000000 ) ) ;
#3635=CARTESIAN_POINT ( 'NONE',  ( 6.963573770753527903, -4.510305581628758276, -1.500000000000000222 ) ) ;
#3637=( BOUNDED_SURFACE ( )  B_SPLINE_SURFACE ( 3, 2, ( 
 ( #12855, #2184, #30436 ),
 ( #15368, #12371, #22591 ),
 ( #10188, #20410, #19924 ),
 ( #30628, #2683, #19735 ) ),
 .UNSPECIFIED., .F., .F., .F. ) 
 B_SPLINE_SURFACE_WITH_KNOTS ( ( 4, 4 ),
 ( 3, 3 ),
 ( 0.003849315137956214883, 0.007259385487753089797 ),
 ( 0.000000000000000000, 1.000000000000000000 ),
 .UNSPECIFIED. ) 
 GEOMETRIC_REPRESENTATION_ITEM ( )  RATIONAL_B_SPLINE_SURFACE ( (
 ( 1.000000000000000000, 0.7074525376973934687, 1.000000000000000000),
 ( 1.000000000000000000, 0.7074519917813385517, 1.000000000000000000),
 ( 1.000000000000000000, 0.7074511013186139952, 1.000000000000000000),
 ( 1.000000000000000000, 0.7074498840443294023, 1.000000000000000000) ) ) 
 REPRESENTATION_ITEM ( '' )  SURFACE ( )  );
#3639=CARTESIAN_POINT ( 'NONE',  ( 5.543469847163194686, -12.78081252332906637, 1.500000000000000000 ) ) ;
#3646=ORIENTED_EDGE ( 'NONE', *, *, #19376, .T. ) ;
#3659=CARTESIAN_POINT ( 'NONE',  ( -2.386718424894570312, -9.330009425478156260, 4.522129901861159595 ) ) ;
#3676=CARTESIAN_POINT ( 'NONE',  ( -23.35000000000000142, -10.96966150227469505, -1.500000000000000000 ) ) ;
#3685=B_SPLINE_CURVE_WITH_KNOTS ( 'NONE', 3,
 ( #21048, #23224, #15694, #25900 ),
 .UNSPECIFIED., .F., .F.,
 ( 4, 4 ),
 ( -5.999999996298584598E-08, 0.0003583794985564089713 ),
 .UNSPECIFIED. ) ;
#3686=CARTESIAN_POINT ( 'NONE',  ( 1.205419605580912767, -3.374343154704484427, -1.499999999999999556 ) ) ;
#3697=CARTESIAN_POINT ( 'NONE',  ( 25.29647048078943783, -17.54044502839390773, 1.294083243069050093 ) ) ;
#3699=CARTESIAN_POINT ( 'NONE',  ( -4.272733292961548912, -6.150071936795129091, -1.499999999999920064 ) ) ;
#3704=CARTESIAN_POINT ( 'NONE',  ( 107.8806307222008627, -16.35047421165092985, 1.384330804614037236 ) ) ;
#3705=ORIENTED_EDGE ( 'NONE', *, *, #5410, .F. ) ;
#3708=CARTESIAN_POINT ( 'NONE',  ( -17.85000000000000142, -10.96966150227469505, 4.500000000000000888 ) ) ;
#3710=CARTESIAN_POINT ( 'NONE',  ( 107.9801083150606900, -17.78292680192075892, 4.320020057268043168 ) ) ;
#3715=CARTESIAN_POINT ( 'NONE',  ( 21.36097421961356702, -21.76718868951428121, -1.410897148389125277 ) ) ;
#3717=ORIENTED_EDGE ( 'NONE', *, *, #32659, .F. ) ;
#3724=CARTESIAN_POINT ( 'NONE',  ( 0.6621927554280921946, -15.34504050551903021, -1.745995324132502136 ) ) ;
#3727=CARTESIAN_POINT ( 'NONE',  ( 15.81086013942911350, -14.68957281887592892, -0.9999999999999995559 ) ) ;
#3728=CARTESIAN_POINT ( 'NONE',  ( 107.9802527803231129, -17.78500706576168611, -4.325704939595124365 ) ) ;
#3734=EDGE_CURVE ( 'NONE', #3159, #27553, #30330, .T. ) ;
#3735=CARTESIAN_POINT ( 'NONE',  ( 0.9232102171129938917, 0.000000000000000000, -4.522129901861164925 ) ) ;
#3750=ORIENTED_EDGE ( 'NONE', *, *, #4512, .T. ) ;
#3769=CARTESIAN_POINT ( 'NONE',  ( -1.327193056402532045, -8.327227690482029487, -5.485967528433937979 ) ) ;
#3791=CARTESIAN_POINT ( 'NONE',  ( 0.6081216625945999876, -7.499966554744998071, 1.500000000000000444 ) ) ;
#3795=VECTOR ( 'NONE', #13925, 1000.000000000000000 ) ;
#3802=CARTESIAN_POINT ( 'NONE',  ( 21.64180102898196978, -16.89820628832873339, -1.499999999999857447 ) ) ;
#3805=CARTESIAN_POINT ( 'NONE',  ( -3.103431213610433836, -2.413098734550712128E-13, 1.052805373823281210 ) ) ;
#3808=CIRCLE ( 'NONE', #27832, 0.5000000000000004441 ) ;
#3814=DIRECTION ( 'NONE',  ( 0.000000000000000000, 1.000000000000000000, 0.000000000000000000 ) ) ;
#3819=CARTESIAN_POINT ( 'NONE',  ( -1.023266466338824454, -9.291661594691762005, 5.485967528433933538 ) ) ;
#3823=DIRECTION ( 'NONE',  ( 1.000000000000000000, 0.000000000000000000, 0.000000000000000000 ) ) ;
#3830=EDGE_CURVE ( 'NONE', #18408, #9983, #18756, .T. ) ;
#3834=CIRCLE ( 'NONE', #23036, 10.96966150227469328 ) ;
#3835=VERTEX_POINT ( 'NONE', #10735 ) ;
#3838=VECTOR ( 'NONE', #19351, 1000.000000000000000 ) ;
#3854=CARTESIAN_POINT ( 'NONE',  ( 1.448939188974345038, -2.783086940837860457, -1.500000000000000000 ) ) ;
#3860=CARTESIAN_POINT ( 'NONE',  ( 8.151896291536630201, -19.35435381133223842, 1.499999999999999112 ) ) ;
#3870=CARTESIAN_POINT ( 'NONE',  ( -4.250504261574428178, -7.586801008987120731, -1.500000000000318190 ) ) ;
#3871=AXIS2_PLACEMENT_3D ( 'NONE', #18068, #24632, #17742 ) ;
#3875=DIRECTION ( 'NONE',  ( -0.000000000000000000, 0.000000000000000000, 1.000000000000000000 ) ) ;
#3880=VECTOR ( 'NONE', #30973, 1000.000000000000000 ) ;
#3881=EDGE_CURVE ( 'NONE', #21586, #9413, #13239, .T. ) ;
#3882=CARTESIAN_POINT ( 'NONE',  ( 21.05407077897152845, -21.72523992960347883, 1.419373079978943464 ) ) ;
#3889=CARTESIAN_POINT ( 'NONE',  ( 21.32535692059155963, -21.82495604402122069, 1.318256435726650633 ) ) ;
#3906=CARTESIAN_POINT ( 'NONE',  ( 14.03158388662403411, -14.04624128054154042, -0.9999999999999995559 ) ) ;
#3907=CARTESIAN_POINT ( 'NONE',  ( 107.4505246733081094, -17.36694227132590029, -4.540110608227355904 ) ) ;
#3911=AXIS2_PLACEMENT_3D ( 'NONE', #17762, #22931, #30167 ) ;
#3915=UNCERTAINTY_MEASURE_WITH_UNIT (LENGTH_MEASURE( 1.000000000000000082E-05 ), #27348, 'distance_accuracy_value', 'NONE');
#3920=CARTESIAN_POINT ( 'NONE',  ( -23.35000000000000142, -10.96966150227469505, 1.500000000000000000 ) ) ;
#3922=ORIENTED_EDGE ( 'NONE', *, *, #26113, .F. ) ;
#3930=CARTESIAN_POINT ( 'NONE',  ( 19.80242846375582388, -16.61789548659649896, -1.500000000000000222 ) ) ;
#3933=AXIS2_PLACEMENT_3D ( 'NONE', #22236, #16879, #29420 ) ;
#3942=ORIENTED_EDGE ( 'NONE', *, *, #19288, .F. ) ;
#3946=ORIENTED_EDGE ( 'NONE', *, *, #21394, .T. ) ;
#3952=CARTESIAN_POINT ( 'NONE',  ( 6.270432871730932334, -15.60322400927264397, -5.485967528433937979 ) ) ;
#3957=AXIS2_PLACEMENT_3D ( 'NONE', #11100, #8910, #16283 ) ;
#3964=EDGE_CURVE ( 'NONE', #19481, #8502, #21937, .T. ) ;
#3970=CARTESIAN_POINT ( 'NONE',  ( 7.230698034991899448, -5.790874021893926304, 1.500000000000000222 ) ) ;
#3973=AXIS2_PLACEMENT_3D ( 'NONE', #20040, #27866, #25016 ) ;
#3975=CARTESIAN_POINT ( 'NONE',  ( 3.091298606786377245, -11.74967118460379467, 1.759199775826757017 ) ) ;
#3984=CARTESIAN_POINT ( 'NONE',  ( 23.03407491560847475, -17.39674082715732339, -1.686926596850272908 ) ) ;
#3990=FACE_OUTER_BOUND ( 'NONE', #3229, .T. ) ;
#3992=DIRECTION ( 'NONE',  ( 1.000000000000000000, 0.000000000000000000, -0.000000000000000000 ) ) ;
#4004=CARTESIAN_POINT ( 'NONE',  ( 25.09406982928240737, -17.52096209994179787, -1.402054309285089673 ) ) ;
#4012=B_SPLINE_CURVE_WITH_KNOTS ( 'NONE', 3,
 ( #14682, #1840, #2331, #24882 ),
 .UNSPECIFIED., .F., .F.,
 ( 4, 4 ),
 ( 0.000000000000000000, 0.0003584394985563508270 ),
 .UNSPECIFIED. ) ;
#4016=CARTESIAN_POINT ( 'NONE',  ( 7.161332922825494940, -6.537789733078093413, -0.9999999999999997780 ) ) ;
#4024=CARTESIAN_POINT ( 'NONE',  ( 5.543719668239277532, -12.78094047433792468, -1.499999999999999112 ) ) ;
#4030=FACE_OUTER_BOUND ( 'NONE', #7408, .T. ) ;
#4036=EDGE_CURVE ( 'NONE', #6686, #27584, #15493, .T. ) ;
#4043=CARTESIAN_POINT ( 'NONE',  ( 107.4811544939906867, -15.87715700148073239, 1.499966567242846383 ) ) ;
#4046=EDGE_LOOP ( 'NONE', ( #19969, #22333, #3598, #30642 ) ) ;
#4051=LINE ( 'NONE', #11710, #24078 ) ;
#4059=ORIENTED_EDGE ( 'NONE', *, *, #29651, .T. ) ;
#4067=CARTESIAN_POINT ( 'NONE',  ( 108.1013391355022861, -19.52862045784693024, -2.195867232700793981 ) ) ;
#4068=CARTESIAN_POINT ( 'NONE',  ( 10.90710808013608002, -12.60204455941997992, -1.000000000000000000 ) ) ;
#4069=CARTESIAN_POINT ( 'NONE',  ( 108.0210557654949213, -18.37255990186116250, -5.108931023128011617 ) ) ;
#4070=VERTEX_POINT ( 'NONE', #14726 ) ;
#4076=CARTESIAN_POINT ( 'NONE',  ( 24.39659513448100725, -17.41072360183587264, -1.416990234759457401 ) ) ;
#4080=FACE_BOUND ( 'NONE', #17194, .T. ) ;
#4087=CARTESIAN_POINT ( 'NONE',  ( 8.778793719788994920, -1.107495284042741668, 0.9999999999999997780 ) ) ;
#4102=CARTESIAN_POINT ( 'NONE',  ( 22.45654965262580660, -21.89488356522464230, 1.207177750837651775 ) ) ;
#4116=EDGE_LOOP ( 'NONE', ( #32107, #16025 ) ) ;
#4119=EDGE_CURVE ( 'NONE', #32242, #7729, #2749, .T. ) ;
#4121=CARTESIAN_POINT ( 'NONE',  ( 8.305304941488214965, -2.146676032724874617, 1.500000000000000222 ) ) ;
#4125=CARTESIAN_POINT ( 'NONE',  ( 0.5438373813056243122, -6.199957864112706218, 1.500000000000000444 ) ) ;
#4129=CARTESIAN_POINT ( 'NONE',  ( 14.44927029820895292, -20.94157174084352491, 1.499999999999999556 ) ) ;
#4131=CARTESIAN_POINT ( 'NONE',  ( -2.620518043835247113, -0.1971982189170117805, 1.631770423870609221 ) ) ;
#4132=CARTESIAN_POINT ( 'NONE',  ( 24.25321317638936947, -17.33169478063224389, -1.345077977219350185 ) ) ;
#4146=CARTESIAN_POINT ( 'NONE',  ( -31.69719015456885103, -21.93932300455405482, 1.000000000000000444 ) ) ;
#4148=DIRECTION ( 'NONE',  ( -1.000000000000000000, 0.000000000000000000, 0.000000000000000000 ) ) ;
#4156=ADVANCED_FACE ( 'NONE', ( #12552 ), #27258, .T. ) ;
#4171=CARTESIAN_POINT ( 'NONE',  ( 2.123790277358594381, -10.79657358825966540, -1.499999999999929834 ) ) ;
#4183=EDGE_CURVE ( 'NONE', #7539, #635, #32467, .T. ) ;
#4192=ORIENTED_EDGE ( 'NONE', *, *, #187, .F. ) ;
#4200=ORIENTED_EDGE ( 'NONE', *, *, #32445, .T. ) ;
#4204=CARTESIAN_POINT ( 'NONE',  ( 17.39502519978889694, -21.04076415203780925, 1.751145182513948351 ) ) ;
#4207=CARTESIAN_POINT ( 'NONE',  ( -4.176564909271631265, -3.225750814637073915, -1.500000000000000000 ) ) ;
#4211=CARTESIAN_POINT ( 'NONE',  ( -3.135269660805080516, -0.4999999999999986122, 1.499999999999999112 ) ) ;
#4212=CARTESIAN_POINT ( 'NONE',  ( 6.734961451239279029, -5.723322302742661627, -1.500000000000000000 ) ) ;
#4213=CARTESIAN_POINT ( 'NONE',  ( 107.4706864324941762, -17.65962134356383473, -4.956537357604676508 ) ) ;
#4225=PLANE ( 'NONE',  #1198 ) ;
#4231=CARTESIAN_POINT ( 'NONE',  ( 3.295700863922525148, -0.1006852655820348191, -1.307585114970547746 ) ) ;
#4233=CARTESIAN_POINT ( 'NONE',  ( 8.265818664828525897, -2.240834465000072662, 1.000000000000000000 ) ) ;
#4257=CARTESIAN_POINT ( 'NONE',  ( 17.49368528860006222, -18.49828807951654497, -5.485967528433937979 ) ) ;
#4259=DIRECTION ( 'NONE',  ( -1.000000000000000000, 0.000000000000000000, 0.000000000000000000 ) ) ;
#4280=CARTESIAN_POINT ( 'NONE',  ( 9.054625866885391616, -14.53177083716424889, 1.499999999999929390 ) ) ;
#4290=EDGE_LOOP ( 'NONE', ( #25318, #17320, #13618, #7211 ) ) ;
#4320=CARTESIAN_POINT ( 'NONE',  ( -23.35000000000000142, -10.96966150227469505, -11.50000000000000000 ) ) ;
#4321=AXIS2_PLACEMENT_3D ( 'NONE', #18066, #20598, #28256 ) ;
#4334=CARTESIAN_POINT ( 'NONE',  ( 0.000000000000000000, -27.93932300454937590, 11.00000000000000000 ) ) ;
#4336=ORIENTED_EDGE ( 'NONE', *, *, #15816, .T. ) ;
#4342=CARTESIAN_POINT ( 'NONE',  ( 0.2309693770184315653, -6.520999745069206099, -1.500000000000070832 ) ) ;
#4346=CARTESIAN_POINT ( 'NONE',  ( 21.32535692059155963, -21.82495604402122069, 1.318256435726650633 ) ) ;
#4350=CARTESIAN_POINT ( 'NONE',  ( 107.5951944727603404, -19.46454432636559417, -3.536284406027203175 ) ) ;
#4354=CIRCLE ( 'NONE', #19836, 0.5000000000000004441 ) ;
#4363=CARTESIAN_POINT ( 'NONE',  ( -2.454768102818410291, -12.18272399704959064, -1.743819976092190416 ) ) ;
#4364=AXIS2_PLACEMENT_3D ( 'NONE', #2978, #13132, #10618 ) ;
#4383=ORIENTED_EDGE ( 'NONE', *, *, #26972, .T. ) ;
#4391=CARTESIAN_POINT ( 'NONE',  ( 107.4398938657686671, -17.21413326613983941, 4.222672820008001260 ) ) ;
#4392=VERTEX_POINT ( 'NONE', #16213 ) ;
#4397=CARTESIAN_POINT ( 'NONE',  ( 8.690022415557999480, -0.1784382875756254372, -1.500000000000000000 ) ) ;
#4398=CARTESIAN_POINT ( 'NONE',  ( 108.0076416556349841, -18.17940005675781379, -4.637887581615233401 ) ) ;
#4405=AXIS2_PLACEMENT_3D ( 'NONE', #22355, #12157, #29732 ) ;
#4423=CARTESIAN_POINT ( 'NONE',  ( 7.196283458169095759, -7.682271642713033089, 1.000000000000000444 ) ) ;
#4431=ORIENTED_EDGE ( 'NONE', *, *, #3964, .T. ) ;
#4437=EDGE_LOOP ( 'NONE', ( #15762, #12391, #14912, #15303 ) ) ;
#4445=CARTESIAN_POINT ( 'NONE',  ( -14.63259398290947289, -27.93932300454937590, -0.9045955023117272509 ) ) ;
#4447=CARTESIAN_POINT ( 'NONE',  ( -2.092582746845232489, -9.051626392537000854, -5.485967528433938867 ) ) ;
#4451=CARTESIAN_POINT ( 'NONE',  ( -2.223027892448377951, -2.927336879245634460, 4.522129901861159595 ) ) ;
#4464=CARTESIAN_POINT ( 'NONE',  ( 23.19698494435080960, -21.93770714115886378, -1.040523891066395201 ) ) ;
#4475=CARTESIAN_POINT ( 'NONE',  ( -3.135269660805080516, -0.5000000000000000000, 1.500000000000000000 ) ) ;
#4485=CARTESIAN_POINT ( 'NONE',  ( 23.22564588060109259, -21.93932300456764040, -1.000000000000000000 ) ) ;
#4486=CARTESIAN_POINT ( 'NONE',  ( -15.51216819290874227, 0.000000000000000000, 1.000000000000000000 ) ) ;
#4495=EDGE_CURVE ( 'NONE', #27584, #593, #21827, .T. ) ;
#4506=AXIS2_PLACEMENT_3D ( 'NONE', #19523, #19025, #29720 ) ;
#4509=EDGE_LOOP ( 'NONE', ( #32318, #7322, #32085, #31877, #10658 ) ) ;
#4512=EDGE_CURVE ( 'NONE', #14095, #2672, #20244, .T. ) ;
#4519=ORIENTED_EDGE ( 'NONE', *, *, #5574, .F. ) ;
#4523=CARTESIAN_POINT ( 'NONE',  ( 9.144688568536819773, -14.26363490968651071, -1.499999999999999556 ) ) ;
#4524=CARTESIAN_POINT ( 'NONE',  ( 6.013832568680315127, -13.53405802968792848, 1.500000000000000444 ) ) ;
#4528=DIRECTION ( 'NONE',  ( 0.000000000000000000, 0.000000000000000000, -1.000000000000000000 ) ) ;
#4530=CARTESIAN_POINT ( 'NONE',  ( 108.1293191351601877, -19.93152549159189135, -2.509206947347181416 ) ) ;
#4540=CARTESIAN_POINT ( 'NONE',  ( -1.898110288140231861, -13.58794273181078438, -1.499999999999999556 ) ) ;
#4562=ORIENTED_EDGE ( 'NONE', *, *, #6001, .F. ) ;
#4565=SPHERICAL_SURFACE ( 'NONE', #23062, 0.5000000000000000000 ) ;
#4567=CARTESIAN_POINT ( 'NONE',  ( 107.9910452807461638, -17.94041638701884267, -4.566009972856815757 ) ) ;
#4569=EDGE_CURVE ( 'NONE', #32499, #17584, #8294, .T. ) ;
#4583=EDGE_CURVE ( 'NONE', #24312, #4070, #18141, .T. ) ;
#4592=EDGE_LOOP ( 'NONE', ( #29294, #28533, #3179, #8053 ) ) ;
#4593=EDGE_LOOP ( 'NONE', ( #27261, #26979, #6287, #31088 ) ) ;
#4595=EDGE_LOOP ( 'NONE', ( #6117, #25342, #29758, #26951 ) ) ;
#4597=DIRECTION ( 'NONE',  ( -1.000000000000000000, 2.473959037481237219E-13, -0.000000000000000000 ) ) ;
#4603=LINE ( 'NONE', #12448, #17148 ) ;
#4605=CYLINDRICAL_SURFACE ( 'NONE', #23213, 5.000000000000000888 ) ;
#4611=EDGE_CURVE ( 'NONE', #15271, #17041, #23555, .T. ) ;
#4628=CARTESIAN_POINT ( 'NONE',  ( 107.9852729111968728, -17.85729570149337064, -4.475837141004190833 ) ) ;
#4633=FACE_OUTER_BOUND ( 'NONE', #29254, .T. ) ;
#4637=ADVANCED_FACE ( 'NONE', ( #5928 ), #26352, .T. ) ;
#4638=DIRECTION ( 'NONE',  ( -1.000000000000000000, 0.000000000000000000, -0.000000000000000000 ) ) ;
#4653=EDGE_CURVE ( 'NONE', #1302, #7812, #11298, .T. ) ;
#4654=CARTESIAN_POINT ( 'NONE',  ( 107.5617723795401872, -18.98359893170738744, -4.522129901861166701 ) ) ;
#4658=CARTESIAN_POINT ( 'NONE',  ( 21.56498441094940688, -21.75760761563370949, 1.480179746966302945 ) ) ;
#4664=EDGE_CURVE ( 'NONE', #11567, #20134, #3808, .T. ) ;
#4674=CARTESIAN_POINT ( 'NONE',  ( 7.321588594920942938, -13.58956495849201929, -1.499999999999999556 ) ) ;
#4675=CARTESIAN_POINT ( 'NONE',  ( 1.828104818894226380, -1.262475772535087915, 1.500000000000000444 ) ) ;
#4683=CARTESIAN_POINT ( 'NONE',  ( 22.16261821944387123, -17.22505787984022874, 1.541391846741430260 ) ) ;
#4684=VERTEX_POINT ( 'NONE', #23485 ) ;
#4687=DIRECTION ( 'NONE',  ( -1.000000000000000000, -0.000000000000000000, -0.000000000000000000 ) ) ;
#4692=CARTESIAN_POINT ( 'NONE',  ( 10.35382568889080979, -19.59147244278173261, -1.750308525318766684 ) ) ;
#4694=PRODUCT ( 'Part1_handle1', 'Part1_handle1', '', ( #26859 ) ) ;
#4709=PLANE ( 'NONE',  #6027 ) ;
#4717=CARTESIAN_POINT ( 'NONE',  ( 107.5617797207340800, -18.98359842993768964, 4.522129901861158707 ) ) ;
#4720=CARTESIAN_POINT ( 'NONE',  ( 9.283830569144292610, -0.1241467201999828379, -1.500000000000000000 ) ) ;
#4721=CARTESIAN_POINT ( 'NONE',  ( 108.0613680874162554, -18.95304730895377432, -4.512352198926723901 ) ) ;
#4737=FACE_OUTER_BOUND ( 'NONE', #19242, .T. ) ;
#4745=CARTESIAN_POINT ( 'NONE',  ( -2.672624763096138167, -0.4219952926969707807, 1.725256589882031344 ) ) ;
#4746=DIRECTION ( 'NONE',  ( -8.519590295723598769E-19, -5.916484360648977690E-20, -1.000000000000000000 ) ) ;
#4751=DIRECTION ( 'NONE',  ( -0.000000000000000000, -0.000000000000000000, 1.000000000000000000 ) ) ;
#4752=FACE_OUTER_BOUND ( 'NONE', #7083, .T. ) ;
#4756=FACE_OUTER_BOUND ( 'NONE', #31174, .T. ) ;
#4760=CARTESIAN_POINT ( 'NONE',  ( 107.8806061107227379, -16.35011981549162741, -2.521000801038054906 ) ) ;
#4761=CARTESIAN_POINT ( 'NONE',  ( 24.55820472632769835, -17.37661330403878424, 1.293157874817708164 ) ) ;
#4763=CARTESIAN_POINT ( 'NONE',  ( 6.220890055303850197, -15.20372210278348035, 4.522129901861156931 ) ) ;
#4764=LINE ( 'NONE', #28013, #11337 ) ;
#4766=B_SPLINE_CURVE_WITH_KNOTS ( 'NONE', 3,
 ( #6595, #32509, #21794, #22146, #24622, #14411, #9417, #32001, #32357, #1752 ),
 .UNSPECIFIED., .F., .F.,
 ( 4, 2, 2, 2, 4 ),
 ( -0.0003514200626105848141, 0.0001564218602127746675, 0.0006642637830361342033, 0.001679947628682841023, 0.003711315319976244906 ),
 .UNSPECIFIED. ) ;
#4775=CARTESIAN_POINT ( 'NONE',  ( 107.9522592018893192, -17.38190650023669548, 4.650312831055688712 ) ) ;
#4778=CARTESIAN_POINT ( 'NONE',  ( 7.321283561615676838, -13.58944227021806128, 1.499999999999999556 ) ) ;
#4785=CARTESIAN_POINT ( 'NONE',  ( 107.9802527803231129, -17.78500706576168611, -4.325704939595124365 ) ) ;
#4794=CARTESIAN_POINT ( 'NONE',  ( -5.304000690461529555E-12, -21.43932300456189566, -1.500000000000000000 ) ) ;
#4802=CARTESIAN_POINT ( 'NONE',  ( 23.03032540518177385, -21.91564990537362689, 1.226001752879403606 ) ) ;
#4804=ORIENTED_EDGE ( 'NONE', *, *, #854, .F. ) ;
#4811=CARTESIAN_POINT ( 'NONE',  ( 0.4080279096648676274, -4.540264344697044763, 1.766711686091106959 ) ) ;
#4815=EDGE_LOOP ( 'NONE', ( #20785, #31518, #28810, #10230 ) ) ;
#4829=CARTESIAN_POINT ( 'NONE',  ( 15.94387883179147281, -16.27117267478923424, -1.500000000000139222 ) ) ;
#4831=CARTESIAN_POINT ( 'NONE',  ( 109.5084093630373729, -17.21855534384546971, 4.522129901861157819 ) ) ;
#4832=VERTEX_POINT ( 'NONE', #10255 ) ;
#4839=CARTESIAN_POINT ( 'NONE',  ( 24.30482536760843715, -17.42173634883311095, 1.458717893414389177 ) ) ;
#4848=CARTESIAN_POINT ( 'NONE',  ( -1.597341074173299846, -13.32274319403951601, -1.744099774574995987 ) ) ;
#4871=DIRECTION ( 'NONE',  ( -1.000000000000000000, 0.000000000000000000, 0.000000000000000000 ) ) ;
#4876=CARTESIAN_POINT ( 'NONE',  ( -61.56966150227469114, -10.96966150227468972, 1.000000000000000000 ) ) ;
#4879=DIRECTION ( 'NONE',  ( 6.938893903907222067E-15, 1.000000000000000000, 0.000000000000000000 ) ) ;
#4881=CARTESIAN_POINT ( 'NONE',  ( 3.541509388326462116, -13.88765124358084968, 4.522129901861156931 ) ) ;
#4883=CARTESIAN_POINT ( 'NONE',  ( 7.278212736155910356, -5.482579125107631235, -1.500000000000000000 ) ) ;
#4886=DIRECTION ( 'NONE',  ( 1.000000000000000000, 0.000000000000000000, 0.000000000000000000 ) ) ;
#4892=B_SPLINE_CURVE_WITH_KNOTS ( 'NONE', 3,
 ( #31002, #18462, #2591, #25992, #23454, #23311, #8269, #7775, #10753, #10439, #10591, #28311, #18290 ),
 .UNSPECIFIED., .F., .F.,
 ( 4, 3, 3, 3, 4 ),
 ( 1.301042606982605321E-18, 0.0005743798323162931140, 0.001512856554034470568, 0.002920571641052362513, 0.003274063357800027687 ),
 .UNSPECIFIED. ) ;
#4894=FACE_OUTER_BOUND ( 'NONE', #33069, .T. ) ;
#4906=CARTESIAN_POINT ( 'NONE',  ( 3.090086839177710321, 0.04810462266637633572, -0.6765469099969410038 ) ) ;
#4915=EDGE_LOOP ( 'NONE', ( #10887, #12325, #28221, #29751, #29239, #2822, #4919, #15962, #3459, #10361 ) ) ;
#4919=ORIENTED_EDGE ( 'NONE', *, *, #23946, .T. ) ;
#4928=CARTESIAN_POINT ( 'NONE',  ( 2.865321775463968379, -11.57729440622175154, -1.759700797516209114 ) ) ;
#4929=AXIS2_PLACEMENT_3D ( 'NONE', #5678, #11016, #15859 ) ;
#4936=CARTESIAN_POINT ( 'NONE',  ( 25.16500339546638187, -17.49275296966148474, 1.172809483626021665 ) ) ;
#4939=CARTESIAN_POINT ( 'NONE',  ( -1.331261126401621420, -14.27417440010058414, 0.9788672205877712029 ) ) ;
#4940=DIRECTION ( 'NONE',  ( 0.000000000000000000, 0.000000000000000000, -1.000000000000000000 ) ) ;
#4950=CARTESIAN_POINT ( 'NONE',  ( 23.21956271100826541, -21.93898037844929760, -1.019911551275596517 ) ) ;
#4951=DIRECTION ( 'NONE',  ( 1.000000000000000000, 0.000000000000000000, 0.000000000000000000 ) ) ;
#4967=ORIENTED_EDGE ( 'NONE', *, *, #15895, .T. ) ;
#4974=CARTESIAN_POINT ( 'NONE',  ( 107.6641581766430278, -20.45810077038846586, 1.500000000000000000 ) ) ;
#4977=CIRCLE ( 'NONE', #27400, 10.96966150227469328 ) ;
#4978=LINE ( 'NONE', #4794, #9079 ) ;
#4989=CARTESIAN_POINT ( 'NONE',  ( 23.24965750580003387, -21.93932300456764395, 1.000000000000000000 ) ) ;
#4995=CARTESIAN_POINT ( 'NONE',  ( 108.1300413742128796, -20.08325238768393461, 1.420916680473288896 ) ) ;
#5022=CARTESIAN_POINT ( 'NONE',  ( 40.91321928711098366, -19.30714377376088464, 0.9788672205888330202 ) ) ;
#5029=CARTESIAN_POINT ( 'NONE',  ( 24.27681693764444049, -17.38739216502004226, 1.394420419282020207 ) ) ;
#5037=CARTESIAN_POINT ( 'NONE',  ( 10.25023147436447069, -19.98140232867044830, -1.499999999999998668 ) ) ;
#5052=EDGE_LOOP ( 'NONE', ( #152, #7642, #15647, #25000 ) ) ;
#5054=CARTESIAN_POINT ( 'NONE',  ( -0.1366093623685602776, -14.96249823008941604, 1.500000000000000000 ) ) ;
#5057=CARTESIAN_POINT ( 'NONE',  ( 107.6023762549644687, -19.56795552613751354, -3.324358428442364843 ) ) ;
#5062=CARTESIAN_POINT ( 'NONE',  ( 2.226738579662389306, -16.57423758818535475, 1.500000000000000444 ) ) ;
#5064=CARTESIAN_POINT ( 'NONE',  ( 8.305304941487758441, -2.146676032726119399, -1.500000000000000000 ) ) ;
#5065=CARTESIAN_POINT ( 'NONE',  ( 108.0293225756549731, -18.49159991151093863, -4.319987168239894260 ) ) ;
#5069=CARTESIAN_POINT ( 'NONE',  ( 107.3477315916820913, -15.88627780335592732, 1.500000000000000000 ) ) ;
#5073=CARTESIAN_POINT ( 'NONE',  ( -3.082813266615065828, -0.4373090928651341414, -1.500000000000000222 ) ) ;
#5078=DIRECTION ( 'NONE',  ( 0.000000000000000000, -0.000000000000000000, -1.000000000000000000 ) ) ;
#5085=CARTESIAN_POINT ( 'NONE',  ( 15.90111129030948334, -14.71846482507236153, 1.000000000000000000 ) ) ;
#5090=CARTESIAN_POINT ( 'NONE',  ( 107.5574907784328076, -18.92149145723228898, 4.691813801508712523 ) ) ;
#5092=ORIENTED_EDGE ( 'NONE', *, *, #22020, .T. ) ;
#5100=CARTESIAN_POINT ( 'NONE',  ( 1.944141728803306490, -0.8659045317505551509, -1.758037889546375743 ) ) ;
#5105=FACE_OUTER_BOUND ( 'NONE', #30272, .T. ) ;
#5107=CARTESIAN_POINT ( 'NONE',  ( 111.3844470440328251, -20.20075132222358505, 1.500000000000000000 ) ) ;
#5109=DIRECTION ( 'NONE',  ( 0.1908089953765452762, 0.000000000000000000, -0.9816271834476639757 ) ) ;
#5118=LINE ( 'NONE', #7791, #9815 ) ;
#5124=FACE_OUTER_BOUND ( 'NONE', #25683, .T. ) ;
#5125=SHAPE_DEFINITION_REPRESENTATION ( #29774, #5606 ) ;
#5126=CARTESIAN_POINT ( 'NONE',  ( 43.74661801760413482, -24.08792321988613594, -1.499999999999999556 ) ) ;
#5134=EDGE_LOOP ( 'NONE', ( #19692, #7796, #14103, #18314 ) ) ;
#5138=CARTESIAN_POINT ( 'NONE',  ( 22.23809519008879221, -21.82720698518721747, -1.456112634554884933 ) ) ;
#5145=CARTESIAN_POINT ( 'NONE',  ( 24.51577259974246914, -17.45257443369953521, 1.477717642885331140 ) ) ;
#5146=DIRECTION ( 'NONE',  ( -1.000000000000000000, 0.000000000000000000, 0.000000000000000000 ) ) ;
#5147=SPHERICAL_SURFACE ( 'NONE', #32712, 0.5000000000000000000 ) ;
#5148=DIRECTION ( 'NONE',  ( 1.000000000000000000, 0.000000000000000000, 0.000000000000000000 ) ) ;
#5150=B_SPLINE_CURVE_WITH_KNOTS ( 'NONE', 3,
 ( #7542, #22921, #17567, #18237, #27766, #2395, #4881, #28115, #22612, #5212, #30654, #25278, #22772, #7379, #28265, #25597 ),
 .UNSPECIFIED., .F., .F.,
 ( 4, 2, 2, 2, 2, 2, 2, 4 ),
 ( 0.009305842773634975459, 0.5000000000000000000, 0.6250000000000000000, 0.7500000000000000000, 0.8125000000000000000, 0.8750000000000000000, 0.9375000000000000000, 1.000000000000000000 ),
 .UNSPECIFIED. ) ;
#5158=CARTESIAN_POINT ( 'NONE',  ( 25.46419143546241060, -18.07592536767356250, 1.500000000000000000 ) ) ;
#5160=CARTESIAN_POINT ( 'NONE',  ( -32.06740601709051930, -21.93932300455396600, -0.9045955023117262517 ) ) ;
#5174=CARTESIAN_POINT ( 'NONE',  ( 17.36028307725516484, -18.11957666780531895, 4.522129901861157819 ) ) ;
#5190=CARTESIAN_POINT ( 'NONE',  ( 2.632061376486628301, -0.5000000000000000000, -1.500000000000000000 ) ) ;
#5194=ORIENTED_EDGE ( 'NONE', *, *, #22020, .F. ) ;
#5205=CARTESIAN_POINT ( 'NONE',  ( -2.600000000000000089, 0.000000000000000000, -1.500000000000000000 ) ) ;
#5212=CARTESIAN_POINT ( 'NONE',  ( -0.7739934281325634435, -8.972773999336988382, 4.522129901861156931 ) ) ;
#5213=CARTESIAN_POINT ( 'NONE',  ( -4.250518365315470781, -7.586662160519804132, 1.500000000000317746 ) ) ;
#5218=CARTESIAN_POINT ( 'NONE',  ( 108.0617487723258279, -18.95852907696271927, -4.497374936780334842 ) ) ;
#5219=EDGE_LOOP ( 'NONE', ( #14394, #4059 ) ) ;
#5226=CARTESIAN_POINT ( 'NONE',  ( 18.66634262892307916, -21.55284492811556873, -1.491166157331017317 ) ) ;
#5227=ORIENTED_EDGE ( 'NONE', *, *, #18433, .T. ) ;
#5228=CARTESIAN_POINT ( 'NONE',  ( 108.0161339826157985, -18.30168745265750729, 4.597046469859526141 ) ) ;
#5234=CARTESIAN_POINT ( 'NONE',  ( 1.828104818894226380, -1.262475772535087915, -1.500000000000000444 ) ) ;
#5240=CARTESIAN_POINT ( 'NONE',  ( -2.989861291979827751, -0.09348435554463166430, 1.299029471086685428 ) ) ;
#5242=LINE ( 'NONE', #25469, #20298 ) ;
#5243=ORIENTED_EDGE ( 'NONE', *, *, #1304, .T. ) ;
#5244=EDGE_LOOP ( 'NONE', ( #21307, #19788, #30050, #5283 ) ) ;
#5249=CARTESIAN_POINT ( 'NONE',  ( 71.67787245194618606, -18.34520463695562498, -1.500000000000000000 ) ) ;
#5252=CARTESIAN_POINT ( 'NONE',  ( 5.107184442557387349, -13.01286747904930330, -1.756586276081733233 ) ) ;
#5255=CARTESIAN_POINT ( 'NONE',  ( 15.65524065575999835, -15.16498509048940413, -1.499999999999999334 ) ) ;
#5261=CARTESIAN_POINT ( 'NONE',  ( 7.307803584392339680, -13.58393279232337569, 1.499999999999999556 ) ) ;
#5283=ORIENTED_EDGE ( 'NONE', *, *, #11032, .T. ) ;
#5284=CARTESIAN_POINT ( 'NONE',  ( -4.102033191966379277, -5.462572707106480685, 1.745628958864925639 ) ) ;
#5285=EDGE_LOOP ( 'NONE', ( #8486, #12384, #6103, #3717 ) ) ;
#5292=CARTESIAN_POINT ( 'NONE',  ( 21.37868616851651637, -21.75910453120781085, -1.431570888178362200 ) ) ;
#5294=DIRECTION ( 'NONE',  ( 1.000000000000000000, 0.000000000000000000, -1.156482317317873973E-14 ) ) ;
#5300=CARTESIAN_POINT ( 'NONE',  ( 24.47286158058016170, -17.44301205329676918, 1.467080835052755550 ) ) ;
#5301=CARTESIAN_POINT ( 'NONE',  ( -23.35000000000000142, -10.96966150227469505, -1.500000000000000000 ) ) ;
#5310=CARTESIAN_POINT ( 'NONE',  ( 11.96689435878012553, -15.52517353469302108, 1.754064196410228371 ) ) ;
#5311=CARTESIAN_POINT ( 'NONE',  ( 14.03158388684700242, -14.04624127993243476, 1.500000000000415223 ) ) ;
#5312=ORIENTED_EDGE ( 'NONE', *, *, #32787, .T. ) ;
#5318=CARTESIAN_POINT ( 'NONE',  ( 1.449017763428880334, -2.782909769958735513, 1.499999999999999556 ) ) ;
#5331=CARTESIAN_POINT ( 'NONE',  ( 21.08401840680152617, -16.78474387323987216, -1.499999999999999556 ) ) ;
#5339=DIRECTION ( 'NONE',  ( -1.000000000000000000, -0.000000000000000000, -0.000000000000000000 ) ) ;
#5353=TOROIDAL_SURFACE ( 'NONE', #16541, 7.144028715714068056, 0.5000000000000000000 ) ;
#5374=CARTESIAN_POINT ( 'NONE',  ( -4.067339738659994097, -9.772649268812690693, 1.499999999999999112 ) ) ;
#5376=AXIS2_PLACEMENT_3D ( 'NONE', #12174, #23039, #22374 ) ;
#5390=( BOUNDED_SURFACE ( )  B_SPLINE_SURFACE ( 3, 2, ( 
 ( #22648, #22145, #15098 ),
 ( #20138, #19628, #9569 ),
 ( #27642, #19789, #4745 ),
 ( #30332, #7403, #9257 ),
 ( #11948, #254, #18448 ),
 ( #5240, #10738, #10423 ),
 ( #15599, #20287, #62 ),
 ( #13241, #2425, #33003 ),
 ( #22948, #12594, #17953 ),
 ( #25812, #22798, #28140 ) ),
 .UNSPECIFIED., .F., .F., .F. ) 
 B_SPLINE_SURFACE_WITH_KNOTS ( ( 4, 2, 2, 2, 4 ),
 ( 3, 3 ),
 ( 0.000000000000000000, 0.0003906036565455321880, 0.0007812073130910643761, 0.001171810969636596618, 0.001562414626182128752 ),
 ( 0.000000000000000000, 1.000000000000000000 ),
 .UNSPECIFIED. ) 
 GEOMETRIC_REPRESENTATION_ITEM ( )  RATIONAL_B_SPLINE_SURFACE ( (
 ( 1.000000000000000000, 0.8508761217583465930, 1.000000000000000000),
 ( 1.000000000000000000, 0.8641352639599353402, 1.000000000000000000),
 ( 1.000000000000000000, 0.8751274560303189398, 1.000000000000000000),
 ( 1.000000000000000000, 0.8893612744008715376, 1.000000000000000000),
 ( 1.000000000000000000, 0.8931697401228705369, 1.000000000000000000),
 ( 1.000000000000000000, 0.8890347101973011812, 1.000000000000000000),
 ( 1.000000000000000000, 0.8820141521041674482, 1.000000000000000000),
 ( 1.000000000000000000, 0.8603874812462587451, 1.000000000000000000),
 ( 1.000000000000000000, 0.8460710229395462800, 1.000000000000000000),
 ( 1.000000000000000000, 0.8293372616342756798, 1.000000000000000000) ) ) 
 REPRESENTATION_ITEM ( '' )  SURFACE ( )  );
#5392=CARTESIAN_POINT ( 'NONE',  ( 107.9812534396071584, -17.79941631051923068, 4.365082084312397193 ) ) ;
#5398=CARTESIAN_POINT ( 'NONE',  ( 1.305960519821096844, -9.941484022874826465, -1.500000000000000444 ) ) ;
#5400=CARTESIAN_POINT ( 'NONE',  ( 107.9481285810059887, -17.32242658709003535, 4.512007113214639986 ) ) ;
#5410=EDGE_CURVE ( 'NONE', #24839, #12213, #1316, .T. ) ;
#5425=CARTESIAN_POINT ( 'NONE',  ( 1.867159791558850035, -10.11553636635117925, 1.499999999999999334 ) ) ;
#5429=CARTESIAN_POINT ( 'NONE',  ( 2.632061376486628301, -0.5000000000000000000, 1.500000000000000000 ) ) ;
#5443=CARTESIAN_POINT ( 'NONE',  ( 17.33093461831549931, -21.43932300456635076, -1.500000000000000000 ) ) ;
#5451=CARTESIAN_POINT ( 'NONE',  ( -1.921189184902703628, -10.44034746380512857, -4.522129901861166701 ) ) ;
#5454=CARTESIAN_POINT ( 'NONE',  ( 3.722706999676778317, -17.21375729507923680, 1.747812214843357692 ) ) ;
#5469=ORIENTED_EDGE ( 'NONE', *, *, #17942, .F. ) ;
#5482=AXIS2_PLACEMENT_3D ( 'NONE', #3920, #28995, #18966 ) ;
#5493=CARTESIAN_POINT ( 'NONE',  ( 15.81086013898917031, -14.68957282009629495, 1.499999999999169775 ) ) ;
#5511=DIRECTION ( 'NONE',  ( -1.000000000000000000, 0.000000000000000000, 0.000000000000000000 ) ) ;
#5532=( BOUNDED_SURFACE ( )  B_SPLINE_SURFACE ( 3, 2, ( 
 ( #10589, #5603, #560 ),
 ( #10751, #18460, #23626 ),
 ( #28653, #751, #10933 ),
 ( #21136, #16084, #3427 ),
 ( #13587, #23793, #7774 ),
 ( #17965, #28153, #25640 ),
 ( #5255, #15429, #3727 ),
 ( #29292, #6230, #3906 ),
 ( #1398, #31823, #13739 ),
 ( #21933, #26965, #14083 ),
 ( #11919, #6081, #1050 ),
 ( #31978, #19264, #4068 ),
 ( #8564, #18953, #26622 ),
 ( #19104, #8894, #21769 ),
 ( #6378, #16575, #31482 ),
 ( #1720, #31663, #26787 ),
 ( #13893, #16267, #6567 ),
 ( #14235, #24283, #9045 ),
 ( #18774, #23941, #16415 ),
 ( #3579, #21619, #16918 ),
 ( #24431, #1549, #11242 ),
 ( #11571, #21447, #8748 ),
 ( #29648, #29143, #11729 ),
 ( #32153, #27112, #9227 ),
 ( #24105, #29468, #16766 ),
 ( #28982, #19455, #26480 ),
 ( #1232, #11424, #6728 ),
 ( #4212, #14382, #24593 ),
 ( #14581, #4883, #15240 ),
 ( #27959, #15064, #32484 ),
 ( #17749, #17267, #7054 ),
 ( #9545, #7381, #14741 ),
 ( #25093, #5064, #17066 ),
 ( #20263, #22775, #22616 ),
 ( #27465, #32826, #22274 ),
 ( #4397, #19950, #12224 ),
 ( #17569, #4720, #2211 ),
 ( #6877, #25444, #27769 ) ),
 .UNSPECIFIED., .F., .F., .F. ) 
 B_SPLINE_SURFACE_WITH_KNOTS ( ( 4, 2, 2, 2, 2, 2, 2, 2, 2, 2, 2, 2, 2, 2, 2, 2, 2, 2, 4 ),
 ( 3, 3 ),
 ( 0.01025725344258870617, 0.01409333659602720994, 0.01792941974946571371, 0.02176550290290421921, 0.02368354447962347370, 0.02560158605634272472, 0.02656060684470235023, 0.02751962763306197574, 0.02847864842142160124, 0.02943766920978123022, 0.03135571078650048471, 0.03231473157486011022, 0.03327375236321973573, 0.03423277315157936124, 0.03519179393993898675, 0.03710983551665823776, 0.03902787709337748878, 0.03998689788173712123, 0.04094591867009674674 ),
 ( 0.000000000000000000, 1.000000000000000000 ),
 .UNSPECIFIED. ) 
 GEOMETRIC_REPRESENTATION_ITEM ( )  RATIONAL_B_SPLINE_SURFACE ( (
 ( 1.000000000000000000, 0.7071067811865475727, 1.000000000000000000),
 ( 1.000000000000000000, 0.7071067811865475727, 1.000000000000000000),
 ( 1.000000000000000000, 0.7071067811865473507, 1.000000000000000000),
 ( 1.000000000000000000, 0.7071067811865473507, 1.000000000000000000),
 ( 1.000000000000000000, 0.7071067811865475727, 1.000000000000000000),
 ( 1.000000000000000000, 0.7071067811865475727, 1.000000000000000000),
 ( 1.000000000000000000, 0.7071067811865487940, 1.000000000000000000),
 ( 1.000000000000000000, 0.7071067811865487940, 1.000000000000000000),
 ( 1.000000000000000000, 0.7071067811865475727, 1.000000000000000000),
 ( 1.000000000000000000, 0.7071067811865475727, 1.000000000000000000),
 ( 1.000000000000000000, 0.7071067811865475727, 1.000000000000000000),
 ( 1.000000000000000000, 0.7071067811865475727, 1.000000000000000000),
 ( 1.000000000000000000, 0.7071067811865475727, 1.000000000000000000),
 ( 1.000000000000000000, 0.7071067811865475727, 1.000000000000000000),
 ( 1.000000000000000000, 0.7071067811865475727, 1.000000000000000000),
 ( 1.000000000000000000, 0.7071067811865475727, 1.000000000000000000),
 ( 1.000000000000000000, 0.7071067811865475727, 1.000000000000000000),
 ( 1.000000000000000000, 0.7071067811865475727, 1.000000000000000000),
 ( 1.000000000000000000, 0.7071067811865475727, 1.000000000000000000),
 ( 1.000000000000000000, 0.7071067811865475727, 1.000000000000000000),
 ( 1.000000000000000000, 0.7071067811865475727, 1.000000000000000000),
 ( 1.000000000000000000, 0.7071067811865475727, 1.000000000000000000),
 ( 1.000000000000000000, 0.7071067811865475727, 1.000000000000000000),
 ( 1.000000000000000000, 0.7071067811865475727, 1.000000000000000000),
 ( 1.000000000000000000, 0.7071067811865475727, 1.000000000000000000),
 ( 1.000000000000000000, 0.7071067811865475727, 1.000000000000000000),
 ( 1.000000000000000000, 0.7071067811865475727, 1.000000000000000000),
 ( 1.000000000000000000, 0.7071067811865475727, 1.000000000000000000),
 ( 1.000000000000000000, 0.7071067811865475727, 1.000000000000000000),
 ( 1.000000000000000000, 0.7071067811865475727, 1.000000000000000000),
 ( 1.000000000000000000, 0.7071067811865469066, 1.000000000000000000),
 ( 1.000000000000000000, 0.7071067811865469066, 1.000000000000000000),
 ( 1.000000000000000000, 0.7071067811865475727, 1.000000000000000000),
 ( 1.000000000000000000, 0.7071067811865475727, 1.000000000000000000),
 ( 1.000000000000000000, 0.7071067811865475727, 1.000000000000000000),
 ( 1.000000000000000000, 0.7071067811865475727, 1.000000000000000000),
 ( 1.000000000000000000, 0.7071067811865475727, 1.000000000000000000),
 ( 1.000000000000000000, 0.7071067811865475727, 1.000000000000000000) ) ) 
 REPRESENTATION_ITEM ( '' )  SURFACE ( )  );
#5533=VECTOR ( 'NONE', #28061, 1000.000000000000000 ) ;
#5546=CARTESIAN_POINT ( 'NONE',  ( 25.43628654896337693, -17.54453578616444176, -1.000000000000000000 ) ) ;
#5552=CARTESIAN_POINT ( 'NONE',  ( 111.3844470440328251, -20.20075132222358505, -1.500000000000000000 ) ) ;
#5554=CARTESIAN_POINT ( 'NONE',  ( 6.645633185707463753, -7.177124861699095248, 1.500000000000000000 ) ) ;
#5556=CARTESIAN_POINT ( 'NONE',  ( 107.6503521880969885, -20.25877567811641811, -1.908490231610645793 ) ) ;
#5563=CARTESIAN_POINT ( 'NONE',  ( 0.8026073492607572746, -15.44636574315928890, 1.746109330076501820 ) ) ;
#5564=DIRECTION ( 'NONE',  ( -0.000000000000000000, -1.000000000000000000, -0.000000000000000000 ) ) ;
#5566=CARTESIAN_POINT ( 'NONE',  ( 3.381541507458993845, -0.06919447570412246007, 1.261810069052565986 ) ) ;
#5567=DIRECTION ( 'NONE',  ( 1.000000000000000000, 0.000000000000000000, 0.000000000000000000 ) ) ;
#5568=ORIENTED_EDGE ( 'NONE', *, *, #17083, .T. ) ;
#5569=CARTESIAN_POINT ( 'NONE',  ( -15.12340757463330654, -21.43932300455815465, -1.500000000000000000 ) ) ;
#5570=VECTOR ( 'NONE', #28747, 999.9999999999998863 ) ;
#5571=CARTESIAN_POINT ( 'NONE',  ( -31.09064165252238965, -25.43932300454937945, 1.500000000000000000 ) ) ;
#5574=EDGE_CURVE ( 'NONE', #27553, #24839, #31913, .T. ) ;
#5575=DIRECTION ( 'NONE',  ( 1.000000000000000000, 0.000000000000000000, 0.000000000000000000 ) ) ;
#5577=CARTESIAN_POINT ( 'NONE',  ( -2.799189356625064296, 0.2797963115108609289, -0.9035254090732194321 ) ) ;
#5578=VERTEX_POINT ( 'NONE', #9809 ) ;
#5580=CARTESIAN_POINT ( 'NONE',  ( -31.59999999999986997, -21.43932300455407969, 1.500000000000000000 ) ) ;
#5586=CARTESIAN_POINT ( 'NONE',  ( 7.990320970379346299, -10.02608796048407314, 1.000000000000000000 ) ) ;
#5587=CARTESIAN_POINT ( 'NONE',  ( 108.0183845395928302, -18.33409491325710050, 4.565968059339312823 ) ) ;
#5588=ORIENTED_EDGE ( 'NONE', *, *, #5719, .F. ) ;
#5591=CARTESIAN_POINT ( 'NONE',  ( -5.304000690461529555E-12, -21.43932300456189566, 1.000000000000000000 ) ) ;
#5596=CARTESIAN_POINT ( 'NONE',  ( 3.558065962460099652, -17.13340427766722485, -1.747754039643054425 ) ) ;
#5601=CARTESIAN_POINT ( 'NONE',  ( 0.4198231981512192679, -4.496089151576069476, -1.766557846874257764 ) ) ;
#5602=CARTESIAN_POINT ( 'NONE',  ( 21.31323116099696691, -21.82417724537293324, -1.319197765239386699 ) ) ;
#5603=CARTESIAN_POINT ( 'NONE',  ( 25.61042644976673088, -17.59778802277001475, -1.500000000000000000 ) ) ;
#5606=SHAPE_REPRESENTATION ( 'Part1_handle1', ( #2865 ), #179 ) ;
#5614=CARTESIAN_POINT ( 'NONE',  ( 2.454674724652329498, -0.02938977324473661737, 1.729574810602310775 ) ) ;
#5622=CARTESIAN_POINT ( 'NONE',  ( 18.00753636103138078, -21.49658694930015557, -1.499999999999980682 ) ) ;
#5623=VERTEX_POINT ( 'NONE', #11991 ) ;
#5624=CARTESIAN_POINT ( 'NONE',  ( -2.767073886773233848, -0.6621507858625382825, -1.748408842879326075 ) ) ;
#5628=CARTESIAN_POINT ( 'NONE',  ( 3.568565220189176213, -17.77020640689091024, -0.9788672205760856615 ) ) ;
#5634=ORIENTED_EDGE ( 'NONE', *, *, #18015, .T. ) ;
#5646=CARTESIAN_POINT ( 'NONE',  ( 23.15209937164893006, -21.93517043476721895, 1.064739154212363648 ) ) ;
#5647=CARTESIAN_POINT ( 'NONE',  ( 23.27353278736383047, -21.94187821002794436, 1.030224497836262687 ) ) ;
#5648=LINE ( 'NONE', #15828, #8656 ) ;
#5651=ORIENTED_EDGE ( 'NONE', *, *, #387, .F. ) ;
#5654=DIRECTION ( 'NONE',  ( -0.4851627901281766464, 0.000000000000000000, 0.8744238486426606505 ) ) ;
#5655=CARTESIAN_POINT ( 'NONE',  ( 19.46384663066884357, -15.80031286499706056, 1.000000000000000000 ) ) ;
#5659=CARTESIAN_POINT ( 'NONE',  ( 1.947468252185016624, -0.8602631160122127252, 1.758031951640323554 ) ) ;
#5674=DIRECTION ( 'NONE',  ( -0.9151824489413827868, 0.4030398059120878229, 0.000000000000000000 ) ) ;
#5677=CARTESIAN_POINT ( 'NONE',  ( 22.99325939039678701, -17.14855239172946710, -1.466877076793135837 ) ) ;
#5678=CARTESIAN_POINT ( 'NONE',  ( -31.57659242536668032, 0.000000000000000000, -1.000000000000000000 ) ) ;
#5682=B_SPLINE_CURVE_WITH_KNOTS ( 'NONE', 3,
 ( #32401, #24854, #1972, #11493, #21689, #29365, #6456, #20340, #14809, #32555, #5138, #18003 ),
 .UNSPECIFIED., .F., .F.,
 ( 4, 2, 2, 2, 2, 4 ),
 ( 3.252606517456513302E-18, 8.901442616029611027E-05, 0.0001780288523205889679, 0.0003560577046411746833, 0.0007121154092823457887, 0.001424230818564688325 ),
 .UNSPECIFIED. ) ;
#5687=ORIENTED_EDGE ( 'NONE', *, *, #2251, .F. ) ;
#5693=EDGE_CURVE ( 'NONE', #8757, #15269, #30317, .T. ) ;
#5696=CARTESIAN_POINT ( 'NONE',  ( -2.617344628312510135, 0.000000000000000000, -1.468739241856748867 ) ) ;
#5701=CARTESIAN_POINT ( 'NONE',  ( -1.047937531484008478, -4.989690239015235562, -4.522129901861164925 ) ) ;
#5707=CARTESIAN_POINT ( 'NONE',  ( -5.427698642335591239E-12, -21.93932300456189566, -1.000000000000000000 ) ) ;
#5709=CARTESIAN_POINT ( 'NONE',  ( -3.562905260966561904, -10.36268085599621891, 1.499999999999999334 ) ) ;
#5713=CARTESIAN_POINT ( 'NONE',  ( 24.26973362692717018, -17.42849669161154225, 1.479847483350004156 ) ) ;
#5716=CARTESIAN_POINT ( 'NONE',  ( -32.07659242536668387, -21.93932300455396245, -1.000000000000000000 ) ) ;
#5719=EDGE_CURVE ( 'NONE', #19481, #6111, #2471, .T. ) ;
#5722=CARTESIAN_POINT ( 'NONE',  ( -2.989861291979289071, -0.09348435554434110506, -1.299029471086388998 ) ) ;
#5723=CARTESIAN_POINT ( 'NONE',  ( 108.0241571341765621, -18.41721883922283354, 4.475799714874606039 ) ) ;
#5724=B_SPLINE_SURFACE_WITH_KNOTS ( 'NONE', 1, 3, ( 
 ( #15436, #570, #25647, #28010, #2764, #22814, #25333, #10760, #4939, #33019, #10445, #12613, #10091, #20309, #30519, #7603 ),
 ( #5107, #22966, #12945, #15285, #23162, #25487, #274, #2595, #31342, #26795, #11430, #6235, #13418, #23799, #11090, #8901 ),
 ( #10941, #8572, #8420, #16420, #13594, #29299, #23947, #24291, #24114, #31192, #6386, #28990, #8754, #26484, #19110, #21142 ) ),
 .UNSPECIFIED., .F., .F., .F.,
 ( 2, 1, 2 ),
 ( 4, 2, 2, 2, 2, 2, 2, 4 ),
 ( -0.1724389077687537020, 0.000000000000000000, 1.000000000000000000 ),
 ( 0.000000000000000000, 0.5000000000000000000, 0.6250000000000000000, 0.7500000000000000000, 0.8125000000000000000, 0.8750000000000000000, 0.9375000000000000000, 1.000000000000000000 ),
 .UNSPECIFIED. ) ;
#5729=CARTESIAN_POINT ( 'NONE',  ( -2.998975125317107082, -0.2822817718606283055, -1.451460369366592618 ) ) ;
#5732=CARTESIAN_POINT ( 'NONE',  ( 107.5142031382969492, -18.29244943398689927, 5.137641827787525095 ) ) ;
#5734=DIRECTION ( 'NONE',  ( 0.000000000000000000, 1.000000000000000000, -0.000000000000000000 ) ) ;
#5736=DIRECTION ( 'NONE',  ( -2.473959037481232675E-13, -1.000000000000000000, 0.000000000000000000 ) ) ;
#5743=CYLINDRICAL_SURFACE ( 'NONE', #1106, 0.5000000000000000000 ) ;
#5746=FACE_OUTER_BOUND ( 'NONE', #29191, .T. ) ;
#5750=CARTESIAN_POINT ( 'NONE',  ( 107.9011023225883861, -16.64526016453799073, -1.988803970548091993 ) ) ;
#5753=CARTESIAN_POINT ( 'NONE',  ( 10.97394597854683340, -14.84299795458939819, 1.500000000000000000 ) ) ;
#5756=CARTESIAN_POINT ( 'NONE',  ( 3.094741023239449884, -0.1906005183311319795, 1.397910568869148440 ) ) ;
#5757=ORIENTED_EDGE ( 'NONE', *, *, #6143, .F. ) ;
#5766=DIRECTION ( 'NONE',  ( 0.000000000000000000, 0.000000000000000000, 1.000000000000000000 ) ) ;
#5770=ORIENTED_EDGE ( 'NONE', *, *, #29412, .F. ) ;
#5785=CARTESIAN_POINT ( 'NONE',  ( -45.60000000000000142, -10.96966150227468972, 6.999999999999999112 ) ) ;
#5790=CARTESIAN_POINT ( 'NONE',  ( -50.60000000000000142, -21.93932300454937945, -1.000000000000000000 ) ) ;
#5792=CARTESIAN_POINT ( 'NONE',  ( 22.91474812097366254, -21.90304135545737552, 1.273718610094523918 ) ) ;
#5801=CARTESIAN_POINT ( 'NONE',  ( 17.02282544802756448, -15.06900748016092528, 1.500000000000000000 ) ) ;
#5816=ORIENTED_EDGE ( 'NONE', *, *, #11427, .F. ) ;
#5824=CARTESIAN_POINT ( 'NONE',  ( 25.43628654896178176, -17.54453578616395149, 1.000000000000000000 ) ) ;
#5825=DIRECTION ( 'NONE',  ( 1.000000000000000000, 0.000000000000000000, 0.000000000000000000 ) ) ;
#5827=CARTESIAN_POINT ( 'NONE',  ( 107.4817635328069514, -17.82060337710651154, -5.060121585732545668 ) ) ;
#5828=CARTESIAN_POINT ( 'NONE',  ( 107.7139893852324803, -17.39210339641074654, -4.500752875105683337 ) ) ;
#5836=CARTESIAN_POINT ( 'NONE',  ( 23.08530182711102796, -16.84224482508541243, -0.9999999999999997780 ) ) ;
#5840=VERTEX_POINT ( 'NONE', #31860 ) ;
#5841=ORIENTED_EDGE ( 'NONE', *, *, #2609, .F. ) ;
#5844=CARTESIAN_POINT ( 'NONE',  ( 8.037025183208486467, -10.89872694351444871, 1.500000000000000666 ) ) ;
#5847=CARTESIAN_POINT ( 'NONE',  ( 21.03177542174473658, -17.18603084754145982, -1.753176640694677380 ) ) ;
#5852=CARTESIAN_POINT ( 'NONE',  ( 8.273188133893770058, -18.97010227097647928, 1.749556775333751313 ) ) ;
#5854=CARTESIAN_POINT ( 'NONE',  ( -48.50000000000000000, -10.96966150227468972, 7.074999999999997513 ) ) ;
#5860=CARTESIAN_POINT ( 'NONE',  ( 25.09407003920303225, -17.52096212029302436, 1.402054218073202518 ) ) ;
#5870=CARTESIAN_POINT ( 'NONE',  ( 18.02407935480700374, -21.25192265501668842, 1.530583967973806470 ) ) ;
#5875=CARTESIAN_POINT ( 'NONE',  ( 107.4897528024014974, -17.93676709507456479, 5.108846369746858684 ) ) ;
#5879=ORIENTED_EDGE ( 'NONE', *, *, #16302, .T. ) ;
#5880=DIRECTION ( 'NONE',  ( 1.000000000000000000, 0.000000000000000000, 0.000000000000000000 ) ) ;
#5892=CARTESIAN_POINT ( 'NONE',  ( 16.00008021400722669, -20.81650718949249779, -1.751028325393708673 ) ) ;
#5893=CARTESIAN_POINT ( 'NONE',  ( 108.0827968514280144, -19.26161617991734332, -2.743108981515642419 ) ) ;
#5894=DIRECTION ( 'NONE',  ( 1.000000000000000000, 0.000000000000000000, 0.000000000000000000 ) ) ;
#5895=CARTESIAN_POINT ( 'NONE',  ( 107.9443384504777868, -17.26784965035007247, -3.265388143050863334 ) ) ;
#5899=CARTESIAN_POINT ( 'NONE',  ( 107.5617797207334689, -18.98359842993772517, -4.522129901861166701 ) ) ;
#5900=CARTESIAN_POINT ( 'NONE',  ( 2.303719037931331037, -1.057379009928627545, 1.500000000000000000 ) ) ;
#5902=CARTESIAN_POINT ( 'NONE',  ( -29.24402871571405882, -27.93932300454937590, 11.50000000000000000 ) ) ;
#5909=LINE ( 'NONE', #18790, #27929 ) ;
#5912=TOROIDAL_SURFACE ( 'NONE', #27270, 8.000000000000000000, 0.5000000000000000000 ) ;
#5916=CARTESIAN_POINT ( 'NONE',  ( 21.24324854073032043, -21.72960979489735323, -1.457811124649064594 ) ) ;
#5923=CARTESIAN_POINT ( 'NONE',  ( 25.43628628520272272, -17.54453570558254327, -1.030327512441486570 ) ) ;
#5925=CARTESIAN_POINT ( 'NONE',  ( -4.637780547558303823, -6.332425682051282756, -0.9788672205760856615 ) ) ;
#5928=FACE_OUTER_BOUND ( 'NONE', #19450, .T. ) ;
#5933=CARTESIAN_POINT ( 'NONE',  ( 22.85793996273714868, -21.91835824163867130, 1.144021738967093471 ) ) ;
#5936=DIRECTION ( 'NONE',  ( 1.145146108979476986E-14, -3.498552684802598930E-15, 1.000000000000000000 ) ) ;
#5938=CARTESIAN_POINT ( 'NONE',  ( 108.0572798301028996, -18.89417742067558237, 4.649361883339969914 ) ) ;
#5939=CIRCLE ( 'NONE', #6448, 0.5000000000000000000 ) ;
#5949=CARTESIAN_POINT ( 'NONE',  ( -45.60000000000000142, -10.96966150227468972, 7.500000000000000000 ) ) ;
#5955=ORIENTED_EDGE ( 'NONE', *, *, #22241, .F. ) ;
#5961=CARTESIAN_POINT ( 'NONE',  ( 7.289999265597088218, -8.244573099840453168, 1.499999999999714673 ) ) ;
#5965=( BOUNDED_SURFACE ( )  B_SPLINE_SURFACE ( 3, 2, ( 
 ( #22783, #44, #2061 ),
 ( #12233, #32988, #5073 ),
 ( #15250, #532, #23592 ),
 ( #18436, #11056, #18086 ),
 ( #8240, #28468, #23424 ),
 ( #28628, #28772, #5722 ),
 ( #26279, #31310, #3395 ),
 ( #6050, #15902, #30971 ),
 ( #5577, #716, #8386 ),
 ( #15758, #21257, #13082 ) ),
 .UNSPECIFIED., .F., .F., .F. ) 
 B_SPLINE_SURFACE_WITH_KNOTS ( ( 4, 2, 2, 2, 4 ),
 ( 3, 3 ),
 ( 0.000000000000000000, 0.0003906036565455327301, 0.0007812073130910654603, 0.001171810969636598136, 0.001562414626182130921 ),
 ( 0.000000000000000000, 1.000000000000000000 ),
 .UNSPECIFIED. ) 
 GEOMETRIC_REPRESENTATION_ITEM ( )  RATIONAL_B_SPLINE_SURFACE ( (
 ( 1.000000000000000000, 0.8508761217583471481, 1.000000000000000000),
 ( 1.000000000000000000, 0.8641352639599342300, 1.000000000000000000),
 ( 1.000000000000000000, 0.8751274560303193839, 1.000000000000000000),
 ( 1.000000000000000000, 0.8893612744008719817, 1.000000000000000000),
 ( 1.000000000000000000, 0.8931697401227335353, 1.000000000000000000),
 ( 1.000000000000000000, 0.8890347101974386268, 1.000000000000000000),
 ( 1.000000000000000000, 0.8820141521043950439, 1.000000000000000000),
 ( 1.000000000000000000, 0.8603874812460335919, 1.000000000000000000),
 ( 1.000000000000000000, 0.8460710229397098159, 1.000000000000000000),
 ( 1.000000000000000000, 0.8293372616342803427, 1.000000000000000000) ) ) 
 REPRESENTATION_ITEM ( '' )  SURFACE ( )  );
#5966=AXIS2_PLACEMENT_3D ( 'NONE', #25406, #2516, #15518 ) ;
#5968=CARTESIAN_POINT ( 'NONE',  ( 0.5135429646647714508, -4.169291690411378148, 1.765415482494630428 ) ) ;
#5978=CARTESIAN_POINT ( 'NONE',  ( -23.35000000000000142, -10.96966150227469505, -11.00000000000000000 ) ) ;
#5992=VECTOR ( 'NONE', #1541, 999.9999999999998863 ) ;
#5998=CARTESIAN_POINT ( 'NONE',  ( 17.36028307725516839, -18.11957666780532250, 4.522129901861156931 ) ) ;
#6001=EDGE_CURVE ( 'NONE', #11582, #7955, #1587, .T. ) ;
#6014=AXIS2_PLACEMENT_3D ( 'NONE', #8718, #31630, #16244 ) ;
#6024=CARTESIAN_POINT ( 'NONE',  ( 71.38866214474374772, -19.82505015907488755, -4.522129901861164925 ) ) ;
#6026=CARTESIAN_POINT ( 'NONE',  ( 7.106060642427830309, -3.992384276486468320, 1.500000000000000444 ) ) ;
#6027=AXIS2_PLACEMENT_3D ( 'NONE', #9213, #1537, #7039 ) ;
#6028=CARTESIAN_POINT ( 'NONE',  ( 2.632061376486627857, -0.5000000000000015543, -1.499999999999999112 ) ) ;
#6034=DIRECTION ( 'NONE',  ( -2.473959037481232675E-13, -1.000000000000000000, 0.000000000000000000 ) ) ;
#6043=CIRCLE ( 'NONE', #24721, 9.500000000000003553 ) ;
#6050=CARTESIAN_POINT ( 'NONE',  ( -2.742527549463608771, 0.2598362491861793688, -1.021881266978575731 ) ) ;
#6061=ORIENTED_EDGE ( 'NONE', *, *, #8432, .F. ) ;
#6077=CARTESIAN_POINT ( 'NONE',  ( 7.721070889493614864, -18.80910814508606066, -1.749364008687505301 ) ) ;
#6079=DIRECTION ( 'NONE',  ( -1.000000000000000000, 2.473959037481237219E-13, -0.000000000000000000 ) ) ;
#6081=CARTESIAN_POINT ( 'NONE',  ( 11.72844749914836271, -13.05523934214929582, -1.500000000000280220 ) ) ;
#6082=CARTESIAN_POINT ( 'NONE',  ( 107.9806121034343818, -17.79018122917594269, -4.339844731563715641 ) ) ;
#6101=CARTESIAN_POINT ( 'NONE',  ( 21.05407077897105594, -21.72523992960374883, -1.419373079979250551 ) ) ;
#6103=ORIENTED_EDGE ( 'NONE', *, *, #29034, .T. ) ;
#6108=CARTESIAN_POINT ( 'NONE',  ( 24.40424503925390454, -17.45211869376770153, -1.605444122987507383 ) ) ;
#6111=VERTEX_POINT ( 'NONE', #557 ) ;
#6117=ORIENTED_EDGE ( 'NONE', *, *, #9574, .F. ) ;
#6118=DIRECTION ( 'NONE',  ( -0.000000000000000000, 0.000000000000000000, 1.000000000000000000 ) ) ;
#6122=CARTESIAN_POINT ( 'NONE',  ( 107.5620291353747717, -18.98729610813186852, 4.512028494923953303 ) ) ;
#6123=CARTESIAN_POINT ( 'NONE',  ( 6.220890055307039646, -15.20372210278347680, -4.522129901861164925 ) ) ;
#6127=EDGE_CURVE ( 'NONE', #21122, #21390, #17145, .T. ) ;
#6131=DIRECTION ( 'NONE',  ( 0.000000000000000000, 0.000000000000000000, -1.000000000000000000 ) ) ;
#6139=CARTESIAN_POINT ( 'NONE',  ( -0.9232102171129831225, 0.000000000000000000, -4.522129901861166701 ) ) ;
#6140=CARTESIAN_POINT ( 'NONE',  ( 7.289999264625238951, -8.244573099998591559, 1.000000000000000000 ) ) ;
#6143=EDGE_CURVE ( 'NONE', #3835, #6959, #25826, .T. ) ;
#6146=CARTESIAN_POINT ( 'NONE',  ( 6.718200922662554753, -13.33586090649603229, 1.500000000000000000 ) ) ;
#6164=CARTESIAN_POINT ( 'NONE',  ( -32.07659242536668387, -21.93932300455395534, -1.292893218813452538 ) ) ;
#6172=LINE ( 'NONE', #21376, #8707 ) ;
#6181=CARTESIAN_POINT ( 'NONE',  ( 108.1300413742128228, -19.95926608421483195, 0.000000000000000000 ) ) ;
#6189=CARTESIAN_POINT ( 'NONE',  ( 10.28480887676917455, -12.81065604946497061, 1.500000000000000000 ) ) ;
#6196=CARTESIAN_POINT ( 'NONE',  ( 11.65793814731733846, -20.33404869677255888, 1.500000000000000444 ) ) ;
#6202=CARTESIAN_POINT ( 'NONE',  ( -50.60000000000000142, -10.96966150227468972, 0.9999999999999991118 ) ) ;
#6203=CARTESIAN_POINT ( 'NONE',  ( -3.817249540146987474, -10.46527866769224424, -1.500000000000000000 ) ) ;
#6206=CARTESIAN_POINT ( 'NONE',  ( 107.8102081147311821, -16.09624553401233271, 1.444131124663140309 ) ) ;
#6209=CARTESIAN_POINT ( 'NONE',  ( 18.68429645396846439, -21.55436976724084275, 1.490931396286530042 ) ) ;
#6223=B_SPLINE_CURVE_WITH_KNOTS ( 'NONE', 3,
 ( #26143, #5899, #23312, #3430 ),
 .UNSPECIFIED., .F., .F.,
 ( 4, 4 ),
 ( 0.000000000000000000, 2.207496373042337949E-08 ),
 .UNSPECIFIED. ) ;
#6225=DIRECTION ( 'NONE',  ( 1.224646799147353207E-16, 1.000000000000000000, 0.000000000000000000 ) ) ;
#6226=EDGE_LOOP ( 'NONE', ( #29499, #12856, #19965, #11282 ) ) ;
#6228=CARTESIAN_POINT ( 'NONE',  ( 25.43628654896041397, -17.54453578616353582, 1.000000000000000000 ) ) ;
#6230=CARTESIAN_POINT ( 'NONE',  ( 14.03158388684507152, -14.04624127993173843, -1.499999999999859224 ) ) ;
#6231=FACE_OUTER_BOUND ( 'NONE', #825, .T. ) ;
#6235=CARTESIAN_POINT ( 'NONE',  ( -4.317168503051449946, -7.715934794172482292, 1.500000000000000000 ) ) ;
#6240=EDGE_CURVE ( 'NONE', #31647, #29157, #1583, .T. ) ;
#6242=ORIENTED_EDGE ( 'NONE', *, *, #4653, .F. ) ;
#6246=CARTESIAN_POINT ( 'NONE',  ( 3.326984917281274878, -11.41685861481259678, -1.499999999999999334 ) ) ;
#6251=CARTESIAN_POINT ( 'NONE',  ( 25.06773407388217834, -17.47416606015785945, -1.197364706239002485 ) ) ;
#6256=DIRECTION ( 'NONE',  ( 0.000000000000000000, 0.000000000000000000, -1.000000000000000000 ) ) ;
#6269=ADVANCED_FACE ( 'NONE', ( #5746 ), #10781, .F. ) ;
#6271=SPHERICAL_SURFACE ( 'NONE', #32837, 0.5000000000000000000 ) ;
#6277=CARTESIAN_POINT ( 'NONE',  ( -50.60000000000000142, -10.96966150227468972, 7.500000000000000000 ) ) ;
#6282=CARTESIAN_POINT ( 'NONE',  ( -5.304000690461529555E-12, -21.43932300456189566, -1.000000000000000000 ) ) ;
#6287=ORIENTED_EDGE ( 'NONE', *, *, #9385, .F. ) ;
#6288=CARTESIAN_POINT ( 'NONE',  ( 0.5290760861564465234, -6.525414595377379889, 1.500000000000000000 ) ) ;
#6310=DIRECTION ( 'NONE',  ( 0.000000000000000000, -0.000000000000000000, -1.000000000000000000 ) ) ;
#6311=CARTESIAN_POINT ( 'NONE',  ( 72.72614267423888634, -20.12349919362671358, 5.485967528433933538 ) ) ;
#6323=EDGE_LOOP ( 'NONE', ( #1710, #30315, #17140, #14867, #8014 ) ) ;
#6331=VERTEX_POINT ( 'NONE', #24781 ) ;
#6333=CARTESIAN_POINT ( 'NONE',  ( 0.8407900506754626413, -11.56055812333295130, -4.522129901861164925 ) ) ;
#6341=CARTESIAN_POINT ( 'NONE',  ( 15.90621216620982281, -21.21021934853489910, 1.499999999999999112 ) ) ;
#6351=CARTESIAN_POINT ( 'NONE',  ( -4.125275233336413550, -7.575318389262013064, -1.744514813436137235 ) ) ;
#6354=CARTESIAN_POINT ( 'NONE',  ( 2.632061376486628301, -0.4999999999999997780, -1.949999999999999956 ) ) ;
#6357=CARTESIAN_POINT ( 'NONE',  ( 20.69942760064479259, -21.74528614261434711, 1.396244390126957224 ) ) ;
#6359=DIRECTION ( 'NONE',  ( 0.1908089953765452762, 0.000000000000000000, 0.9816271834476639757 ) ) ;
#6360=CARTESIAN_POINT ( 'NONE',  ( -23.35000000000000142, -10.96966150227469505, 4.500000000000000888 ) ) ;
#6361=CARTESIAN_POINT ( 'NONE',  ( 21.08401840680159367, -16.78474387324287775, 1.500000000000000000 ) ) ;
#6365=ORIENTED_EDGE ( 'NONE', *, *, #13487, .T. ) ;
#6370=VERTEX_POINT ( 'NONE', #23100 ) ;
#6376=CARTESIAN_POINT ( 'NONE',  ( -4.121060316658296863, -7.626742303306310866, -1.744488848298825223 ) ) ;
#6378=CARTESIAN_POINT ( 'NONE',  ( 9.555580689062686872, -12.32072190999758021, -1.500000000000000000 ) ) ;
#6386=CARTESIAN_POINT ( 'NONE',  ( -2.386718424894567203, -9.330009425478154483, 4.522129901861158707 ) ) ;
#6391=CARTESIAN_POINT ( 'NONE',  ( 107.4223672430906049, -16.96176113054595547, -3.705237567694021461 ) ) ;
#6392=EDGE_CURVE ( 'NONE', #1933, #9859, #5150, .T. ) ;
#6398=CARTESIAN_POINT ( 'NONE',  ( 21.19329141388233850, -21.80292992253813367, -1.345625751489397226 ) ) ;
#6405=B_SPLINE_CURVE_WITH_KNOTS ( 'NONE', 3,
 ( #10229, #2562, #5226, #19964, #14899, #27629, #25104, #12409, #19769, #10058 ),
 .UNSPECIFIED., .F., .F.,
 ( 4, 2, 2, 2, 4 ),
 ( 1.387948177032400748E-17, 0.002010218194407704159, 0.003015327291611544312, 0.003517881840213458750, 0.004020436388815372755 ),
 .UNSPECIFIED. ) ;
#6406=CARTESIAN_POINT ( 'NONE',  ( 25.42756288599143133, -17.55292975162308267, -1.197473197311734294 ) ) ;
#6413=VECTOR ( 'NONE', #24203, 1000.000000000000000 ) ;
#6417=CARTESIAN_POINT ( 'NONE',  ( -50.60000000000000142, -10.96966150227468972, 1.500000000000000000 ) ) ;
#6421=CARTESIAN_POINT ( 'NONE',  ( 108.0282448396077797, -18.47608078053866265, 4.361986266605526907 ) ) ;
#6425=FACE_OUTER_BOUND ( 'NONE', #5285, .T. ) ;
#6437=CARTESIAN_POINT ( 'NONE',  ( 7.166310626577053533, -7.340520188511631794, 1.000000000000000000 ) ) ;
#6438=ORIENTED_EDGE ( 'NONE', *, *, #26427, .T. ) ;
#6439=CARTESIAN_POINT ( 'NONE',  ( 21.08401840680096129, -16.78474387324269657, -1.500000000000000000 ) ) ;
#6440=VERTEX_POINT ( 'NONE', #20260 ) ;
#6441=CARTESIAN_POINT ( 'NONE',  ( 2.820807997218022223, -11.54323945762161507, 1.759797141769505968 ) ) ;
#6448=AXIS2_PLACEMENT_3D ( 'NONE', #32392, #9451, #16650 ) ;
#6451=VECTOR ( 'NONE', #30735, 999.9999999999998863 ) ;
#6452=CARTESIAN_POINT ( 'NONE',  ( 24.09939086539479192, -17.43210107469705861, -1.523452847364070939 ) ) ;
#6456=CARTESIAN_POINT ( 'NONE',  ( 23.07496354194262977, -21.92049040218789457, -1.202267097226756176 ) ) ;
#6461=ORIENTED_EDGE ( 'NONE', *, *, #25064, .T. ) ;
#6470=CARTESIAN_POINT ( 'NONE',  ( 25.43628654896337693, -17.54453578616444176, -1.000000000000000000 ) ) ;
#6472=CARTESIAN_POINT ( 'NONE',  ( 110.4915906369627123, -18.78144465615450187, 4.522129901861159595 ) ) ;
#6473=B_SPLINE_CURVE_WITH_KNOTS ( 'NONE', 3,
 ( #22080, #9358, #32108, #9184, #27236, #19568, #29764, #22239 ),
 .UNSPECIFIED., .F., .F.,
 ( 4, 2, 2, 4 ),
 ( 0.000000000000000000, 0.0003683317334693677692, 0.0007366634669387355384, 0.001473326933877471077 ),
 .UNSPECIFIED. ) ;
#6474=ORIENTED_EDGE ( 'NONE', *, *, #612, .T. ) ;
#6503=EDGE_LOOP ( 'NONE', ( #11061, #15462, #7917, #22388, #31779, #15868 ) ) ;
#6514=CARTESIAN_POINT ( 'NONE',  ( 23.22564588060107482, -21.93932300456764040, -1.000000000000000000 ) ) ;
#6517=AXIS2_PLACEMENT_3D ( 'NONE', #30414, #17693, #22883 ) ;
#6528=CARTESIAN_POINT ( 'NONE',  ( -4.060002436691794614, -5.088205424081681194, -1.745854636721019260 ) ) ;
#6531=CIRCLE ( 'NONE', #30065, 4.999999999999997335 ) ;
#6534=DIRECTION ( 'NONE',  ( 0.8616149568369098066, -0.5075624751249150357, 0.000000000000000000 ) ) ;
#6541=VECTOR ( 'NONE', #370, 1000.000000000000000 ) ;
#6546=VERTEX_POINT ( 'NONE', #6514 ) ;
#6549=B_SPLINE_CURVE_WITH_KNOTS ( 'NONE', 3,
 ( #7968, #30746, #20352, #31233, #15670, #15826, #10128, #20694, #5145, #31053, #5300, #12994, #15478, #18010, #20842, #30564, #8309, #28364, #28698, #25373, #7652, #23204 ),
 .UNSPECIFIED., .F., .F.,
 ( 4, 3, 3, 3, 3, 3, 3, 4 ),
 ( 1.041059936534947552E-17, 0.0001461945829181783975, 0.0002459472205448162371, 0.0003138760397545359141, 0.0003818610883897723303, 0.0004082995574110840752, 0.0004281800295585239330, 0.0004357603615204788520 ),
 .UNSPECIFIED. ) ;
#6565=LINE ( 'NONE', #26964, #9684 ) ;
#6566=AXIS2_PLACEMENT_3D ( 'NONE', #24024, #13675, #3823 ) ;
#6567=CARTESIAN_POINT ( 'NONE',  ( 9.126991456844553596, -11.32614230912571429, -1.000000000000000000 ) ) ;
#6568=CARTESIAN_POINT ( 'NONE',  ( 108.0265109756391553, -18.45111357072248737, -4.417761971609380112 ) ) ;
#6577=CARTESIAN_POINT ( 'NONE',  ( -50.60000000000000142, 0.000000000000000000, 1.000000000000000000 ) ) ;
#6586=CARTESIAN_POINT ( 'NONE',  ( 20.55463713078601629, -21.58103817311699402, 1.582345582279547358 ) ) ;
#6595=CARTESIAN_POINT ( 'NONE',  ( 21.36097421961356702, -21.76718868951428121, -1.410897148389125277 ) ) ;
#6605=CARTESIAN_POINT ( 'NONE',  ( 21.64920974929931674, -21.84574742533145297, 1.293063406869986443 ) ) ;
#6609=EDGE_CURVE ( 'NONE', #4684, #11449, #31012, .T. ) ;
#6611=ADVANCED_FACE ( 'NONE', ( #6688 ), #19563, .F. ) ;
#6620=CYLINDRICAL_SURFACE ( 'NONE', #20904, 4.999999999999997335 ) ;
#6626=CARTESIAN_POINT ( 'NONE',  ( 8.706508904963646600, -1.271749511502713093, 1.500000000000000222 ) ) ;
#6628=CARTESIAN_POINT ( 'NONE',  ( 9.836026323042709407, -12.51705112700696176, -1.500000000000000444 ) ) ;
#6631=CARTESIAN_POINT ( 'NONE',  ( 0.1360978363991151296, -7.042592391184042455, 1.774497828403761579 ) ) ;
#6635=CARTESIAN_POINT ( 'NONE',  ( 8.862909208978498654, -0.2945138977690187065, -1.470869863057391980 ) ) ;
#6638=CARTESIAN_POINT ( 'NONE',  ( 22.19921710918831081, -17.00655848932595049, -1.494769569001199727 ) ) ;
#6658=CARTESIAN_POINT ( 'NONE',  ( -31.57659242536668032, 0.000000000000000000, -1.500000000000000000 ) ) ;
#6659=FACE_OUTER_BOUND ( 'NONE', #30374, .T. ) ;
#6662=FACE_OUTER_BOUND ( 'NONE', #3501, .T. ) ;
#6684=CARTESIAN_POINT ( 'NONE',  ( 0.8808402398300805292, -9.175602370491700910, -1.499999999999930056 ) ) ;
#6686=VERTEX_POINT ( 'NONE', #4346 ) ;
#6688=FACE_OUTER_BOUND ( 'NONE', #19983, .T. ) ;
#6691=CARTESIAN_POINT ( 'NONE',  ( -14.62340757463330654, -21.93932300455828255, -1.292893218813452538 ) ) ;
#6699=CARTESIAN_POINT ( 'NONE',  ( 3.744708216408842549, 0.000000000000000000, -1.000000000000000000 ) ) ;
#6706=ORIENTED_EDGE ( 'NONE', *, *, #30019, .T. ) ;
#6707=CARTESIAN_POINT ( 'NONE',  ( 21.24324854073028490, -21.72960979489713651, 1.457811124649513346 ) ) ;
#6720=ADVANCED_FACE ( 'NONE', ( #7341 ), #2666, .T. ) ;
#6723=CARTESIAN_POINT ( 'NONE',  ( -4.526546459660798938, -7.591509378209715386, -1.500000000000000888 ) ) ;
#6728=CARTESIAN_POINT ( 'NONE',  ( 7.168700580349904428, -6.410142746794999624, -1.000000000000000000 ) ) ;
#6730=CARTESIAN_POINT ( 'NONE',  ( 107.4616889483734212, -17.52894894125598313, -4.827028120670242117 ) ) ;
#6734=CARTESIAN_POINT ( 'NONE',  ( 21.36097421961356702, -21.76718868951428121, -1.410897148389125277 ) ) ;
#6736=CARTESIAN_POINT ( 'NONE',  ( 24.65887284179023453, -17.47660047452463772, -1.497285395512024442 ) ) ;
#6737=CARTESIAN_POINT ( 'NONE',  ( -0.9232102171129843438, 0.000000000000000000, 4.522129901861158707 ) ) ;
#6744=CARTESIAN_POINT ( 'NONE',  ( 2.535833972131074976, -0.1672301947041132664, -1.432210082195892520 ) ) ;
#6745=ORIENTED_EDGE ( 'NONE', *, *, #26662, .T. ) ;
#6746=CARTESIAN_POINT ( 'NONE',  ( 1.449793745490414176, -2.781154674314748831, -1.500000000000000222 ) ) ;
#6767=CARTESIAN_POINT ( 'NONE',  ( -1.023266466338763614, -9.291661594692715909, -5.485967528433937979 ) ) ;
#6777=ORIENTED_EDGE ( 'NONE', *, *, #11575, .F. ) ;
#6787=CARTESIAN_POINT ( 'NONE',  ( 12.23122861076465817, -15.17374145964417842, 1.499999999999998668 ) ) ;
#6792=CARTESIAN_POINT ( 'NONE',  ( 9.350000000000004974, 2.117582368135760237E-19, -1.049909311857671668 ) ) ;
#6799=CARTESIAN_POINT ( 'NONE',  ( 23.19643008672645124, -21.93767770566458353, -1.043375197815119115 ) ) ;
#6808=DIRECTION ( 'NONE',  ( -1.000000000000000000, 0.000000000000000000, 0.000000000000000000 ) ) ;
#6810=CARTESIAN_POINT ( 'NONE',  ( 0.000000000000000000, 0.000000000000000000, 4.137834579201376428 ) ) ;
#6813=DIRECTION ( 'NONE',  ( 0.000000000000000000, 0.000000000000000000, -1.000000000000000000 ) ) ;
#6830=DIRECTION ( 'NONE',  ( -1.000000000000000000, 0.000000000000000000, 0.000000000000000000 ) ) ;
#6836=CARTESIAN_POINT ( 'NONE',  ( 1.306676087840223266, -9.318305894662934463, -1.500000000000000000 ) ) ;
#6850=CARTESIAN_POINT ( 'NONE',  ( -4.067282153467298045, -9.772827192342422364, -1.500000000000000000 ) ) ;
#6877=CARTESIAN_POINT ( 'NONE',  ( 8.996310305901872084, 0.3994363609773625701, -1.500000000000000000 ) ) ;
#6878=CARTESIAN_POINT ( 'NONE',  ( 107.4976397712979690, -18.05149321335032297, -5.137684681196807546 ) ) ;
#6879=ORIENTED_EDGE ( 'NONE', *, *, #30380, .T. ) ;
#6881=ADVANCED_FACE ( 'NONE', ( #29026 ), #8908, .T. ) ;
#6893=CARTESIAN_POINT ( 'NONE',  ( -23.35000000000000142, -10.96966150227469505, -11.00000000000000000 ) ) ;
#6896=CARTESIAN_POINT ( 'NONE',  ( 2.692942092879388127, -0.02443046219423555473, -1.307625729273671933 ) ) ;
#6898=CARTESIAN_POINT ( 'NONE',  ( 7.153595758147059946, -6.747833800172327479, 1.000000000000000222 ) ) ;
#6907=EDGE_CURVE ( 'NONE', #140, #697, #11110, .T. ) ;
#6909=ORIENTED_EDGE ( 'NONE', *, *, #25996, .F. ) ;
#6911=CARTESIAN_POINT ( 'NONE',  ( -4.317168503051449946, -7.715934794172482292, 1.500000000000000000 ) ) ;
#6935=CARTESIAN_POINT ( 'NONE',  ( 21.97279447062591018, -21.86582820552294493, -1.264434309188650518 ) ) ;
#6941=ORIENTED_EDGE ( 'NONE', *, *, #24802, .F. ) ;
#6942=CARTESIAN_POINT ( 'NONE',  ( 7.167971118698460486, -13.96529319322445062, 1.755547229797913333 ) ) ;
#6946=CARTESIAN_POINT ( 'NONE',  ( -4.497573025205830355, -5.387589684568504289, 1.499999999999999556 ) ) ;
#6955=CARTESIAN_POINT ( 'NONE',  ( -2.775371991354582679, -0.000000000000000000, 1.260159510457126819 ) ) ;
#6956=CARTESIAN_POINT ( 'NONE',  ( 23.00622743562070482, -21.91302709721476205, -1.171678142438169701 ) ) ;
#6957=CYLINDRICAL_SURFACE ( 'NONE', #17260, 0.5000000000000000000 ) ;
#6959=VERTEX_POINT ( 'NONE', #31807 ) ;
#6962=CARTESIAN_POINT ( 'NONE',  ( -2.386718424894326063, -9.330009425477191698, -4.522129901861166701 ) ) ;
#6966=EDGE_CURVE ( 'NONE', #2672, #7938, #4051, .T. ) ;
#6968=CARTESIAN_POINT ( 'NONE',  ( 25.29730119701314450, -17.51801463888119059, -1.124408821416490900 ) ) ;
#6982=CARTESIAN_POINT ( 'NONE',  ( -48.50000000000000000, -10.96966150227468972, 7.500000000000000000 ) ) ;
#6998=CARTESIAN_POINT ( 'NONE',  ( 6.555809470822123508, -13.70807884655583742, -1.755773249082955623 ) ) ;
#7006=ORIENTED_EDGE ( 'NONE', *, *, #15477, .F. ) ;
#7007=EDGE_CURVE ( 'NONE', #31320, #31825, #21944, .T. ) ;
#7008=CARTESIAN_POINT ( 'NONE',  ( 21.08401840680222961, -16.78474387324145667, 1.499999999999999556 ) ) ;
#7015=EDGE_CURVE ( 'NONE', #11567, #15410, #31039, .T. ) ;
#7020=CARTESIAN_POINT ( 'NONE',  ( 14.53974964220209110, -20.67385035929880743, -1.499999999999056088 ) ) ;
#7025=ORIENTED_EDGE ( 'NONE', *, *, #22706, .T. ) ;
#7032=ORIENTED_EDGE ( 'NONE', *, *, #10444, .T. ) ;
#7039=DIRECTION ( 'NONE',  ( -0.06927878976713691683, 0.9975973382524639943, 0.000000000000000000 ) ) ;
#7051=DIRECTION ( 'NONE',  ( 0.000000000000000000, 0.000000000000000000, 1.000000000000000000 ) ) ;
#7053=CARTESIAN_POINT ( 'NONE',  ( -4.184188163278487416, -5.072310292433697576, 1.499999999999960254 ) ) ;
#7054=CARTESIAN_POINT ( 'NONE',  ( 7.637044423815050109, -3.948987408040151248, -1.000000000000000000 ) ) ;
#7056=CARTESIAN_POINT ( 'NONE',  ( 107.9522086517191468, -17.38117859037711810, -4.648913506406474383 ) ) ;
#7069=CARTESIAN_POINT ( 'NONE',  ( 0.000000000000000000, -25.93932300454937945, 11.00000000000000000 ) ) ;
#7072=B_SPLINE_CURVE_WITH_KNOTS ( 'NONE', 3,
 ( #29116, #13557, #1369, #26752, #3697, #5860, #31308, #11545 ),
 .UNSPECIFIED., .F., .F.,
 ( 4, 2, 2, 4 ),
 ( 0.000000000000000000, 0.0002326964511452904059, 0.0004653929022905808118, 0.0009307858045811711646 ),
 .UNSPECIFIED. ) ;
#7080=CARTESIAN_POINT ( 'NONE',  ( 1.386174007446685286, -9.662292653395718744, -0.9788672205888330202 ) ) ;
#7081=ORIENTED_EDGE ( 'NONE', *, *, #2150, .F. ) ;
#7083=EDGE_LOOP ( 'NONE', ( #8512, #5227, #32262, #4383, #7950, #26476, #29095, #6745 ) ) ;
#7085=ORIENTED_EDGE ( 'NONE', *, *, #7324, .T. ) ;
#7096=CARTESIAN_POINT ( 'NONE',  ( 108.1288400433390393, -19.92462668933126579, -1.384270303710054328 ) ) ;
#7098=CYLINDRICAL_SURFACE ( 'NONE', #16545, 2.099999999999997868 ) ;
#7101=EDGE_CURVE ( 'NONE', #937, #8978, #20361, .T. ) ;
#7107=CARTESIAN_POINT ( 'NONE',  ( -1.694237876702965329, -1.500727999663087564, -4.522129901861166701 ) ) ;
#7112=CARTESIAN_POINT ( 'NONE',  ( 6.270432871727738444, -15.60322400927903175, 5.485967528433933538 ) ) ;
#7113=AXIS2_PLACEMENT_3D ( 'NONE', #31371, #5936, #5294 ) ;
#7130=DIRECTION ( 'NONE',  ( 1.000000000000000000, 0.000000000000000000, 0.000000000000000000 ) ) ;
#7131=( NAMED_UNIT ( * ) SI_UNIT ( $, .STERADIAN. ) SOLID_ANGLE_UNIT ( ) );
#7132=EDGE_CURVE ( 'NONE', #11567, #3025, #28849, .T. ) ;
#7134=CARTESIAN_POINT ( 'NONE',  ( 10.91172402966645905, -15.11896842049539380, 1.500000000000139000 ) ) ;
#7138=CARTESIAN_POINT ( 'NONE',  ( -4.526559146999415972, -7.591385338581535969, 1.500000000000000222 ) ) ;
#7148=EDGE_CURVE ( 'NONE', #32996, #10544, #30197, .T. ) ;
#7157=CARTESIAN_POINT ( 'NONE',  ( -50.60000000000000142, -0.5000000000000000000, -1.000000000000000000 ) ) ;
#7164=ORIENTED_EDGE ( 'NONE', *, *, #740, .F. ) ;
#7188=CARTESIAN_POINT ( 'NONE',  ( 4.970124631802561588, -12.47916550509082612, -1.500000000000001332 ) ) ;
#7204=CARTESIAN_POINT ( 'NONE',  ( 2.087757557787927265, -16.81476909109668938, -1.499999999999999112 ) ) ;
#7210=DIRECTION ( 'NONE',  ( -0.9816271834476628655, 0.000000000000000000, 0.1908089953765502444 ) ) ;
#7211=ORIENTED_EDGE ( 'NONE', *, *, #6240, .F. ) ;
#7228=ORIENTED_EDGE ( 'NONE', *, *, #14811, .F. ) ;
#7233=CARTESIAN_POINT ( 'NONE',  ( 108.0225149428689377, -18.39357169291826466, -4.507139740279709095 ) ) ;
#7246=( BOUNDED_SURFACE ( )  B_SPLINE_SURFACE ( 3, 2, ( 
 ( #12242, #32179, #24611 ),
 ( #9916, #19972, #25115 ),
 ( #1563, #6744, #14759 ),
 ( #16935, #6896, #9563 ),
 ( #27130, #24956, #22139 ),
 ( #4231, #1923, #9748 ),
 ( #14401, #7397, #30175 ),
 ( #32349, #7248, #17439 ),
 ( #9412, #4906, #12421 ),
 ( #30326, #29820, #17090 ) ),
 .UNSPECIFIED., .F., .F., .F. ) 
 B_SPLINE_SURFACE_WITH_KNOTS ( ( 4, 2, 2, 2, 4 ),
 ( 3, 3 ),
 ( 0.003636727685402253371, 0.004103800047000620739, 0.004570872408598988107, 0.005037944770197356342, 0.005505017131795723710 ),
 ( 0.000000000000000000, 1.000000000000000000 ),
 .UNSPECIFIED. ) 
 GEOMETRIC_REPRESENTATION_ITEM ( )  RATIONAL_B_SPLINE_SURFACE ( (
 ( 1.000000000000000000, 0.8449619147701442623, 1.000000000000000000),
 ( 1.000000000000000000, 0.8255905392900951822, 1.000000000000000000),
 ( 1.000000000000000000, 0.8027571906105874788, 1.000000000000000000),
 ( 1.000000000000000000, 0.7529839109803941888, 1.000000000000000000),
 ( 1.000000000000000000, 0.7260803501548076522, 1.000000000000000000),
 ( 1.000000000000000000, 0.6677408092241539084, 1.000000000000000000),
 ( 1.000000000000000000, 0.6373774895459817236, 1.000000000000000000),
 ( 1.000000000000000000, 0.5732936775528050255, 1.000000000000000000),
 ( 1.000000000000000000, 0.5402556527143969056, 1.000000000000000000),
 ( 1.000000000000000000, 0.5090209295198725448, 1.000000000000000000) ) ) 
 REPRESENTATION_ITEM ( '' )  SURFACE ( )  );
#7248=CARTESIAN_POINT ( 'NONE',  ( 3.066081126419267111, 0.08824576070990676480, -0.7648597189984557287 ) ) ;
#7250=CARTESIAN_POINT ( 'NONE',  ( 1.206392348548081639, -3.371890407423572267, -1.499999999999999334 ) ) ;
#7253=ADVANCED_FACE ( 'NONE', ( #14436 ), #9778, .F. ) ;
#7261=CARTESIAN_POINT ( 'NONE',  ( 108.1296380701674593, -19.93611807713620010, -1.386936492580776559 ) ) ;
#7269=CARTESIAN_POINT ( 'NONE',  ( 24.76851591958510213, -17.41692718791932748, 1.262548836151062615 ) ) ;
#7270=DIRECTION ( 'NONE',  ( -0.000000000000000000, -0.000000000000000000, -1.000000000000000000 ) ) ;
#7271=CARTESIAN_POINT ( 'NONE',  ( -1.033057378353323452, -8.048844657540879410, 4.522129901861156931 ) ) ;
#7287=CARTESIAN_POINT ( 'NONE',  ( -2.600000000000000089, 0.000000000000000000, -1.499999999999999556 ) ) ;
#7298=CARTESIAN_POINT ( 'NONE',  ( 21.57350866840246439, -21.75854512865358714, -1.480343326970304130 ) ) ;
#7299=CARTESIAN_POINT ( 'NONE',  ( -50.60000000000000142, -10.96966150227468972, 1.000000000000000000 ) ) ;
#7310=CARTESIAN_POINT ( 'NONE',  ( 22.98163386837131839, -21.92547295135293695, 1.118948288781482558 ) ) ;
#7311=B_SPLINE_CURVE_WITH_KNOTS ( 'NONE', 3,
 ( #3715, #13393, #18759, #21758 ),
 .UNSPECIFIED., .F., .F.,
 ( 4, 4 ),
 ( 0.000000000000000000, 0.0001149031832736470529 ),
 .UNSPECIFIED. ) ;
#7320=CARTESIAN_POINT ( 'NONE',  ( 3.707192301029357484, -12.18036120888841722, 1.758115348676513534 ) ) ;
#7322=ORIENTED_EDGE ( 'NONE', *, *, #20839, .F. ) ;
#7324=EDGE_CURVE ( 'NONE', #10078, #30308, #2309, .T. ) ;
#7337=CARTESIAN_POINT ( 'NONE',  ( 0.3600058077333471163, -8.266758618787918067, -1.772551491157698278 ) ) ;
#7338=CARTESIAN_POINT ( 'NONE',  ( 72.52374898132006820, -19.78015497542561008, 4.522129901861157819 ) ) ;
#7341=FACE_OUTER_BOUND ( 'NONE', #24054, .T. ) ;
#7344=ORIENTED_EDGE ( 'NONE', *, *, #9454, .F. ) ;
#7345=CARTESIAN_POINT ( 'NONE',  ( 23.32053031413205701, -17.41627278853337657, 1.661539697405882032 ) ) ;
#7348=CARTESIAN_POINT ( 'NONE',  ( -15.71515769256210504, -10.96966150227469505, -11.09540449768827308 ) ) ;
#7353=CARTESIAN_POINT ( 'NONE',  ( -3.674149904271398537, -10.80265656036293720, -1.500000000000000000 ) ) ;
#7379=CARTESIAN_POINT ( 'NONE',  ( -0.3880080537174205313, -2.647099810593992242, 4.522129901861156931 ) ) ;
#7380=DIRECTION ( 'NONE',  ( 0.000000000000000000, 0.000000000000000000, -1.000000000000000000 ) ) ;
#7381=CARTESIAN_POINT ( 'NONE',  ( 8.060276135842835643, -2.738905749622889019, -1.500000000000000888 ) ) ;
#7382=CARTESIAN_POINT ( 'NONE',  ( 107.5622791870681993, -18.99089674742949541, -4.502190851498308888 ) ) ;
#7395=DIRECTION ( 'NONE',  ( 0.000000000000000000, 0.000000000000000000, -1.000000000000000000 ) ) ;
#7397=CARTESIAN_POINT ( 'NONE',  ( 2.974466146320791093, 0.1107971263338030782, -0.9540093664866172718 ) ) ;
#7400=VERTEX_POINT ( 'NONE', #5429 ) ;
#7403=CARTESIAN_POINT ( 'NONE',  ( -2.753702574461988295, -0.2727682784858956322, 1.454428814729294972 ) ) ;
#7408=EDGE_LOOP ( 'NONE', ( #124, #24687, #30320, #7081, #2464 ) ) ;
#7414=DIRECTION ( 'NONE',  ( 1.000000000000000000, 0.000000000000000000, 0.000000000000000000 ) ) ;
#7418=ADVANCED_FACE ( 'NONE', ( #17617 ), #5724, .T. ) ;
#7420=CARTESIAN_POINT ( 'NONE',  ( -0.3880080537174205313, -2.647099810593992242, 4.522129901861156931 ) ) ;
#7422=CARTESIAN_POINT ( 'NONE',  ( 107.6641948605100083, -20.45809826282308208, 1.500000000000000000 ) ) ;
#7433=CARTESIAN_POINT ( 'NONE',  ( 107.9814001905993734, -17.80152948830060211, 4.369786445662967367 ) ) ;
#7440=CARTESIAN_POINT ( 'NONE',  ( 0.6620495146783516027, -15.34493536057754248, 1.745995208913456720 ) ) ;
#7448=CARTESIAN_POINT ( 'NONE',  ( 21.36097421961356702, -21.76718868951428121, -1.410897148389125277 ) ) ;
#7452=FACE_BOUND ( 'NONE', #33006, .T. ) ;
#7457=B_SPLINE_CURVE_WITH_KNOTS ( 'NONE', 3,
 ( #17349, #26883, #24360, #1632, #9470, #1476, #16843, #11821, #9315, #2126, #6962, #27040, #12307, #19530, #24862, #11652 ),
 .UNSPECIFIED., .F., .F.,
 ( 4, 2, 2, 2, 2, 2, 2, 4 ),
 ( 0.01324599089037892946, 0.5000000000000001110, 0.6250000000000000000, 0.7500000000000000000, 0.8125000000000000000, 0.8750000000000000000, 0.9375000000000000000, 1.000000000000000000 ),
 .UNSPECIFIED. ) ;
#7459=CARTESIAN_POINT ( 'NONE',  ( 23.71271855738292800, -17.43088677775545392, -1.604577790254563485 ) ) ;
#7462=CARTESIAN_POINT ( 'NONE',  ( 22.68241379554079629, -21.87740465772228049, 1.258814731509616758 ) ) ;
#7465=EDGE_LOOP ( 'NONE', ( #13176, #16599, #25351 ) ) ;
#7469=CARTESIAN_POINT ( 'NONE',  ( 108.0821972398986617, -20.20655521172211166, 1.448620529800545897 ) ) ;
#7472=VERTEX_POINT ( 'NONE', #3735 ) ;
#7486=EDGE_CURVE ( 'NONE', #23391, #30204, #20976, .T. ) ;
#7488=VERTEX_POINT ( 'NONE', #5902 ) ;
#7507=AXIS2_PLACEMENT_3D ( 'NONE', #12185, #16532, #4528 ) ;
#7513=CARTESIAN_POINT ( 'NONE',  ( -2.559200518355241094, -12.25278053493027031, -1.499999999999920064 ) ) ;
#7529=VERTEX_POINT ( 'NONE', #19963 ) ;
#7532=FACE_OUTER_BOUND ( 'NONE', #6503, .T. ) ;
#7539=VERTEX_POINT ( 'NONE', #32493 ) ;
#7542=CARTESIAN_POINT ( 'NONE',  ( 107.4500373638809947, -17.36019379023286646, 4.522129901861156931 ) ) ;
#7543=CARTESIAN_POINT ( 'NONE',  ( 0.5106493704296974911, -15.23275403072758216, 1.745873292837237800 ) ) ;
#7579=ORIENTED_EDGE ( 'NONE', *, *, #31759, .F. ) ;
#7581=CARTESIAN_POINT ( 'NONE',  ( -2.971049596204458076, -0.1846667992746918174, 1.395223860601304100 ) ) ;
#7585=ORIENTED_EDGE ( 'NONE', *, *, #491, .T. ) ;
#7599=DIRECTION ( 'NONE',  ( 6.938893903907222067E-15, 0.000000000000000000, 1.000000000000000000 ) ) ;
#7603=CARTESIAN_POINT ( 'NONE',  ( -2.889143798718842415, 0.000000000000000000, 0.9788672205877712029 ) ) ;
#7604=CARTESIAN_POINT ( 'NONE',  ( -15.12340757463330654, -27.93932300454937590, -1.000000000000000000 ) ) ;
#7619=DIRECTION ( 'NONE',  ( 0.000000000000000000, 0.000000000000000000, 1.000000000000000000 ) ) ;
#7622=ORIENTED_EDGE ( 'NONE', *, *, #22115, .T. ) ;
#7635=ORIENTED_EDGE ( 'NONE', *, *, #31428, .F. ) ;
#7639=CARTESIAN_POINT ( 'NONE',  ( 21.49636748197312386, -21.75484023020513646, -1.469027763226378847 ) ) ;
#7642=ORIENTED_EDGE ( 'NONE', *, *, #6001, .T. ) ;
#7645=DIRECTION ( 'NONE',  ( 1.000000000000000000, 0.000000000000000000, 0.000000000000000000 ) ) ;
#7649=CIRCLE ( 'NONE', #19922, 4.999999999999997335 ) ;
#7652=CARTESIAN_POINT ( 'NONE',  ( 24.39739546318580565, -17.41185525199284001, 1.419135974561906099 ) ) ;
#7655=CARTESIAN_POINT ( 'NONE',  ( 22.90158751868941778, -21.92087667321492006, 1.135468510342883652 ) ) ;
#7663=CARTESIAN_POINT ( 'NONE',  ( 1.055238632343717731, -2.663178554379440399, 1.761001113085417957 ) ) ;
#7669=ORIENTED_EDGE ( 'NONE', *, *, #26525, .F. ) ;
#7674=EDGE_CURVE ( 'NONE', #4392, #10617, #13800, .T. ) ;
#7675=VECTOR ( 'NONE', #32758, 1000.000000000000000 ) ;
#7677=CARTESIAN_POINT ( 'NONE',  ( -29.24402871571405882, 0.000000000000000000, 11.00000000000000000 ) ) ;
#7686=CARTESIAN_POINT ( 'NONE',  ( 0.1962428234089072521, -6.885380501030516243, 1.500000000000000444 ) ) ;
#7690=B_SPLINE_CURVE_WITH_KNOTS ( 'NONE', 3,
 ( #17061, #4391, #14573, #12073, #22268, #31817, #24278, #1392, #30152, #17417 ),
 .UNSPECIFIED., .F., .F.,
 ( 4, 3, 3, 4 ),
 ( 2.540777767531316248E-16, 0.001000000000058556262, 0.002000000000115103715, 0.003363950672707366474 ),
 .UNSPECIFIED. ) ;
#7694=CARTESIAN_POINT ( 'NONE',  ( 24.31705961743306332, -17.33693665021637287, 1.331050360517170850 ) ) ;
#7698=CARTESIAN_POINT ( 'NONE',  ( 21.08401840680096129, -16.78474387324269657, -1.500000000000000000 ) ) ;
#7703=CARTESIAN_POINT ( 'NONE',  ( 0.5690620474499710202, -15.77263461755453910, -1.499999999999999112 ) ) ;
#7704=B_SPLINE_CURVE_WITH_KNOTS ( 'NONE', 3,
 ( #15007, #32935, #10005, #31400, #645, #30918 ),
 .UNSPECIFIED., .F., .F.,
 ( 4, 2, 4 ),
 ( -1.393543241286607919E-05, 0.0003807901956958054720, 0.0007755158238044769503 ),
 .UNSPECIFIED. ) ;
#7729=VERTEX_POINT ( 'NONE', #30473 ) ;
#7733=CARTESIAN_POINT ( 'NONE',  ( -2.787252791270956376, -12.40549665431308846, 1.499999999999999556 ) ) ;
#7737=CARTESIAN_POINT ( 'NONE',  ( 107.5620253939523820, -18.98724223319534232, -4.512175692148537642 ) ) ;
#7742=EDGE_CURVE ( 'NONE', #15410, #29829, #23053, .T. ) ;
#7756=CARTESIAN_POINT ( 'NONE',  ( 1.565787006715317453, -2.348723853601462075, -0.9788672205888330202 ) ) ;
#7761=ORIENTED_EDGE ( 'NONE', *, *, #302, .F. ) ;
#7762=CARTESIAN_POINT ( 'NONE',  ( 107.4811514614839325, -17.81167296463705085, 5.070933786246803798 ) ) ;
#7772=CARTESIAN_POINT ( 'NONE',  ( 0.1764088899269929123, -7.476879701952443114, -1.774401973390820952 ) ) ;
#7773=DIRECTION ( 'NONE',  ( -1.000000000000000000, 0.000000000000000000, 0.000000000000000000 ) ) ;
#7774=CARTESIAN_POINT ( 'NONE',  ( 19.46384663066824672, -15.80031286499690069, -0.9999999999998614442 ) ) ;
#7775=CARTESIAN_POINT ( 'NONE',  ( 107.9409393647361668, -17.21890366125716199, 3.165031064497942470 ) ) ;
#7791=CARTESIAN_POINT ( 'NONE',  ( -18.35000000000000142, -10.96966150227469505, 1.500000000000000000 ) ) ;
#7796=ORIENTED_EDGE ( 'NONE', *, *, #20179, .F. ) ;
#7799=CARTESIAN_POINT ( 'NONE',  ( 3.566513200368869096, -17.47573827932033197, -1.499999999999999556 ) ) ;
#7800=EDGE_LOOP ( 'NONE', ( #20540, #28435, #28031, #15230 ) ) ;
#7806=ORIENTED_EDGE ( 'NONE', *, *, #31710, .T. ) ;
#7809=DIRECTION ( 'NONE',  ( -0.000000000000000000, 0.000000000000000000, 1.000000000000000000 ) ) ;
#7812=VERTEX_POINT ( 'NONE', #31309 ) ;
#7829=CARTESIAN_POINT ( 'NONE',  ( 7.193574579132851810, -9.614801642835368867, 1.500000000000000000 ) ) ;
#7831=CARTESIAN_POINT ( 'NONE',  ( 21.48306690750116132, -21.75443153431600152, 1.466605545616818995 ) ) ;
#7854=EDGE_CURVE ( 'NONE', #2520, #30204, #25731, .T. ) ;
#7856=ADVANCED_FACE ( 'NONE', ( #16386 ), #16046, .T. ) ;
#7874=CARTESIAN_POINT ( 'NONE',  ( 14.13431920379513862, -20.70626837987542856, 1.500000000000000000 ) ) ;
#7880=CARTESIAN_POINT ( 'NONE',  ( 107.6134620356101550, -19.72758389683053437, 2.997181592065166988 ) ) ;
#7882=CARTESIAN_POINT ( 'NONE',  ( 5.492556933410833508, -18.10995529321820641, 1.499999999999526157 ) ) ;
#7892=DIRECTION ( 'NONE',  ( -1.000000000000000000, 0.000000000000000000, 0.000000000000000000 ) ) ;
#7900=B_SPLINE_CURVE_WITH_KNOTS ( 'NONE', 3,
 ( #16830, #27030, #4131, #14299, #10623, #15308 ),
 .UNSPECIFIED., .F., .F.,
 ( 4, 2, 4 ),
 ( -5.999999986713436683E-08, 0.0003820452512025651701, 0.0007641505024049974944 ),
 .UNSPECIFIED. ) ;
#7903=CARTESIAN_POINT ( 'NONE',  ( -1.170068671574743036, -6.059534462705075342, -4.522129901861164925 ) ) ;
#7904=CARTESIAN_POINT ( 'NONE',  ( 9.970488656677847672, -12.00323977417178867, 1.000000000000000000 ) ) ;
#7908=CARTESIAN_POINT ( 'NONE',  ( 107.5617723795404999, -18.98359893170737323, 4.522129901861158707 ) ) ;
#7910=ORIENTED_EDGE ( 'NONE', *, *, #22639, .F. ) ;
#7916=CARTESIAN_POINT ( 'NONE',  ( 71.67787245194618606, -18.34520463695562498, 1.500000000000000000 ) ) ;
#7917=ORIENTED_EDGE ( 'NONE', *, *, #31710, .F. ) ;
#7927=CARTESIAN_POINT ( 'NONE',  ( 1.206523839548967247, -3.371562291789969468, 1.499999999999999556 ) ) ;
#7932=CARTESIAN_POINT ( 'NONE',  ( 2.770684449829438734, 0.02953710645921867745, 1.228046178477532946 ) ) ;
#7938=VERTEX_POINT ( 'NONE', #6699 ) ;
#7948=CARTESIAN_POINT ( 'NONE',  ( -3.889464452585704723, -3.181828567483031112, -1.499999999999999556 ) ) ;
#7950=ORIENTED_EDGE ( 'NONE', *, *, #3223, .F. ) ;
#7951=CARTESIAN_POINT ( 'NONE',  ( -0.1874251621923629929, -14.67762397772687777, 1.745313648524859262 ) ) ;
#7952=ORIENTED_EDGE ( 'NONE', *, *, #21181, .T. ) ;
#7955=VERTEX_POINT ( 'NONE', #32305 ) ;
#7962=CARTESIAN_POINT ( 'NONE',  ( 0.000000000000000000, 0.000000000000000000, -1.500000000000000000 ) ) ;
#7963=LINE ( 'NONE', #18007, #12937 ) ;
#7964=LINE ( 'NONE', #28360, #17123 ) ;
#7968=CARTESIAN_POINT ( 'NONE',  ( 24.80306213860341558, -17.49230408913766865, 1.499999999999999778 ) ) ;
#7969=CARTESIAN_POINT ( 'NONE',  ( 21.59559372540891786, -17.25941758357568645, -1.753144073646022649 ) ) ;
#7976=CARTESIAN_POINT ( 'NONE',  ( 2.948241552139481580, -0.000000000000000000, -1.325451157388740198 ) ) ;
#7977=CARTESIAN_POINT ( 'NONE',  ( 15.65524065576216017, -15.16498509049018040, 1.500000000000000000 ) ) ;
#7981=VECTOR ( 'NONE', #18111, 1000.000000000000000 ) ;
#7986=APPLICATION_CONTEXT ( 'configuration controlled 3d designs of mechanical parts and assemblies' ) ;
#7989=CARTESIAN_POINT ( 'NONE',  ( 44.05836296526000240, -19.40445080606629702, -1.500000000000000000 ) ) ;
#7996=CARTESIAN_POINT ( 'NONE',  ( 19.80502601021794362, -16.61823365775807559, -1.499999999999999556 ) ) ;
#8004=ORIENTED_EDGE ( 'NONE', *, *, #7101, .T. ) ;
#8006=AXIS2_PLACEMENT_3D ( 'NONE', #2950, #28796, #5894 ) ;
#8014=ORIENTED_EDGE ( 'NONE', *, *, #23019, .T. ) ;
#8028=ADVANCED_FACE ( 'NONE', ( #31723 ), #6620, .T. ) ;
#8040=CARTESIAN_POINT ( 'NONE',  ( -2.559292292825085191, -12.25264313511502223, 1.500000000000079492 ) ) ;
#8044=CARTESIAN_POINT ( 'NONE',  ( 107.6641765185853501, -20.45809951660527659, -1.499999999999999556 ) ) ;
#8050=CARTESIAN_POINT ( 'NONE',  ( -23.35000000000000142, -10.96966150227469505, 4.000000000000000000 ) ) ;
#8053=ORIENTED_EDGE ( 'NONE', *, *, #3013, .F. ) ;
#8061=CARTESIAN_POINT ( 'NONE',  ( 7.378890305931267157, -8.603354364037917534, 1.000000000000000000 ) ) ;
#8062=CARTESIAN_POINT ( 'NONE',  ( 108.0403038335384451, -18.64972729361248582, 4.956758977629584173 ) ) ;
#8080=CARTESIAN_POINT ( 'NONE',  ( 6.304370421170641947, -13.59668101824182429, -1.755882049235860221 ) ) ;
#8115=CARTESIAN_POINT ( 'NONE',  ( -4.148661379613653111, -6.185305878765366749, 1.745226859798899577 ) ) ;
#8119=( BOUNDED_SURFACE ( )  B_SPLINE_SURFACE ( 3, 2, ( 
 ( #5443, #18312, #28521 ),
 ( #5622, #25498, #15799 ),
 ( #2780, #26008, #26159 ),
 ( #10775, #3114, #20322 ),
 ( #31206, #3266, #2605 ),
 ( #30531, #12770, #22979 ),
 ( #21297, #21154, #28818 ),
 ( #24129, #6101, #18624 ),
 ( #6398, #1415, #5916 ),
 ( #19117, #14101, #13754 ) ),
 .UNSPECIFIED., .F., .F., .F. ) 
 B_SPLINE_SURFACE_WITH_KNOTS ( ( 4, 2, 2, 2, 4 ),
 ( 3, 3 ),
 ( 0.01791456443259262232, 0.01997296323899121900, 0.02100216264219051734, 0.02151676234379016478, 0.02203136204538981568 ),
 ( 0.000000000000000000, 1.000000000000000000 ),
 .UNSPECIFIED. ) 
 GEOMETRIC_REPRESENTATION_ITEM ( )  RATIONAL_B_SPLINE_SURFACE ( (
 ( 1.000000000000000000, 0.8490876263418722925, 1.000000000000000000),
 ( 1.000000000000000000, 0.8789005871660122704, 1.000000000000000000),
 ( 1.000000000000000000, 0.9052476245291617429, 1.000000000000000000),
 ( 1.000000000000000000, 0.9409176603639005654, 1.000000000000000000),
 ( 1.000000000000000000, 0.9521522767063923531, 1.000000000000000000),
 ( 1.000000000000000000, 0.9681060328970257922, 1.000000000000000000),
 ( 1.000000000000000000, 0.9732806895433457894, 1.000000000000000000),
 ( 1.000000000000000000, 0.9832765258107477591, 1.000000000000000000),
 ( 1.000000000000000000, 0.9881226520952709480, 1.000000000000000000),
 ( 1.000000000000000000, 0.9925898118721191432, 1.000000000000000000) ) ) 
 REPRESENTATION_ITEM ( '' )  SURFACE ( )  );
#8122=VERTEX_POINT ( 'NONE', #11131 ) ;
#8130=AXIS2_PLACEMENT_3D ( 'NONE', #18941, #28965, #5880 ) ;
#8133=CARTESIAN_POINT ( 'NONE',  ( -2.624406592062199728, -0.1993550914063198232, -1.626071056744967214 ) ) ;
#8139=CARTESIAN_POINT ( 'NONE',  ( 23.00820037127621731, -17.39482224626771156, -1.688990564600181488 ) ) ;
#8142=CIRCLE ( 'NONE', #5482, 8.500000000000000000 ) ;
#8143=CIRCLE ( 'NONE', #4405, 0.5000000000000004441 ) ;
#8151=CIRCLE ( 'NONE', #26827, 0.5000000000000004441 ) ;
#8154=CARTESIAN_POINT ( 'NONE',  ( 20.55552624091973968, -16.63177717300951741, 1.500000000000000000 ) ) ;
#8195=AXIS2_PLACEMENT_3D ( 'NONE', #25111, #8947, #9914 ) ;
#8211=CARTESIAN_POINT ( 'NONE',  ( 20.72684859436193250, -16.16085785620104076, -1.000000000000000222 ) ) ;
#8220=CARTESIAN_POINT ( 'NONE',  ( 107.5922305810999688, -19.42186344497500983, -3.623800042533074972 ) ) ;
#8223=LINE ( 'NONE', #5707, #6541 ) ;
#8225=CARTESIAN_POINT ( 'NONE',  ( -2.829357234188641712, -11.58112209631934419, 1.743702880379067066 ) ) ;
#8235=CARTESIAN_POINT ( 'NONE',  ( -31.12328840805762553, -25.43932300454937945, 1.499999999999999778 ) ) ;
#8240=CARTESIAN_POINT ( 'NONE',  ( -2.609487367014430070, -0.08210191867354442452, -1.553472644056464569 ) ) ;
#8241=CARTESIAN_POINT ( 'NONE',  ( 108.0270956946189926, -18.45953337857165266, 4.403826084184283118 ) ) ;
#8248=CARTESIAN_POINT ( 'NONE',  ( -3.135269660805078740, -0.5000000000000000000, -1.500000000000000000 ) ) ;
#8249=CARTESIAN_POINT ( 'NONE',  ( 1.278428506419904798, -2.392608122357158251, -1.500000000000000444 ) ) ;
#8251=CARTESIAN_POINT ( 'NONE',  ( 107.9807428589029286, -17.79206407539387769, 4.344990111930268739 ) ) ;
#8262=DIRECTION ( 'NONE',  ( 0.000000000000000000, 0.000000000000000000, -1.000000000000000000 ) ) ;
#8265=CARTESIAN_POINT ( 'NONE',  ( -3.405997759315474660, -10.41452980168814868, -1.743528089750926657 ) ) ;
#8266=CARTESIAN_POINT ( 'NONE',  ( 21.36776303755842932, -21.72386242187981864, -1.606475753954833108 ) ) ;
#8268=CARTESIAN_POINT ( 'NONE',  ( 107.9478736030354327, -17.31875496774473078, -4.501973445319090494 ) ) ;
#8269=CARTESIAN_POINT ( 'NONE',  ( 107.9266616237874246, -17.01330774345008123, 2.743473114337553920 ) ) ;
#8270=VECTOR ( 'NONE', #31672, 1000.000000000000000 ) ;
#8272=CARTESIAN_POINT ( 'NONE',  ( 5.532104225389706365, -12.77500742877625939, 1.499999999999998668 ) ) ;
#8281=VERTEX_POINT ( 'NONE', #9942 ) ;
#8294=B_SPLINE_CURVE_WITH_KNOTS ( 'NONE', 3,
 ( #15649, #2789, #30370, #12970, #5284, #8115, #23185, #17831, #15148, #294, #25509, #20678, #9960, #30880, #28032, #28532, #20517, #25357, #27845, #7951, #15305, #7440, #28182, #12633, #5454, #12780, #30730, #22991, #17639, #2617, #438, #28341 ),
 .UNSPECIFIED., .F., .F.,
 ( 4, 2, 2, 2, 2, 2, 2, 2, 2, 2, 2, 2, 2, 2, 2, 4 ),
 ( 0.000000000000000000, 0.004269922980577924194, 0.005337403725722405026, 0.006404884470866884991, 0.008539845961155846654, 0.009607326706300330088, 0.01067480745144481179, 0.01174228819658929696, 0.01280976894173377865, 0.01494473043202274032, 0.01601221117716722375, 0.01707969192231171066, 0.02134961490288964092, 0.02561953788346757466, 0.02988946086404550492, 0.03415938384462344213 ),
 .UNSPECIFIED. ) ;
#8302=DIRECTION ( 'NONE',  ( 0.000000000000000000, 0.000000000000000000, 1.000000000000000000 ) ) ;
#8305=CARTESIAN_POINT ( 'NONE',  ( 109.7220438555052056, -17.55815402607574782, -5.485967528433937979 ) ) ;
#8309=CARTESIAN_POINT ( 'NONE',  ( 24.40680557455002386, -17.41959047392573012, 1.432979604635828075 ) ) ;
#8318=CARTESIAN_POINT ( 'NONE',  ( 11.72844750001789649, -13.05523934058538238, 1.000000000000000000 ) ) ;
#8319=EDGE_LOOP ( 'NONE', ( #9803, #19476, #25380, #14970 ) ) ;
#8323=CARTESIAN_POINT ( 'NONE',  ( 0.9068484513889774057, -4.286977062749324219, 1.499999999999999334 ) ) ;
#8334=CARTESIAN_POINT ( 'NONE',  ( 0.4082220075202627196, -6.684754012654100741, 0.9788672205888330202 ) ) ;
#8343=CARTESIAN_POINT ( 'NONE',  ( 107.6300027435836313, -19.96576125925905032, -2.508990583258498663 ) ) ;
#8366=CARTESIAN_POINT ( 'NONE',  ( 21.08401840680159367, -16.78474387324287775, 1.500000000000000000 ) ) ;
#8367=CARTESIAN_POINT ( 'NONE',  ( 0.9354051327728147847, -3.271575928939224553, -1.500000000000276890 ) ) ;
#8373=CARTESIAN_POINT ( 'NONE',  ( 14.56323991668084794, -20.55228079977623068, 1.750894133678834841 ) ) ;
#8375=CARTESIAN_POINT ( 'NONE',  ( 2.998015176062106324, -0.2419477797672030250, 1.432989973798650452 ) ) ;
#8386=CARTESIAN_POINT ( 'NONE',  ( -3.162653373153519798, 0.0004983460144661164444, -1.055926639513774745 ) ) ;
#8387=CARTESIAN_POINT ( 'NONE',  ( 24.39659513448239991, -17.41072360183627055, 1.416990234759656575 ) ) ;
#8392=CARTESIAN_POINT ( 'NONE',  ( -3.222375984151267581, 0.000000000000000000, -1.000000000000000000 ) ) ;
#8395=CARTESIAN_POINT ( 'NONE',  ( 108.0493838057754914, -18.78047663426704617, 4.827283856852130128 ) ) ;
#8410=CARTESIAN_POINT ( 'NONE',  ( 14.60944221173904722, -20.56080756410654331, -1.750898334667394973 ) ) ;
#8411=CARTESIAN_POINT ( 'NONE',  ( 108.0291781248180598, -18.48951985539477505, -4.325670280508457921 ) ) ;
#8416=B_SPLINE_CURVE_WITH_KNOTS ( 'NONE', 3,
 ( #22920, #12880, #20756, #10212, #18423, #7880, #15887, #23574, #30653, #220 ),
 .UNSPECIFIED., .F., .F.,
 ( 4, 3, 3, 4 ),
 ( 2.385244779468109755E-18, 0.001000000000068484085, 0.002000000000134635400, 0.003364209820971502535 ),
 .UNSPECIFIED. ) ;
#8418=CARTESIAN_POINT ( 'NONE',  ( 0.6070402175060268801, -7.493581194466792716, 1.500000000000000444 ) ) ;
#8420=CARTESIAN_POINT ( 'NONE',  ( 42.88108885380913193, -22.62752020922543750, 4.522129901861158707 ) ) ;
#8421=CARTESIAN_POINT ( 'NONE',  ( 2.458207506242486851, -0.2539630985812899033, 1.478790212540433746 ) ) ;
#8432=EDGE_CURVE ( 'NONE', #8281, #635, #8142, .T. ) ;
#8435=FACE_OUTER_BOUND ( 'NONE', #28885, .T. ) ;
#8438=ORIENTED_EDGE ( 'NONE', *, *, #16302, .F. ) ;
#8439=CARTESIAN_POINT ( 'NONE',  ( -15.12340757463330654, -27.93932300454937590, -1.000000000000000000 ) ) ;
#8440=EDGE_LOOP ( 'NONE', ( #30495, #32182, #7228, #24539, #7952, #23709, #16862, #15094 ) ) ;
#8450=CARTESIAN_POINT ( 'NONE',  ( 108.0279038916327323, -18.47117121451548272, 4.374159544809090860 ) ) ;
#8453=FACE_OUTER_BOUND ( 'NONE', #30731, .T. ) ;
#8457=CARTESIAN_POINT ( 'NONE',  ( 22.80257594975842395, -21.89069150541910957, 1.310091732169401668 ) ) ;
#8458=DIRECTION ( 'NONE',  ( -0.000000000000000000, -0.000000000000000000, -1.000000000000000000 ) ) ;
#8459=CARTESIAN_POINT ( 'NONE',  ( 107.6641398346956890, -20.45810202417174750, -1.499999999999999556 ) ) ;
#8465=CARTESIAN_POINT ( 'NONE',  ( 7.931701156347861215, -9.929036423920559074, 1.500000000000000000 ) ) ;
#8468=B_SPLINE_CURVE_WITH_KNOTS ( 'NONE', 3,
 ( #12027, #12520, #12338, #10154 ),
 .UNSPECIFIED., .F., .F.,
 ( 4, 4 ),
 ( 0.000000000000000000, 2.202192133514975633E-08 ),
 .UNSPECIFIED. ) ;
#8470=CARTESIAN_POINT ( 'NONE',  ( 2.053765210313523770, -0.9196025812828518831, 1.500000000001123768 ) ) ;
#8476=ORIENTED_EDGE ( 'NONE', *, *, #32671, .F. ) ;
#8480=CARTESIAN_POINT ( 'NONE',  ( 2.889143798718252221, 0.000000000000000000, 0.9788672205888330202 ) ) ;
#8485=ORIENTED_EDGE ( 'NONE', *, *, #10856, .F. ) ;
#8486=ORIENTED_EDGE ( 'NONE', *, *, #7854, .F. ) ;
#8490=CARTESIAN_POINT ( 'NONE',  ( 109.5084093630373872, -17.21855534384547326, 4.522129901861156931 ) ) ;
#8495=( BOUNDED_SURFACE ( )  B_SPLINE_SURFACE ( 3, 2, ( 
 ( #29618, #26937, #26598 ),
 ( #31952, #19077, #13713 ),
 ( #11393, #8870, #22092 ),
 ( #24405, #1523, #6528 ),
 ( #24070, #11699, #16734 ),
 ( #24563, #3699, #1195 ),
 ( #26754, #32306, #19575 ),
 ( #31624, #3870, #6351 ),
 ( #14048, #21591, #18928 ),
 ( #31799, #29265, #29771 ),
 ( #6850, #8714, #29118 ),
 ( #6203, #16387, #20087 ),
 ( #7353, #27741, #14862 ),
 ( #27591, #30280, #2179 ),
 ( #27246, #30433, #24912 ),
 ( #32800, #7513, #4363 ),
 ( #24755, #22585, #25418 ),
 ( #4540, #25062, #4848 ),
 ( #2526, #9872, #12694 ),
 ( #17544, #15030, #9693 ),
 ( #25249, #2371, #10024 ),
 ( #12544, #22748, #22898 ),
 ( #7703, #14541, #14713 ),
 ( #7204, #1875, #10183 ),
 ( #2025, #12051, #5596 ),
 ( #32954, #27924, #12197 ),
 ( #22247, #20234, #12366 ),
 ( #20406, #30620, #22397 ),
 ( #32456, #17715, #27436 ),
 ( #5037, #9515, #4692 ),
 ( #15216, #19731, #29933 ),
 ( #32614, #7020, #17230 ),
 ( #19918, #30129, #17397 ),
 ( #11020, #20887, #2874 ) ),
 .UNSPECIFIED., .F., .F., .F. ) 
 B_SPLINE_SURFACE_WITH_KNOTS ( ( 4, 2, 2, 2, 2, 2, 2, 2, 2, 2, 2, 2, 2, 2, 2, 2, 4 ),
 ( 3, 3 ),
 ( 0.000000000000000000, 0.004360795930118540123, 0.005450994912648174720, 0.006541193895177810184, 0.008721591860237080246, 0.009811790842766714843, 0.01090198982529634944, 0.01199218880782598404, 0.01308238779035562037, 0.01526278575541489130, 0.01635298473794452589, 0.01744318372047416049, 0.02180397965059269888, 0.02398437761565196807, 0.02616477558071124074, 0.03052557151082978260, 0.03488636744094832098 ),
 ( 0.000000000000000000, 1.000000000000000000 ),
 .UNSPECIFIED. ) 
 GEOMETRIC_REPRESENTATION_ITEM ( )  RATIONAL_B_SPLINE_SURFACE ( (
 ( 1.000000000000000000, 0.8508761217583473702, 1.000000000000000000),
 ( 1.000000000000000000, 0.8513495135180835227, 1.000000000000000000),
 ( 1.000000000000000000, 0.8517270363692717172, 1.000000000000000000),
 ( 1.000000000000000000, 0.8525422031685686575, 1.000000000000000000),
 ( 1.000000000000000000, 0.8526809929701213431, 1.000000000000000000),
 ( 1.000000000000000000, 0.8529405693517642106, 1.000000000000000000),
 ( 1.000000000000000000, 0.8530607691951643812, 1.000000000000000000),
 ( 1.000000000000000000, 0.8534148638638719975, 1.000000000000000000),
 ( 1.000000000000000000, 0.8536546893696659311, 1.000000000000000000),
 ( 1.000000000000000000, 0.8539620067557214256, 1.000000000000000000),
 ( 1.000000000000000000, 0.8540316192635319936, 1.000000000000000000),
 ( 1.000000000000000000, 0.8540602109241151041, 1.000000000000000000),
 ( 1.000000000000000000, 0.8540396564185858130, 1.000000000000000000),
 ( 1.000000000000000000, 0.8539811336537593833, 1.000000000000000000),
 ( 1.000000000000000000, 0.8539432050989358425, 1.000000000000000000),
 ( 1.000000000000000000, 0.8538670370114783692, 1.000000000000000000),
 ( 1.000000000000000000, 0.8538286120051845618, 1.000000000000000000),
 ( 1.000000000000000000, 0.8536849753243391792, 1.000000000000000000),
 ( 1.000000000000000000, 0.8533602685196585158, 1.000000000000000000),
 ( 1.000000000000000000, 0.8529654596012481438, 1.000000000000000000),
 ( 1.000000000000000000, 0.8528244218823842759, 1.000000000000000000),
 ( 1.000000000000000000, 0.8525299725566436448, 1.000000000000000000),
 ( 1.000000000000000000, 0.8523761395252034134, 1.000000000000000000),
 ( 1.000000000000000000, 0.8516129481394613121, 1.000000000000000000),
 ( 1.000000000000000000, 0.8513036087791725492, 1.000000000000000000),
 ( 1.000000000000000000, 0.8508287454031215891, 1.000000000000000000),
 ( 1.000000000000000000, 0.8506601076795354821, 1.000000000000000000),
 ( 1.000000000000000000, 0.8503078255506797412, 1.000000000000000000),
 ( 1.000000000000000000, 0.8501262613430246029, 1.000000000000000000),
 ( 1.000000000000000000, 0.8496349353270501448, 1.000000000000000000),
 ( 1.000000000000000000, 0.8494863696526087082, 1.000000000000000000),
 ( 1.000000000000000000, 0.8492518783361784340, 1.000000000000000000),
 ( 1.000000000000000000, 0.8491664931671285554, 1.000000000000000000),
 ( 1.000000000000000000, 0.8490876263417841407, 1.000000000000000000) ) ) 
 REPRESENTATION_ITEM ( '' )  SURFACE ( )  );
#8496=CARTESIAN_POINT ( 'NONE',  ( -30.49402871571406948, -10.96966150227469505, -11.00000000000000000 ) ) ;
#8498=CARTESIAN_POINT ( 'NONE',  ( 107.9802527803231129, -17.78500706576168611, -4.325704939595124365 ) ) ;
#8500=ORIENTED_EDGE ( 'NONE', *, *, #7101, .F. ) ;
#8502=VERTEX_POINT ( 'NONE', #26631 ) ;
#8506=AXIS2_PLACEMENT_3D ( 'NONE', #14949, #22681, #16972 ) ;
#8507=EDGE_CURVE ( 'NONE', #20422, #10078, #1467, .T. ) ;
#8511=ORIENTED_EDGE ( 'NONE', *, *, #17976, .F. ) ;
#8512=ORIENTED_EDGE ( 'NONE', *, *, #31237, .T. ) ;
#8522=CYLINDRICAL_SURFACE ( 'NONE', #30015, 0.5000000000000004441 ) ;
#8540=CARTESIAN_POINT ( 'NONE',  ( 20.03174988220922614, -21.67712946496415682, 1.441661034764442073 ) ) ;
#8541=CARTESIAN_POINT ( 'NONE',  ( -3.029003146408718372, -0.04861012228918290545, -1.223725428626261991 ) ) ;
#8545=ORIENTED_EDGE ( 'NONE', *, *, #28340, .F. ) ;
#8547=EDGE_LOOP ( 'NONE', ( #31215, #8896, #6706, #32559, #25499, #4967, #1072 ) ) ;
#8554=ADVANCED_FACE ( 'NONE', ( #17084, #4080 ), #4225, .T. ) ;
#8561=CARTESIAN_POINT ( 'NONE',  ( -4.102049215352101541, -5.462733247114307744, -1.745628864018728743 ) ) ;
#8564=CARTESIAN_POINT ( 'NONE',  ( 10.37705096095362123, -12.86926679082229263, -1.500000000000000000 ) ) ;
#8572=CARTESIAN_POINT ( 'NONE',  ( 73.45519860863089434, -21.36028973287599086, 4.522129901861158707 ) ) ;
#8585=CARTESIAN_POINT ( 'NONE',  ( 21.36097421961354925, -21.76718868951427055, 1.410897148389129052 ) ) ;
#8587=CARTESIAN_POINT ( 'NONE',  ( 0.9077343987014625526, -4.284037799451631656, -1.499999999999999334 ) ) ;
#8589=AXIS2_PLACEMENT_3D ( 'NONE', #24767, #2035, #22411 ) ;
#8591=CARTESIAN_POINT ( 'NONE',  ( 24.79284380060802206, -17.49144841392629246, -1.371632250993898294 ) ) ;
#8597=ORIENTED_EDGE ( 'NONE', *, *, #387, .T. ) ;
#8607=CARTESIAN_POINT ( 'NONE',  ( 108.0280430118043142, -18.47317451037714164, 4.369308448245075915 ) ) ;
#8611=CARTESIAN_POINT ( 'NONE',  ( -2.614103913510795962, -0.09422588260484983380, -1.555412231120104849 ) ) ;
#8627=CARTESIAN_POINT ( 'NONE',  ( 23.22564588060096469, -22.38932300456763969, 1.000000000000000000 ) ) ;
#8628=CARTESIAN_POINT ( 'NONE',  ( 9.134478070117602044, -0.4075412269879192806, 1.500000000000000000 ) ) ;
#8631=EDGE_CURVE ( 'NONE', #2628, #28480, #31115, .T. ) ;
#8632=VECTOR ( 'NONE', #16145, 1000.000000000000000 ) ;
#8636=CARTESIAN_POINT ( 'NONE',  ( 0.2669397441535706350, -7.206081505926538178, 1.499999999999929390 ) ) ;
#8656=VECTOR ( 'NONE', #8458, 1000.000000000000000 ) ;
#8663=CARTESIAN_POINT ( 'NONE',  ( -32.06740601709051930, 0.000000000000000000, -0.9045955023117262517 ) ) ;
#8673=CARTESIAN_POINT ( 'NONE',  ( 2.998015176062106768, -0.2419477797672031638, -1.432989973798650229 ) ) ;
#8685=CARTESIAN_POINT ( 'NONE',  ( 7.642108059735714498, -9.326698953827136762, -1.000000000000000000 ) ) ;
#8693=CARTESIAN_POINT ( 'NONE',  ( 6.840024017557634117, -8.509480309817995192, 1.499999999999999778 ) ) ;
#8695=CARTESIAN_POINT ( 'NONE',  ( 0.5438053540825241727, -6.200476582808712500, -1.499999999999999556 ) ) ;
#8707=VECTOR ( 'NONE', #21073, 1000.000000000000000 ) ;
#8714=CARTESIAN_POINT ( 'NONE',  ( -3.806083282599349804, -9.689094992912284710, -1.500000000000080158 ) ) ;
#8718=CARTESIAN_POINT ( 'NONE',  ( -50.60000000000000142, -10.96966150227468972, 1.000000000000000000 ) ) ;
#8723=EDGE_CURVE ( 'NONE', #15410, #11567, #6531, .T. ) ;
#8726=CARTESIAN_POINT ( 'NONE',  ( 23.26681913458019224, -17.19558280316135779, 1.454198315410549336 ) ) ;
#8727=EDGE_LOOP ( 'NONE', ( #15346, #2549, #2911, #30119, #25131 ) ) ;
#8746=CARTESIAN_POINT ( 'NONE',  ( 108.0371116761128576, -18.60376102042065938, -4.091500227421209779 ) ) ;
#8748=CARTESIAN_POINT ( 'NONE',  ( 7.362531900907011817, -8.542914936921272684, -1.000000000000000000 ) ) ;
#8754=CARTESIAN_POINT ( 'NONE',  ( -2.786590204610738475, -5.640011313470055576, 4.522129901861158707 ) ) ;
#8757=VERTEX_POINT ( 'NONE', #2726 ) ;
#8761=DIRECTION ( 'NONE',  ( -1.000000000000000000, 0.000000000000000000, 0.000000000000000000 ) ) ;
#8762=ORIENTED_EDGE ( 'NONE', *, *, #23507, .T. ) ;
#8773=CARTESIAN_POINT ( 'NONE',  ( -0.2168228499960635214, -15.24168959957554215, -0.9788672205760856615 ) ) ;
#8778=VERTEX_POINT ( 'NONE', #20458 ) ;
#8779=CARTESIAN_POINT ( 'NONE',  ( -2.819379691724115400, -6.927609664242504017, 4.522129901861158707 ) ) ;
#8780=LINE ( 'NONE', #29171, #3795 ) ;
#8788=CARTESIAN_POINT ( 'NONE',  ( 107.5619444582182354, -18.98608621969496113, 4.515334266560267373 ) ) ;
#8791=DIRECTION ( 'NONE',  ( 1.000000000000000000, 0.000000000000000000, 0.000000000000000000 ) ) ;
#8798=EDGE_CURVE ( 'NONE', #15271, #14502, #23428, .T. ) ;
#8806=CARTESIAN_POINT ( 'NONE',  ( 8.305304940806680136, -2.146676032412352164, 1.000000000000000000 ) ) ;
#8810=CARTESIAN_POINT ( 'NONE',  ( 0.8635714481620181404, -8.446712017869664635, 1.500000000000000000 ) ) ;
#8817=CARTESIAN_POINT ( 'NONE',  ( 23.30536738591935730, -17.34558290870676700, -1.520589546895734001 ) ) ;
#8818=CARTESIAN_POINT ( 'NONE',  ( 107.8806307222008627, -16.35047421165092985, 3.636029349014985090 ) ) ;
#8820=CARTESIAN_POINT ( 'NONE',  ( -2.986084103915760846, 1.331507122045496354E-29, 1.110774563390631409 ) ) ;
#8832=CARTESIAN_POINT ( 'NONE',  ( -0.5220033361344453837, 0.000000000000000000, 5.485967528433935314 ) ) ;
#8833=EDGE_CURVE ( 'NONE', #3232, #9843, #13086, .T. ) ;
#8834=CARTESIAN_POINT ( 'NONE',  ( 25.29725835852283922, -17.51800646107394854, 1.124426024579843642 ) ) ;
#8836=CARTESIAN_POINT ( 'NONE',  ( 25.52557118915447631, -17.56218954043520597, -1.078818547980193943 ) ) ;
#8839=CARTESIAN_POINT ( 'NONE',  ( 107.5817932186935622, -17.35116855567646965, -4.522076874643048860 ) ) ;
#8851=DIRECTION ( 'NONE',  ( 1.000000000000000000, 0.000000000000000000, 0.000000000000000000 ) ) ;
#8854=CARTESIAN_POINT ( 'NONE',  ( 0.5134311721232786008, -4.169659756541258311, -1.765416748134584157 ) ) ;
#8859=CARTESIAN_POINT ( 'NONE',  ( 10.35374396645284989, -19.59145211855898339, 1.750308502512231579 ) ) ;
#8870=CARTESIAN_POINT ( 'NONE',  ( -3.910130424047638442, -3.305169137730107121, -1.500000000000157652 ) ) ;
#8874=ORIENTED_EDGE ( 'NONE', *, *, #18015, .F. ) ;
#8878=CARTESIAN_POINT ( 'NONE',  ( 107.4492989043458664, -17.34924253231580593, 4.492206751594263636 ) ) ;
#8889=CARTESIAN_POINT ( 'NONE',  ( 11.59716086141860458, -20.31972538710700960, -1.499999999999999334 ) ) ;
#8893=CARTESIAN_POINT ( 'NONE',  ( 108.1227634682907848, -19.83712552029795617, -1.563595750885480085 ) ) ;
#8894=CARTESIAN_POINT ( 'NONE',  ( 10.11068946041623740, -12.10067465432455869, -1.499999999999573896 ) ) ;
#8895=CARTESIAN_POINT ( 'NONE',  ( 107.8874544901744912, -16.44873477293144859, -1.585822557233536934 ) ) ;
#8896=ORIENTED_EDGE ( 'NONE', *, *, #23066, .T. ) ;
#8901=CARTESIAN_POINT ( 'NONE',  ( -2.600000000000000089, 0.000000000000000000, 1.500000000000000000 ) ) ;
#8905=CARTESIAN_POINT ( 'NONE',  ( 107.4085326904115334, -16.76255377593236418, -3.296787005979242124 ) ) ;
#8908=( BOUNDED_SURFACE ( )  B_SPLINE_SURFACE ( 3, 2, ( 
 ( #21499, #31524, #11462 ),
 ( #31709, #3470, #21809 ),
 ( #21319, #13627, #16451 ),
 ( #13936, #18992, #6122 ),
 ( #24158, #1281, #8788 ),
 ( #29180, #21657, #31864 ),
 ( #11613, #23977, #23830 ),
 ( #8933, #3616, #19139 ),
 ( #6421, #29329, #31372 ),
 ( #8607, #1095, #942 ),
 ( #8450, #16619, #26834 ),
 ( #16137, #11120, #18644 ),
 ( #28841, #5938, #26362 ),
 ( #12472, #15910, #395 ),
 ( #17631, #8395, #10731 ),
 ( #5587, #8062, #14950 ),
 ( #18591, #13386, #23436 ),
 ( #31465, #25164, #20166 ),
 ( #26121, #13093, #5732 ),
 ( #3226, #23606, #890 ),
 ( #17474, #23292, #5875 ),
 ( #18266, #15767, #27673 ),
 ( #21266, #28288, #28479 ),
 ( #10572, #2285, #726 ),
 ( #10914, #25972, #28780 ),
 ( #22683, #4775, #30364 ),
 ( #26295, #3080, #3405 ),
 ( #21121, #31319, #32886 ),
 ( #7433, #30982, #20945 ),
 ( #13236, #16062, #20779 ),
 ( #9953, #542, #13568 ),
 ( #15593, #25807, #31163 ),
 ( #8251, #18444, #23775 ),
 ( #11066, #5400, #2931 ),
 ( #28636, #14061, #19436 ),
 ( #32132, #13724, #18750 ),
 ( #9208, #18937, #28960 ),
 ( #3710, #26608, #8878 ) ),
 .UNSPECIFIED., .F., .F., .F. ) 
 B_SPLINE_SURFACE_WITH_KNOTS ( ( 4, 2, 2, 2, 2, 2, 2, 2, 2, 2, 2, 2, 2, 2, 2, 2, 2, 2, 4 ),
 ( 3, 3 ),
 ( 0.007231348716683458529, 0.007247137925435321107, 0.007262927134187182818, 0.007270821738563113673, 0.007278716342939045396, 0.007294505551690907974, 0.007357662386698358287, 0.007483976056713257177, 0.007610289726728156068, 0.007736603396743054958, 0.007862917066757953849, 0.007989230736772852740, 0.008115544406787751630, 0.008178701241795201943, 0.008194490450547063654, 0.008210279659298925364, 0.008218174263674856220, 0.008226068868050787075, 0.008241858076802650521 ),
 ( 0.000000000000000000, 1.000000000000000000 ),
 .UNSPECIFIED. ) 
 GEOMETRIC_REPRESENTATION_ITEM ( )  RATIONAL_B_SPLINE_SURFACE ( (
 ( 1.000000000000000000, 0.7067447072241932471, 1.000000000000000000),
 ( 1.000000000000000000, 0.7067447061585132584, 1.000000000000000000),
 ( 1.000000000000000000, 0.7067447050979218659, 1.000000000000000000),
 ( 1.000000000000000000, 0.7067447029864426522, 1.000000000000000000),
 ( 1.000000000000000000, 0.7067442384298668889, 1.000000000000000000),
 ( 1.000000000000000000, 0.7067449321202956547, 1.000000000000000000),
 ( 1.000000000000000000, 0.7067458649492553979, 1.000000000000000000),
 ( 1.000000000000000000, 0.7067471220154400990, 1.000000000000000000),
 ( 1.000000000000000000, 0.7067477637805932300, 1.000000000000000000),
 ( 1.000000000000000000, 0.7067497297540578094, 1.000000000000000000),
 ( 1.000000000000000000, 0.7067510945828608948, 1.000000000000000000),
 ( 1.000000000000000000, 0.7067582039293559548, 1.000000000000000000),
 ( 1.000000000000000000, 0.7067647927017992604, 1.000000000000000000),
 ( 1.000000000000000000, 0.7067880497366301196, 1.000000000000000000),
 ( 1.000000000000000000, 0.7068082938633269974, 1.000000000000000000),
 ( 1.000000000000000000, 0.7068628506264388323, 1.000000000000000000),
 ( 1.000000000000000000, 0.7068980583899157066, 1.000000000000000000),
 ( 1.000000000000000000, 0.7069883395600154996, 1.000000000000000000),
 ( 1.000000000000000000, 0.7070467650740049903, 1.000000000000000000),
 ( 1.000000000000000000, 0.7071655611593249402, 1.000000000000000000),
 ( 1.000000000000000000, 0.7072232875170134658, 1.000000000000000000),
 ( 1.000000000000000000, 0.7073145313144446611, 1.000000000000000000),
 ( 1.000000000000000000, 0.7073497553658054660, 1.000000000000000000),
 ( 1.000000000000000000, 0.7074042560665476653, 1.000000000000000000),
 ( 1.000000000000000000, 0.7074245345453707978, 1.000000000000000000),
 ( 1.000000000000000000, 0.7074478136499360303, 1.000000000000000000),
 ( 1.000000000000000000, 0.7074544300748824011, 1.000000000000000000),
 ( 1.000000000000000000, 0.7074615795605810886, 1.000000000000000000),
 ( 1.000000000000000000, 0.7074629527376177229, 1.000000000000000000),
 ( 1.000000000000000000, 0.7074655910163150097, 1.000000000000000000),
 ( 1.000000000000000000, 0.7074674355297142503, 1.000000000000000000),
 ( 1.000000000000000000, 0.7074683863501984860, 1.000000000000000000),
 ( 1.000000000000000000, 0.7074680773870454242, 1.000000000000000000),
 ( 1.000000000000000000, 0.7074680753537760936, 1.000000000000000000),
 ( 1.000000000000000000, 0.7074680743359408330, 1.000000000000000000),
 ( 1.000000000000000000, 0.7074680712787539960, 1.000000000000000000),
 ( 1.000000000000000000, 0.7074680692358628065, 1.000000000000000000),
 ( 1.000000000000000000, 0.7074680671880581029, 1.000000000000000000) ) ) 
 REPRESENTATION_ITEM ( '' )  SURFACE ( )  );
#8910=DIRECTION ( 'NONE',  ( 0.000000000000000000, 0.000000000000000000, 1.000000000000000000 ) ) ;
#8912=CARTESIAN_POINT ( 'NONE',  ( -3.135269660805079628, -0.5000000000000024425, -1.949999999999999956 ) ) ;
#8914=EDGE_LOOP ( 'NONE', ( #3152, #5243, #25005 ) ) ;
#8916=EDGE_CURVE ( 'NONE', #28886, #9323, #2848, .T. ) ;
#8921=CARTESIAN_POINT ( 'NONE',  ( -46.10000000000000142, -10.96966150227468972, 6.999999999999999112 ) ) ;
#8933=CARTESIAN_POINT ( 'NONE',  ( 108.0283109730694520, -18.47703308593441562, 4.359537947287052795 ) ) ;
#8934=CARTESIAN_POINT ( 'NONE',  ( -0.2493515011840002071, -1.403010508276435031, -5.485967528433937979 ) ) ;
#8943=ORIENTED_EDGE ( 'NONE', *, *, #9566, .F. ) ;
#8944=ADVANCED_FACE ( 'NONE', ( #13378 ), #11886, .T. ) ;
#8946=CARTESIAN_POINT ( 'NONE',  ( 22.85793694858476144, -21.91835806764118999, -1.144022321087336813 ) ) ;
#8947=DIRECTION ( 'NONE',  ( -0.000000000000000000, -0.000000000000000000, -1.000000000000000000 ) ) ;
#8949=ORIENTED_EDGE ( 'NONE', *, *, #328, .F. ) ;
#8952=CARTESIAN_POINT ( 'NONE',  ( 2.123522008129191008, -10.79631020383399864, 1.499999999999645173 ) ) ;
#8958=CARTESIAN_POINT ( 'NONE',  ( 23.72064572292702778, -17.26593119145025668, -1.418862781619861346 ) ) ;
#8964=CARTESIAN_POINT ( 'NONE',  ( 22.70718278262463841, -21.88016059487463849, -1.342589741762356237 ) ) ;
#8977=CARTESIAN_POINT ( 'NONE',  ( -1.528445841742499756, -6.248157669862440144, 5.485967528433933538 ) ) ;
#8978=VERTEX_POINT ( 'NONE', #23768 ) ;
#8984=CARTESIAN_POINT ( 'NONE',  ( 107.4500593345376558, -17.36019228850485163, -4.522129901861164925 ) ) ;
#8990=EDGE_LOOP ( 'NONE', ( #31214, #11045, #808, #18335, #5312, #163, #30458, #19822, #16947, #31364 ) ) ;
#9004=VERTEX_POINT ( 'NONE', #28630 ) ;
#9007=CARTESIAN_POINT ( 'NONE',  ( 7.541562596972942956, -18.86384717194523475, 1.499999999999760192 ) ) ;
#9012=DIRECTION ( 'NONE',  ( 1.000000000000000000, 0.000000000000000000, 0.000000000000000000 ) ) ;
#9016=CARTESIAN_POINT ( 'NONE',  ( -17.85000000000000142, -10.96966150227469505, 4.000000000000000000 ) ) ;
#9033=DIRECTION ( 'NONE',  ( 0.9816271834476637537, 0.000000000000000000, 0.1908089953765453872 ) ) ;
#9037=ORIENTED_EDGE ( 'NONE', *, *, #10444, .F. ) ;
#9040=CARTESIAN_POINT ( 'NONE',  ( -4.456262821554182629, -5.024290100364269485, -1.500000000000000000 ) ) ;
#9045=CARTESIAN_POINT ( 'NONE',  ( 8.690654615650263537, -10.89241706942853583, -1.000000000000000000 ) ) ;
#9046=CARTESIAN_POINT ( 'NONE',  ( 108.0529299568327986, -18.83154032767301445, -4.758045365066062793 ) ) ;
#9053=CARTESIAN_POINT ( 'NONE',  ( 24.51663722516862620, -17.45316359950712837, -1.478737313599387093 ) ) ;
#9056=VERTEX_POINT ( 'NONE', #21112 ) ;
#9065=CARTESIAN_POINT ( 'NONE',  ( 6.706201599914444422, -13.33059280214037123, -1.500000000000000444 ) ) ;
#9069=CIRCLE ( 'NONE', #2716, 0.5000000000000007772 ) ;
#9072=CARTESIAN_POINT ( 'NONE',  ( -48.50000000000000000, -10.96966150227468972, 0.9999999999999991118 ) ) ;
#9079=VECTOR ( 'NONE', #33050, 1000.000000000000000 ) ;
#9081=DIRECTION ( 'NONE',  ( 1.000000000000000000, 0.000000000000000000, 0.000000000000000000 ) ) ;
#9083=CARTESIAN_POINT ( 'NONE',  ( 108.0291781248180598, -18.48951985539477505, -4.325670280508457921 ) ) ;
#9087=CARTESIAN_POINT ( 'NONE',  ( -0.4046470899337971106, -12.07320251013791790, -5.485967528433938867 ) ) ;
#9089=CARTESIAN_POINT ( 'NONE',  ( -29.35000000000000497, -10.96966150227469505, -11.50000000000000000 ) ) ;
#9104=CARTESIAN_POINT ( 'NONE',  ( 23.15209817170719120, -21.93517036684206900, -1.064739674281773185 ) ) ;
#9107=CARTESIAN_POINT ( 'NONE',  ( 8.571721676197185502, -11.50721971753343809, -1.500000000000000000 ) ) ;
#9109=CARTESIAN_POINT ( 'NONE',  ( 4.138787901720749396, -11.97482149199507084, 1.500000000000000000 ) ) ;
#9116=CARTESIAN_POINT ( 'NONE',  ( -4.456246017397374359, -5.024161734168909099, 1.500000000000000666 ) ) ;
#9136=DIRECTION ( 'NONE',  ( -0.000000000000000000, 1.000000000000000000, -0.000000000000000000 ) ) ;
#9169=CIRCLE ( 'NONE', #3342, 2.524999999999999467 ) ;
#9173=CARTESIAN_POINT ( 'NONE',  ( 0.4717033495752643857, -8.231128558055790023, -1.500000000000035305 ) ) ;
#9176=ORIENTED_EDGE ( 'NONE', *, *, #11575, .T. ) ;
#9184=CARTESIAN_POINT ( 'NONE',  ( 2.838908144950905932, -0.000000000000000000, 1.380700491544036623 ) ) ;
#9186=VECTOR ( 'NONE', #776, 999.9999999999998863 ) ;
#9192=CIRCLE ( 'NONE', #15068, 7.144028715714068056 ) ;
#9196=EDGE_CURVE ( 'NONE', #28480, #15957, #24168, .T. ) ;
#9208=CARTESIAN_POINT ( 'NONE',  ( 107.9802352237659022, -17.78475425570491453, 4.325014068553558744 ) ) ;
#9211=CARTESIAN_POINT ( 'NONE',  ( 20.49917871223711785, -21.72428526870503163, 1.411325660096738766 ) ) ;
#9213=CARTESIAN_POINT ( 'NONE',  ( 108.0048053234951198, -18.13855757953442449, 3.636029349014985090 ) ) ;
#9215=ORIENTED_EDGE ( 'NONE', *, *, #24107, .F. ) ;
#9216=ORIENTED_EDGE ( 'NONE', *, *, #4664, .F. ) ;
#9220=CARTESIAN_POINT ( 'NONE',  ( 5.994454021012749934, -18.63465724242956156, -1.500000000000001332 ) ) ;
#9225=CIRCLE ( 'NONE', #21015, 8.500000000000000000 ) ;
#9226=DIRECTION ( 'NONE',  ( 1.000000000000000000, 0.000000000000000000, 0.000000000000000000 ) ) ;
#9227=CARTESIAN_POINT ( 'NONE',  ( 7.192400643299275309, -7.644771086295416573, -1.000000000000000000 ) ) ;
#9228=CARTESIAN_POINT ( 'NONE',  ( 107.5579200398152295, -18.92771086533201341, -4.650503970115479113 ) ) ;
#9250=DIRECTION ( 'NONE',  ( 1.000000000000000000, -2.473959037481237219E-13, 0.000000000000000000 ) ) ;
#9253=CARTESIAN_POINT ( 'NONE',  ( 7.227634085595994407, -5.813588965143285492, 1.000000000000000222 ) ) ;
#9255=AXIS2_PLACEMENT_3D ( 'NONE', #21951, #9250, #29665 ) ;
#9257=CARTESIAN_POINT ( 'NONE',  ( -2.619378609982116135, -0.1905507107691023216, 1.628225384166350764 ) ) ;
#9263=EDGE_LOOP ( 'NONE', ( #14187, #13730, #27872 ) ) ;
#9289=CARTESIAN_POINT ( 'NONE',  ( -17.45597128428592981, 0.000000000000000000, 11.00000000000000000 ) ) ;
#9290=CARTESIAN_POINT ( 'NONE',  ( 7.278212735265134015, -5.482579124931374004, 1.000000000000000000 ) ) ;
#9293=CARTESIAN_POINT ( 'NONE',  ( 11.20269353100511367, -13.34333142745220613, -1.500000000000000000 ) ) ;
#9296=CARTESIAN_POINT ( 'NONE',  ( 0.2074580698797141576, -5.485259797753295530, 1.769984832060537139 ) ) ;
#9300=CARTESIAN_POINT ( 'NONE',  ( -4.436766851201613626, -8.315976708237174719, 1.500000000000000222 ) ) ;
#9301=CARTESIAN_POINT ( 'NONE',  ( -31.57659242536668032, -21.43932300455408679, -1.500000000000000000 ) ) ;
#9303=CARTESIAN_POINT ( 'NONE',  ( 23.32053031413095567, -17.41627278853254168, -1.661539697404067484 ) ) ;
#9304=CARTESIAN_POINT ( 'NONE',  ( 107.8102081147311964, -16.09624553401235048, -1.444131124663050159 ) ) ;
#9307=FACE_OUTER_BOUND ( 'NONE', #5244, .T. ) ;
#9315=CARTESIAN_POINT ( 'NONE',  ( -0.5616989984784648282, -12.44624546261723985, -4.522129901861166701 ) ) ;
#9323=VERTEX_POINT ( 'NONE', #26242 ) ;
#9324=CARTESIAN_POINT ( 'NONE',  ( -15.12340757463330654, 0.000000000000000000, -1.000000000000000222 ) ) ;
#9326=B_SPLINE_CURVE_WITH_KNOTS ( 'NONE', 3,
 ( #26219, #3162, #21206, #30920, #829, #23375, #13319, #18379, #21056, #3019 ),
 .UNSPECIFIED., .F., .F.,
 ( 4, 2, 2, 2, 4 ),
 ( -4.729241382666856280E-06, 0.0005792517583992175863, 0.0008712422582901618731, 0.001017237508235635697, 0.001163232758181109629 ),
 .UNSPECIFIED. ) ;
#9332=CARTESIAN_POINT ( 'NONE',  ( 25.43628654896337693, -17.54453578616444176, -1.000000000000000000 ) ) ;
#9349=CARTESIAN_POINT ( 'NONE',  ( 8.533814948527936650, -14.05305963826104332, -1.499999999999999556 ) ) ;
#9356=EDGE_CURVE ( 'NONE', #9547, #30308, #16346, .T. ) ;
#9358=CARTESIAN_POINT ( 'NONE',  ( 2.542834076925224007, 1.635051133492022979E-17, 1.603031904926282891 ) ) ;
#9379=DIRECTION ( 'NONE',  ( 0.9816271834476637537, 0.000000000000000000, -0.1908089953765453872 ) ) ;
#9385=EDGE_CURVE ( 'NONE', #8778, #5623, #6172, .T. ) ;
#9387=FACE_OUTER_BOUND ( 'NONE', #3081, .T. ) ;
#9388=CARTESIAN_POINT ( 'NONE',  ( -0.3438197445875938452, -15.06918786293965873, -1.500000000000000000 ) ) ;
#9393=EDGE_CURVE ( 'NONE', #25587, #7938, #31512, .T. ) ;
#9395=CARTESIAN_POINT ( 'NONE',  ( 107.9493514742475071, -17.34003594554901539, -4.558238555758752142 ) ) ;
#9407=DIRECTION ( 'NONE',  ( -1.000000000000000000, 2.473959037481237219E-13, 0.000000000000000000 ) ) ;
#9412=CARTESIAN_POINT ( 'NONE',  ( 3.673334745431914072, 0.0007210401945499157229, -1.066984883845929932 ) ) ;
#9413=VERTEX_POINT ( 'NONE', #9332 ) ;
#9417=CARTESIAN_POINT ( 'NONE',  ( 19.72835230534419537, -21.42792461751441735, -1.670332045613319050 ) ) ;
#9430=CARTESIAN_POINT ( 'NONE',  ( 107.5951944728457477, -19.46454432635805532, 3.536284406030664407 ) ) ;
#9443=CARTESIAN_POINT ( 'NONE',  ( 21.32535692059145660, -21.82495604402121003, -1.318256435726663955 ) ) ;
#9447=CARTESIAN_POINT ( 'NONE',  ( 7.189332377417054332, -9.531173777828719551, -1.500000000000000666 ) ) ;
#9449=CARTESIAN_POINT ( 'NONE',  ( 10.98820359953467829, -14.84698140496809415, 1.499999999999999112 ) ) ;
#9451=DIRECTION ( 'NONE',  ( -1.000000000000000000, -0.000000000000000000, -0.000000000000000000 ) ) ;
#9453=CARTESIAN_POINT ( 'NONE',  ( 9.350000000000001421, 0.000000000000000000, -1.000000000000000000 ) ) ;
#9454=EDGE_CURVE ( 'NONE', #12752, #32996, #31171, .T. ) ;
#9463=CARTESIAN_POINT ( 'NONE',  ( 23.11934981620009921, -21.92529594990386599, -1.124851831741316754 ) ) ;
#9470=CARTESIAN_POINT ( 'NONE',  ( 13.65718777918027271, -19.09288791508984318, -4.522129901861166701 ) ) ;
#9482=B_SPLINE_CURVE_WITH_KNOTS ( 'NONE', 3,
 ( #31756, #13183, #18391, #21368 ),
 .UNSPECIFIED., .F., .F.,
 ( 4, 4 ),
 ( -6.746902117120830621E-06, 2.872315617951276588E-05 ),
 .UNSPECIFIED. ) ;
#9494=CARTESIAN_POINT ( 'NONE',  ( 9.350000000000001421, 0.000000000000000000, -1.000000000000000000 ) ) ;
#9501=CARTESIAN_POINT ( 'NONE',  ( 1.653263284061800453, -10.31364870257782762, -1.500000000000000222 ) ) ;
#9515=CARTESIAN_POINT ( 'NONE',  ( 10.32252699260177131, -19.71148491318491480, -1.500000000000157208 ) ) ;
#9536=EDGE_CURVE ( 'NONE', #29208, #8502, #15181, .T. ) ;
#9545=CARTESIAN_POINT ( 'NONE',  ( 7.594557537343171738, -2.555973540833195390, -1.500000000000000000 ) ) ;
#9546=CARTESIAN_POINT ( 'NONE',  ( 107.5140540107968548, -18.29027999154679307, -5.137983268504266121 ) ) ;
#9547=VERTEX_POINT ( 'NONE', #28208 ) ;
#9548=DIRECTION ( 'NONE',  ( 0.000000000000000000, 1.000000000000000000, 0.000000000000000000 ) ) ;
#9560=( BOUNDED_CURVE ( )  B_SPLINE_CURVE ( 3, ( #14200, #1515, #16881, #14706 ),
 .UNSPECIFIED., .F., .F. ) 
 B_SPLINE_CURVE_WITH_KNOTS ( ( 4, 4 ),
 ( 4.712388980383416914, 4.904375198102664868 ),
 .UNSPECIFIED. ) 
 CURVE ( )  GEOMETRIC_REPRESENTATION_ITEM ( )  RATIONAL_B_SPLINE_CURVE ( ( 1.000000000000000000, 0.9969307989114565283, 0.9969307989114565283, 1.000000000000000000 ) ) 
 REPRESENTATION_ITEM ( '' )  );
#9563=CARTESIAN_POINT ( 'NONE',  ( 2.648464616715308306, 0.1990047044050247960, -1.630908343631500168 ) ) ;
#9566=EDGE_CURVE ( 'NONE', #16376, #6370, #20182, .T. ) ;
#9567=ORIENTED_EDGE ( 'NONE', *, *, #13071, .F. ) ;
#9569=CARTESIAN_POINT ( 'NONE',  ( -2.715612589025598211, -0.5453662152015974485, 1.748464016170372393 ) ) ;
#9574=EDGE_CURVE ( 'NONE', #7938, #926, #18576, .T. ) ;
#9576=ORIENTED_EDGE ( 'NONE', *, *, #30491, .F. ) ;
#9587=CARTESIAN_POINT ( 'NONE',  ( 17.84081991000783063, -19.48375781953909325, -5.485967528433938867 ) ) ;
#9588=CARTESIAN_POINT ( 'NONE',  ( 107.3476768466315150, -15.88628154573193463, -1.500000000000000444 ) ) ;
#9591=CARTESIAN_POINT ( 'NONE',  ( -0.2493515011842071527, -1.403010508276806068, 5.485967528433933538 ) ) ;
#9598=EDGE_LOOP ( 'NONE', ( #14318, #26629, #14340, #32343, #173, #4804 ) ) ;
#9615=CARTESIAN_POINT ( 'NONE',  ( -1.924689738998526689, -13.55751938318336514, 1.500000000000000222 ) ) ;
#9620=CARTESIAN_POINT ( 'NONE',  ( 107.8717334959383010, -16.22235636682134441, -1.414040860180981740 ) ) ;
#9653=CARTESIAN_POINT ( 'NONE',  ( 21.36097421961354925, -21.76718868951427055, 1.410897148389129052 ) ) ;
#9655=AXIS2_PLACEMENT_3D ( 'NONE', #30779, #25562, #33094 ) ;
#9670=CARTESIAN_POINT ( 'NONE',  ( 3.091618246663842218, -11.74990798379343104, -1.759199118974999587 ) ) ;
#9671=CARTESIAN_POINT ( 'NONE',  ( 41.06247019076344884, -19.55897407381494091, 1.500000000000000444 ) ) ;
#9684=VECTOR ( 'NONE', #6079, 1000.000000000000000 ) ;
#9688=ADVANCED_FACE ( 'NONE', ( #957 ), #18514, .F. ) ;
#9690=EDGE_CURVE ( 'NONE', #7539, #2628, #9225, .T. ) ;
#9693=CARTESIAN_POINT ( 'NONE',  ( -0.3252456059815400646, -14.55958727885318993, -1.745204947688217434 ) ) ;
#9704=CARTESIAN_POINT ( 'NONE',  ( -15.12340757463330654, -21.93932300455815465, -1.000000000000000222 ) ) ;
#9715=DIRECTION ( 'NONE',  ( 1.000000000000000000, 0.000000000000000000, 0.000000000000000000 ) ) ;
#9724=CARTESIAN_POINT ( 'NONE',  ( 107.4538619861916402, -17.41535791789517518, -4.649137322120033389 ) ) ;
#9748=CARTESIAN_POINT ( 'NONE',  ( 2.949938889207336601, 0.4708014538555321260, -1.389575531037015477 ) ) ;
#9753=CARTESIAN_POINT ( 'NONE',  ( 107.4500593345376558, -17.36019228850485163, -4.522129901861164925 ) ) ;
#9754=VECTOR ( 'NONE', #20773, 1000.000000000000000 ) ;
#9755=CARTESIAN_POINT ( 'NONE',  ( 0.000000000000000000, -28.43932300454937590, -1.500000000000000000 ) ) ;
#9761=AXIS2_PLACEMENT_3D ( 'NONE', #21900, #14355, #16543 ) ;
#9774=CARTESIAN_POINT ( 'NONE',  ( -50.60000000000000142, -10.96966150227468972, -0.2618072999578781590 ) ) ;
#9775=CARTESIAN_POINT ( 'NONE',  ( 24.35085591271619876, -17.33674746172420811, 1.318654801572268553 ) ) ;
#9776=EDGE_CURVE ( 'NONE', #12927, #18318, #13789, .T. ) ;
#9778=CYLINDRICAL_SURFACE ( 'NONE', #77, 5.000000000000000888 ) ;
#9787=TOROIDAL_SURFACE ( 'NONE', #21022, 5.500000000000001776, 0.5000000000000000000 ) ;
#9796=ADVANCED_FACE ( 'NONE', ( #15087 ), #24339, .T. ) ;
#9798=CARTESIAN_POINT ( 'NONE',  ( 21.04767255915003332, -17.06392231637734724, 1.500000000000000666 ) ) ;
#9801=ORIENTED_EDGE ( 'NONE', *, *, #10496, .T. ) ;
#9802=CARTESIAN_POINT ( 'NONE',  ( 5.994372355876373959, -18.63462559044425149, 1.499999999999998668 ) ) ;
#9803=ORIENTED_EDGE ( 'NONE', *, *, #31759, .T. ) ;
#9809=CARTESIAN_POINT ( 'NONE',  ( 107.9802527803230419, -17.78500706576073753, 4.325704939602341703 ) ) ;
#9811=CARTESIAN_POINT ( 'NONE',  ( 107.5617944031221640, -18.98359742639815551, -4.522129901861166701 ) ) ;
#9814=CARTESIAN_POINT ( 'NONE',  ( 21.44478664388827127, -21.75412686751143099, -1.457848360901668139 ) ) ;
#9815=VECTOR ( 'NONE', #10607, 1000.000000000000000 ) ;
#9820=DIRECTION ( 'NONE',  ( -0.1908089953765452762, 0.000000000000000000, 0.9816271834476639757 ) ) ;
#9829=CARTESIAN_POINT ( 'NONE',  ( 23.24441267594672311, -21.93876234581717810, 1.082412871822684419 ) ) ;
#9834=B_SPLINE_CURVE_WITH_KNOTS ( 'NONE', 3,
 ( #772, #3930, #31843, #16285, #13756, #18972, #21299, #14104, #24131, #24304, #9065, #29158, #10954, #1417, #21787, #6246, #31995, #19292, #15945, #13431, #3268, #23652, #31354, #18626, #28820, #16110, #26342, #18798, #3449, #13605, #23811, #31502, #8587, #7250, #6746, #2239, #27484, #30177 ),
 .UNSPECIFIED., .F., .F.,
 ( 4, 2, 2, 2, 2, 2, 2, 2, 2, 2, 2, 2, 2, 2, 2, 2, 2, 2, 4 ),
 ( 2.954127631045189498E-16, 0.003856977557342960126, 0.007713955114685625350, 0.01157093267202828971, 0.01349942145069962102, 0.01542791022937095233, 0.01735639900804228711, 0.01832064339737795103, 0.01928488778671362189, 0.02121337656538495320, 0.02217762095472062753, 0.02314186534405629492, 0.02362398753872413382, 0.02410610973339196578, 0.02507035412272764011, 0.02603459851206331443, 0.02699884290139898529, 0.02892733168007033048, 0.03085582045874168261 ),
 .UNSPECIFIED. ) ;
#9837=CARTESIAN_POINT ( 'NONE',  ( 0.1347475173545765736, -7.019624077805855400, 1.774480656747167373 ) ) ;
#9843=VERTEX_POINT ( 'NONE', #26674 ) ;
#9857=CARTESIAN_POINT ( 'NONE',  ( 0.7551355282337928188, -8.141491703254255086, -1.499999999999999556 ) ) ;
#9858=CARTESIAN_POINT ( 'NONE',  ( 71.53201042711403090, -18.09776336788796058, 0.9788672205888330202 ) ) ;
#9859=VERTEX_POINT ( 'NONE', #16818 ) ;
#9866=CARTESIAN_POINT ( 'NONE',  ( 24.37248106196387454, -17.41561295275149135, 1.432003413861882901 ) ) ;
#9867=ORIENTED_EDGE ( 'NONE', *, *, #9196, .F. ) ;
#9872=CARTESIAN_POINT ( 'NONE',  ( -1.201691756929461397, -13.92897885394997992, -1.500000000000556222 ) ) ;
#9881=DIRECTION ( 'NONE',  ( 2.473959037481237219E-13, 1.000000000000000000, -0.000000000000000000 ) ) ;
#9889=ADVANCED_FACE ( 'NONE', ( #4737 ), #32223, .T. ) ;
#9893=CARTESIAN_POINT ( 'NONE',  ( -31.57659242536668742, -28.43932300454937590, -0.9999999999999997780 ) ) ;
#9901=CARTESIAN_POINT ( 'NONE',  ( 108.0288784395952320, -18.48520446273847995, -4.337460765736292245 ) ) ;
#9905=CARTESIAN_POINT ( 'NONE',  ( 23.27353278736380204, -21.94187821002792660, 1.000000000000000000 ) ) ;
#9914=DIRECTION ( 'NONE',  ( -1.000000000000000000, 0.000000000000000000, 0.000000000000000000 ) ) ;
#9916=CARTESIAN_POINT ( 'NONE',  ( 2.712282326253041553, -0.4283266402566512365, -1.500000000000000666 ) ) ;
#9920=ADVANCED_FACE ( 'NONE', ( #12419 ), #1300, .T. ) ;
#9922=VERTEX_POINT ( 'NONE', #28284 ) ;
#9930=CARTESIAN_POINT ( 'NONE',  ( 21.36097421961354925, -21.76718868951427055, 1.410897148389129052 ) ) ;
#9942=CARTESIAN_POINT ( 'NONE',  ( -14.85000000000000142, -10.96966150227469328, 1.500000000000000000 ) ) ;
#9943=EDGE_CURVE ( 'NONE', #11449, #7955, #15038, .T. ) ;
#9948=CARTESIAN_POINT ( 'NONE',  ( -15.00280984543113583, -21.93932300455818307, 1.000000000000000000 ) ) ;
#9952=CYLINDRICAL_SURFACE ( 'NONE', #13483, 0.5000000000000000000 ) ;
#9953=CARTESIAN_POINT ( 'NONE',  ( 107.9809968313877562, -17.79572121599716539, 4.354976952678953239 ) ) ;
#9957=CARTESIAN_POINT ( 'NONE',  ( 74.44693909927218556, -23.04272217940714995, -0.9788672205760856615 ) ) ;
#9960=CARTESIAN_POINT ( 'NONE',  ( -3.262323615140995781, -10.74303876590519558, 1.743566368971870340 ) ) ;
#9967=DIRECTION ( 'NONE',  ( -0.000000000000000000, -0.000000000000000000, 1.000000000000000000 ) ) ;
#9970=CARTESIAN_POINT ( 'NONE',  ( 107.6641765185768378, -20.45809951660586634, 1.500000000000000000 ) ) ;
#9983=VERTEX_POINT ( 'NONE', #23288 ) ;
#9985=ORIENTED_EDGE ( 'NONE', *, *, #11427, .T. ) ;
#9991=EDGE_LOOP ( 'NONE', ( #15353, #14610 ) ) ;
#10005=CARTESIAN_POINT ( 'NONE',  ( 107.9916441005483563, -18.73362038781918315, -4.428447085748415724 ) ) ;
#10009=CARTESIAN_POINT ( 'NONE',  ( 0.9232102171129921153, 0.000000000000000000, 4.522129901861157819 ) ) ;
#10016=CARTESIAN_POINT ( 'NONE',  ( 23.30536738592035562, -17.34558290870699793, 1.520589546897618716 ) ) ;
#10017=ORIENTED_EDGE ( 'NONE', *, *, #12640, .T. ) ;
#10024=CARTESIAN_POINT ( 'NONE',  ( -0.05272361993596155066, -14.78973072807761469, -1.745421474541472007 ) ) ;
#10040=CARTESIAN_POINT ( 'NONE',  ( -3.616018626656801960, -10.49347358198851943, 1.500000000000000000 ) ) ;
#10043=CARTESIAN_POINT ( 'NONE',  ( 107.6226684525294814, -19.86014998405252641, -2.725480252158540839 ) ) ;
#10048=CARTESIAN_POINT ( 'NONE',  ( -4.161566758114229714, -8.294289541356487661, 1.499999999999999778 ) ) ;
#10051=EDGE_LOOP ( 'NONE', ( #25127, #7761, #28582, #31280 ) ) ;
#10058=CARTESIAN_POINT ( 'NONE',  ( 21.32535692059145660, -21.82495604402121003, -1.318256435726663955 ) ) ;
#10075=CARTESIAN_POINT ( 'NONE',  ( 107.5184162292005539, -18.35373766169381327, 5.121412927745073951 ) ) ;
#10078=VERTEX_POINT ( 'NONE', #26944 ) ;
#10081=CARTESIAN_POINT ( 'NONE',  ( -50.60000000000000142, -10.96966150227468972, -1.000000000000000000 ) ) ;
#10082=CARTESIAN_POINT ( 'NONE',  ( 1.828104818894226380, -1.262475772535087915, -1.500000000000000000 ) ) ;
#10084=CARTESIAN_POINT ( 'NONE',  ( 8.161453797571457613, -14.35007110565979183, -1.755185239838192857 ) ) ;
#10085=CARTESIAN_POINT ( 'NONE',  ( 23.24441267594537308, -21.93876234581703599, -1.082412871821091471 ) ) ;
#10086=CARTESIAN_POINT ( 'NONE',  ( -17.45597128428593692, -25.93932300454937945, 11.00000000000000000 ) ) ;
#10090=CARTESIAN_POINT ( 'NONE',  ( 25.43628654896174623, -17.54453578616395149, 1.000000000000000444 ) ) ;
#10091=CARTESIAN_POINT ( 'NONE',  ( -4.637780547552199373, -6.332425682048902438, 0.9788672205877712029 ) ) ;
#10092=CARTESIAN_POINT ( 'NONE',  ( 0.8407900506754618641, -11.56055812333405441, 4.522129901861156931 ) ) ;
#10107=CARTESIAN_POINT ( 'NONE',  ( 18.53107884607683076, -16.42960242685250449, 1.500000000000000000 ) ) ;
#10110=ORIENTED_EDGE ( 'NONE', *, *, #14920, .T. ) ;
#10112=CARTESIAN_POINT ( 'NONE',  ( 107.6641398346805545, -20.45810202417278134, -1.500000000000000000 ) ) ;
#10115=CARTESIAN_POINT ( 'NONE',  ( 107.9932960675740219, -17.97282715741293302, -4.597091762064528631 ) ) ;
#10117=ORIENTED_EDGE ( 'NONE', *, *, #24107, .T. ) ;
#10120=CARTESIAN_POINT ( 'NONE',  ( 21.68866787702163634, -21.76712446977036919, -1.490904000146909159 ) ) ;
#10128=CARTESIAN_POINT ( 'NONE',  ( 24.55981180825490640, -17.46058140477835963, 1.484973660491783143 ) ) ;
#10142=CARTESIAN_POINT ( 'NONE',  ( 0.1152454363327600484, -6.520582226636352452, 1.773866594758318538 ) ) ;
#10154=CARTESIAN_POINT ( 'NONE',  ( 107.4500373638809947, -17.36019379023286646, 4.522129901861156931 ) ) ;
#10159=ADVANCED_FACE ( 'NONE', ( #29123 ), #11070, .F. ) ;
#10161=CARTESIAN_POINT ( 'NONE',  ( -52.69999999999999574, -10.96966150227468972, 7.500000000000000000 ) ) ;
#10171=CARTESIAN_POINT ( 'NONE',  ( 107.5617723795401872, -18.98359893170738744, -4.522129901861166701 ) ) ;
#10175=CARTESIAN_POINT ( 'NONE',  ( 24.08745121460989225, -17.31475877198389668, -1.374955925957151992 ) ) ;
#10183=CARTESIAN_POINT ( 'NONE',  ( 2.288217443798745698, -16.46508028272004154, -1.747280182634695977 ) ) ;
#10188=CARTESIAN_POINT ( 'NONE',  ( 107.9116956367129205, -16.79780125264633384, 2.301619431081807221 ) ) ;
#10201=ORIENTED_EDGE ( 'NONE', *, *, #740, .T. ) ;
#10202=AXIS2_PLACEMENT_3D ( 'NONE', #23835, #13945, #11467 ) ;
#10208=VECTOR ( 'NONE', #5339, 1000.000000000000000 ) ;
#10212=CARTESIAN_POINT ( 'NONE',  ( 107.6337546485926993, -20.01978338540836688, 2.398305884358065576 ) ) ;
#10213=AXIS2_PLACEMENT_3D ( 'NONE', #23374, #478, #31746 ) ;
#10215=CARTESIAN_POINT ( 'NONE',  ( -3.111318361680354805, -11.33170398610737450, 1.499999999999761080 ) ) ;
#10218=CARTESIAN_POINT ( 'NONE',  ( 108.0286880956687412, -18.48246355754853454, -4.344949451024058718 ) ) ;
#10223=VECTOR ( 'NONE', #3124, 1000.000000000000000 ) ;
#10229=CARTESIAN_POINT ( 'NONE',  ( 17.33093461831547444, -21.43932300456618378, -1.500000000000000000 ) ) ;
#10230=ORIENTED_EDGE ( 'NONE', *, *, #31449, .T. ) ;
#10233=MANIFOLD_SOLID_BREP ( 'Fillet2', #28586 ) ;
#10242=CARTESIAN_POINT ( 'NONE',  ( 13.13178786249840435, -17.31629153505178920, -4.522129901861164925 ) ) ;
#10244=CARTESIAN_POINT ( 'NONE',  ( 24.24719734710406627, -17.18125539888338693, 1.000000000000000222 ) ) ;
#10255=CARTESIAN_POINT ( 'NONE',  ( -31.69719015456885103, -21.93932300455405482, 1.000000000000000444 ) ) ;
#10258=CARTESIAN_POINT ( 'NONE',  ( 12.65465643788354200, -15.70291107026620914, 1.500000000000000000 ) ) ;
#10261=CARTESIAN_POINT ( 'NONE',  ( 0.5105742983572999494, -4.179359922481789447, -1.765450449227109919 ) ) ;
#10263=DIRECTION ( 'NONE',  ( 0.4851627901281758692, 0.000000000000000000, -0.8744238486426610946 ) ) ;
#10274=CIRCLE ( 'NONE', #24645, 0.5000000000000000000 ) ;
#10285=DIRECTION ( 'NONE',  ( 0.4851627901281774236, 0.000000000000000000, 0.8744238486426602064 ) ) ;
#10291=TOROIDAL_SURFACE ( 'NONE', #28985, 4.499999999999997335, 0.5000000000000000000 ) ;
#10295=CIRCLE ( 'NONE', #32721, 0.4499999999999990119 ) ;
#10309=PLANE ( 'NONE',  #2363 ) ;
#10316=CARTESIAN_POINT ( 'NONE',  ( 2.600000000000000089, -0.5000000000000000000, 1.500000000000000000 ) ) ;
#10319=TOROIDAL_SURFACE ( 'NONE', #6566, 4.499999999999997335, 0.5000000000000000000 ) ;
#10322=CARTESIAN_POINT ( 'NONE',  ( 23.20536337411656902, -21.93817982951601664, 1.034580775994869528 ) ) ;
#10323=DIRECTION ( 'NONE',  ( -0.000000000000000000, -0.000000000000000000, 1.000000000000000000 ) ) ;
#10332=CARTESIAN_POINT ( 'NONE',  ( 0.6825714480081905844, -9.110483382199172198, 1.769152918636197835 ) ) ;
#10333=CARTESIAN_POINT ( 'NONE',  ( 13.25896750271793145, -14.28336940137698541, 1.500000000000000000 ) ) ;
#10334=EDGE_LOOP ( 'NONE', ( #22980, #19725, #7910, #15449 ) ) ;
#10340=AXIS2_PLACEMENT_3D ( 'NONE', #25460, #2730, #23127 ) ;
#10355=CARTESIAN_POINT ( 'NONE',  ( 41.92799935459299832, -21.01937708444107500, 4.522129901861157819 ) ) ;
#10360=CARTESIAN_POINT ( 'NONE',  ( 0.000000000000000000, 0.000000000000000000, -1.000000000000000000 ) ) ;
#10361=ORIENTED_EDGE ( 'NONE', *, *, #3830, .T. ) ;
#10362=CARTESIAN_POINT ( 'NONE',  ( 23.85741365831481176, -17.28578219493698143, 1.405688364265740065 ) ) ;
#10365=AXIS2_PLACEMENT_3D ( 'NONE', #5978, #21352, #5511 ) ;
#10370=CARTESIAN_POINT ( 'NONE',  ( -50.60000000000000142, -10.96966150227468972, 6.999999999999999112 ) ) ;
#10388=EDGE_CURVE ( 'NONE', #6959, #4832, #21320, .T. ) ;
#10390=CARTESIAN_POINT ( 'NONE',  ( 43.74661801760413482, -24.08792321988613594, 1.500000000000000000 ) ) ;
#10395=EDGE_LOOP ( 'NONE', ( #7032, #31118, #3347, #12766, #4192 ) ) ;
#10398=CARTESIAN_POINT ( 'NONE',  ( 3.379077383500962650, -17.49391738930246376, 1.500000000000001332 ) ) ;
#10423=CARTESIAN_POINT ( 'NONE',  ( -2.626726202933858723, 0.09953226261353739779, 1.366272513173315772 ) ) ;
#10424=CARTESIAN_POINT ( 'NONE',  ( -2.994539215707400892, -0.08249776133298661329, 1.285182061456009439 ) ) ;
#10434=FACE_OUTER_BOUND ( 'NONE', #29046, .T. ) ;
#10439=CARTESIAN_POINT ( 'NONE',  ( 107.9694961684101457, -17.63011453012341789, 4.008137637261066644 ) ) ;
#10440=B_SPLINE_CURVE_WITH_KNOTS ( 'NONE', 3,
 ( #17419, #27616, #4717, #17566 ),
 .UNSPECIFIED., .F., .F.,
 ( 4, 4 ),
 ( 0.000000000000000000, 2.207496556392325519E-08 ),
 .UNSPECIFIED. ) ;
#10442=CARTESIAN_POINT ( 'NONE',  ( 6.705444383089634641, -13.33025968055571120, 1.499999999999998446 ) ) ;
#10444=EDGE_CURVE ( 'NONE', #21614, #8757, #31738, .T. ) ;
#10445=CARTESIAN_POINT ( 'NONE',  ( -3.827997810768590359, -10.69410007036526267, 0.9788672205877712029 ) ) ;
#10454=CARTESIAN_POINT ( 'NONE',  ( 23.22564588060105706, -21.93932300456764395, -1.010482809524661629 ) ) ;
#10464=CARTESIAN_POINT ( 'NONE',  ( -2.819379691724114512, -6.927609664243465026, -4.522129901861166701 ) ) ;
#10471=ORIENTED_EDGE ( 'NONE', *, *, #8916, .F. ) ;
#10473=CARTESIAN_POINT ( 'NONE',  ( 108.0887845003129542, -19.34783683432074142, 2.566390659084664350 ) ) ;
#10475=DIRECTION ( 'NONE',  ( 0.000000000000000000, 1.000000000000000000, -0.000000000000000000 ) ) ;
#10491=CARTESIAN_POINT ( 'NONE',  ( 0.8040887157109507521, -3.277015635683791395, 1.762426081327307825 ) ) ;
#10492=CARTESIAN_POINT ( 'NONE',  ( 24.38441422956826088, -17.22282062799385116, 1.499999999999444222 ) ) ;
#10496=EDGE_CURVE ( 'NONE', #9056, #29074, #9192, .T. ) ;
#10498=CARTESIAN_POINT ( 'NONE',  ( 1.635980141547796585, -1.437409680492520936, 1.758786303110331906 ) ) ;
#10509=CARTESIAN_POINT ( 'NONE',  ( 19.76529769139576587, -16.89702959469647325, -1.499999999998181677 ) ) ;
#10514=CARTESIAN_POINT ( 'NONE',  ( -15.12340757463330654, -28.43932300454936879, -1.500000000000000000 ) ) ;
#10516=ORIENTED_EDGE ( 'NONE', *, *, #28340, .T. ) ;
#10518=CARTESIAN_POINT ( 'NONE',  ( 24.01922593961184305, -17.30645187339492352, -1.384626276794869604 ) ) ;
#10527=CARTESIAN_POINT ( 'NONE',  ( -31.57659242536668742, -27.93932300454937590, -0.9999999999999997780 ) ) ;
#10532=ORIENTED_EDGE ( 'NONE', *, *, #31449, .F. ) ;
#10544=VERTEX_POINT ( 'NONE', #14484 ) ;
#10547=CARTESIAN_POINT ( 'NONE',  ( -4.548081766001798698, -6.140004230154746168, 1.499999999999999556 ) ) ;
#10550=CARTESIAN_POINT ( 'NONE',  ( 22.00639167669224960, -21.80013755708282730, -1.499999999999999556 ) ) ;
#10572=CARTESIAN_POINT ( 'NONE',  ( 107.9869154117469492, -17.88094730081049377, 4.507188101940097447 ) ) ;
#10578=ORIENTED_EDGE ( 'NONE', *, *, #9690, .F. ) ;
#10580=ORIENTED_EDGE ( 'NONE', *, *, #7674, .F. ) ;
#10582=EDGE_CURVE ( 'NONE', #12204, #25155, #6549, .T. ) ;
#10584=CARTESIAN_POINT ( 'NONE',  ( 21.34939358370770535, -21.78237682584225254, 1.377397332511454353 ) ) ;
#10587=CARTESIAN_POINT ( 'NONE',  ( 1.853623169654749159, -10.69666880112111684, -1.762806831122527118 ) ) ;
#10589=CARTESIAN_POINT ( 'NONE',  ( 25.46419143545908526, -18.07592536767254643, -1.500000000000000000 ) ) ;
#10591=CARTESIAN_POINT ( 'NONE',  ( 107.9730816776244069, -17.68174497084636343, 4.113993602947243033 ) ) ;
#10593=EDGE_CURVE ( 'NONE', #6331, #18408, #10891, .T. ) ;
#10607=DIRECTION ( 'NONE',  ( -0.000000000000000000, -0.000000000000000000, -1.000000000000000000 ) ) ;
#10611=EDGE_CURVE ( 'NONE', #31289, #6686, #29277, .T. ) ;
#10617=VERTEX_POINT ( 'NONE', #1432 ) ;
#10618=DIRECTION ( 'NONE',  ( 2.498001805406600196E-13, 1.000000000000000000, 0.000000000000000000 ) ) ;
#10619=EDGE_CURVE ( 'NONE', #21890, #15271, #22026, .T. ) ;
#10623=CARTESIAN_POINT ( 'NONE',  ( -2.715578077270538682, -0.5452878916197804182, 1.748464050160077887 ) ) ;
#10624=ORIENTED_EDGE ( 'NONE', *, *, #3504, .T. ) ;
#10625=CARTESIAN_POINT ( 'NONE',  ( -15.09999999999999609, -27.93932300454937590, 1.500000000000000000 ) ) ;
#10626=CARTESIAN_POINT ( 'NONE',  ( 108.1216519843055295, -19.82112042741262670, 1.596396689095263222 ) ) ;
#10627=DIRECTION ( 'NONE',  ( 1.000000000000000000, 0.000000000000000000, 0.000000000000000000 ) ) ;
#10631=CARTESIAN_POINT ( 'NONE',  ( -1.047937531484008700, -4.989690239014953121, -4.522129901861164925 ) ) ;
#10644=DIRECTION ( 'NONE',  ( 1.000000000000000000, 0.000000000000000000, 0.000000000000000000 ) ) ;
#10645=CARTESIAN_POINT ( 'NONE',  ( 9.555580689063649658, -12.32072190999856431, 1.500000000000000000 ) ) ;
#10646=VERTEX_POINT ( 'NONE', #9083 ) ;
#10658=ORIENTED_EDGE ( 'NONE', *, *, #10619, .F. ) ;
#10659=DIRECTION ( 'NONE',  ( -1.224646799147353207E-16, 1.000000000000000000, 0.000000000000000000 ) ) ;
#10688=TOROIDAL_SURFACE ( 'NONE', #19798, 8.000000000000000000, 0.5000000000000000000 ) ;
#10689=CARTESIAN_POINT ( 'NONE',  ( 10.93412304894858167, -12.62793677521797164, -0.9999999999999997780 ) ) ;
#10690=ORIENTED_EDGE ( 'NONE', *, *, #2729, .F. ) ;
#10697=CARTESIAN_POINT ( 'NONE',  ( 11.20269353100556486, -13.34333142745244238, 1.499999999999999778 ) ) ;
#10699=DIRECTION ( 'NONE',  ( -0.1908089953765453595, 1.324003374828971999E-15, -0.9816271834476638647 ) ) ;
#10704=CARTESIAN_POINT ( 'NONE',  ( -4.125289193777756935, -7.575181221222853090, 1.744514882266629874 ) ) ;
#10729=CARTESIAN_POINT ( 'NONE',  ( 0.3277201397524639459, -5.271209332775584677, -1.500000000000000444 ) ) ;
#10731=CARTESIAN_POINT ( 'NONE',  ( 107.5501414772658961, -18.81481929958330568, 4.827012719627553849 ) ) ;
#10735=CARTESIAN_POINT ( 'NONE',  ( -31.67864539881508179, -25.93932300454937945, 1.095404497688271528 ) ) ;
#10738=CARTESIAN_POINT ( 'NONE',  ( -2.760161469795538558, -0.06813755667566065433, 1.269913365998487365 ) ) ;
#10751=CARTESIAN_POINT ( 'NONE',  ( 24.24156412053827836, -17.70199322286653043, -1.500000000000000000 ) ) ;
#10753=CARTESIAN_POINT ( 'NONE',  ( 107.9552175441146176, -17.42450589234269387, 3.586585920852337406 ) ) ;
#10760=CARTESIAN_POINT ( 'NONE',  ( -0.2168228499942651821, -15.24168959956947234, 0.9788672205877712029 ) ) ;
#10763=FACE_OUTER_BOUND ( 'NONE', #11187, .T. ) ;
#10775=CARTESIAN_POINT ( 'NONE',  ( 19.69555400981637661, -21.64588847999016252, -1.456500879219860600 ) ) ;
#10779=LINE ( 'NONE', #28335, #9186 ) ;
#10781=B_SPLINE_SURFACE_WITH_KNOTS ( 'NONE', 3, 1, ( 
 ( #6228, #14079 ),
 ( #16412, #13890 ),
 ( #24281, #17262 ),
 ( #24936, #27277 ) ),
 .UNSPECIFIED., .F., .F., .F.,
 ( 4, 4 ),
 ( 2, 2 ),
 ( 0.001101513941755155341, 1.000000000000000000 ),
 ( 0.000000000000000000, 1.000000000000000000 ),
 .UNSPECIFIED. ) ;
#10799=CARTESIAN_POINT ( 'NONE',  ( -23.35000000000000142, -10.96966150227469505, -11.50000000000000000 ) ) ;
#10802=DIRECTION ( 'NONE',  ( -1.000000000000000000, 0.000000000000000000, 0.000000000000000000 ) ) ;
#10805=CARTESIAN_POINT ( 'NONE',  ( 23.19698579062264443, -21.93770718891966709, 1.040523306341560428 ) ) ;
#10809=CARTESIAN_POINT ( 'NONE',  ( 21.36776303755519635, -21.72386242187942429, 1.606475753955313612 ) ) ;
#10821=CARTESIAN_POINT ( 'NONE',  ( 10.11068945975240396, -12.10067465535042963, 1.000000000000000000 ) ) ;
#10822=AXIS2_PLACEMENT_3D ( 'NONE', #10527, #20741, #7210 ) ;
#10823=ORIENTED_EDGE ( 'NONE', *, *, #21682, .F. ) ;
#10827=CARTESIAN_POINT ( 'NONE',  ( 1.205515411592139596, -3.374104910866653650, 1.499999999999999334 ) ) ;
#10856=EDGE_CURVE ( 'NONE', #635, #8281, #16144, .T. ) ;
#10857=CARTESIAN_POINT ( 'NONE',  ( -2.617344628312510135, 0.000000000000000000, -1.468739241856748867 ) ) ;
#10862=CARTESIAN_POINT ( 'NONE',  ( 107.9718772962921776, -17.66440217927672762, -4.377269687808228227 ) ) ;
#10863=DIRECTION ( 'NONE',  ( -0.000000000000000000, 0.000000000000000000, 1.000000000000000000 ) ) ;
#10867=B_SPLINE_CURVE_WITH_KNOTS ( 'NONE', 3,
 ( #22768, #15385, #30456, #8220, #5057, #18420, #10043, #25773, #5556, #27950 ),
 .UNSPECIFIED., .F., .F.,
 ( 4, 3, 3, 4 ),
 ( 8.673617379884035472E-19, 0.001000000000064768307, 0.002000000000131801729, 0.003364209820980246842 ),
 .UNSPECIFIED. ) ;
#10882=CARTESIAN_POINT ( 'NONE',  ( 13.13178786249840435, -17.31629153505178920, -4.522129901861164925 ) ) ;
#10885=CARTESIAN_POINT ( 'NONE',  ( 0.9067410411906208223, -4.287332675150268280, -1.499999999999999556 ) ) ;
#10887=ORIENTED_EDGE ( 'NONE', *, *, #13334, .T. ) ;
#10891=( BOUNDED_CURVE ( )  B_SPLINE_CURVE ( 3, ( #25879, #3138, #12650, #26034 ),
 .UNSPECIFIED., .F., .F. ) 
 B_SPLINE_CURVE_WITH_KNOTS ( ( 4, 4 ),
 ( 1.570796326794896558, 1.762782544514152949 ),
 .UNSPECIFIED. ) 
 CURVE ( )  GEOMETRIC_REPRESENTATION_ITEM ( )  RATIONAL_B_SPLINE_CURVE ( ( 1.000000000000000000, 0.9969307989114561952, 0.9969307989114561952, 1.000000000000000000 ) ) 
 REPRESENTATION_ITEM ( '' )  );
#10893=CARTESIAN_POINT ( 'NONE',  ( -15.12340757463330654, -27.93932300454937590, -1.500000000000000000 ) ) ;
#10899=CARTESIAN_POINT ( 'NONE',  ( 107.3476950949991391, -15.88628029827230925, 1.500000000000000000 ) ) ;
#10911=DIRECTION ( 'NONE',  ( 1.000000000000000000, 0.000000000000000000, 0.000000000000000000 ) ) ;
#10914=CARTESIAN_POINT ( 'NONE',  ( 107.9851147162994351, -17.85501773432275741, 4.472621839076901473 ) ) ;
#10916=ORIENTED_EDGE ( 'NONE', *, *, #3420, .T. ) ;
#10923=ORIENTED_EDGE ( 'NONE', *, *, #19820, .F. ) ;
#10929=ORIENTED_EDGE ( 'NONE', *, *, #32794, .T. ) ;
#10933=CARTESIAN_POINT ( 'NONE',  ( 23.15368348421675293, -16.86203458153637058, -1.000000000000000444 ) ) ;
#10938=CARTESIAN_POINT ( 'NONE',  ( 9.130194559407742716, -14.25877845138838751, 1.499999999999999778 ) ) ;
#10941=CARTESIAN_POINT ( 'NONE',  ( 110.4915906369627123, -18.78144465615449832, 4.522129901861158707 ) ) ;
#10942=CARTESIAN_POINT ( 'NONE',  ( 3.406359441062990268, 0.6647459039674525894, 0.7949826693599013616 ) ) ;
#10954=CARTESIAN_POINT ( 'NONE',  ( 4.959835597591649048, -12.47346298686548849, -1.499999999999999334 ) ) ;
#10956=EDGE_LOOP ( 'NONE', ( #5194, #18135, #28606, #5568, #1748, #24892, #16121, #3528 ) ) ;
#10968=CARTESIAN_POINT ( 'NONE',  ( 21.32535692059155963, -21.82495604402122069, 1.318256435726650633 ) ) ;
#10976=CARTESIAN_POINT ( 'NONE',  ( -2.673784050203184215, -0.4252642838279113713, -1.725835265963347798 ) ) ;
#10980=DIRECTION ( 'NONE',  ( 1.000000000000000000, 0.000000000000000000, 0.000000000000000000 ) ) ;
#10991=CARTESIAN_POINT ( 'NONE',  ( 8.486535498732452609, -10.66169397748241998, 1.000000000000000000 ) ) ;
#10996=CARTESIAN_POINT ( 'NONE',  ( 2.281627749324421917, -0.2935656086769610207, 1.757435426329174044 ) ) ;
#11007=CARTESIAN_POINT ( 'NONE',  ( -23.35000000000000142, -10.96966150227469505, -11.00000000000000000 ) ) ;
#11016=DIRECTION ( 'NONE',  ( 0.000000000000000000, -1.000000000000000000, 0.000000000000000000 ) ) ;
#11017=CARTESIAN_POINT ( 'NONE',  ( -1.425727661597485874, -5.130997865967673377, 5.485967528433933538 ) ) ;
#11019=FACE_OUTER_BOUND ( 'NONE', #4592, .T. ) ;
#11020=CARTESIAN_POINT ( 'NONE',  ( 17.33093461831550286, -21.43932300456650353, -1.499999999999999112 ) ) ;
#11023=EDGE_CURVE ( 'NONE', #140, #13341, #30481, .T. ) ;
#11032=EDGE_CURVE ( 'NONE', #13341, #28440, #9326, .T. ) ;
#11035=CARTESIAN_POINT ( 'NONE',  ( -2.986472588763606328, 8.217301096052205839E-30, -1.110524573187248620 ) ) ;
#11040=CARTESIAN_POINT ( 'NONE',  ( 6.751043368244950216, -5.560327249377744252, 1.500000000000000222 ) ) ;
#11042=CARTESIAN_POINT ( 'NONE',  ( 0.5362739657699832074, -4.520875221154571300, -1.499999999999964917 ) ) ;
#11045=ORIENTED_EDGE ( 'NONE', *, *, #20557, .T. ) ;
#11056=CARTESIAN_POINT ( 'NONE',  ( -2.753702574462014052, -0.2727682784858890819, -1.454428814729283870 ) ) ;
#11061=ORIENTED_EDGE ( 'NONE', *, *, #13580, .T. ) ;
#11062=CARTESIAN_POINT ( 'NONE',  ( 20.08514749461460269, -21.49093168682494692, 1.640482353826733242 ) ) ;
#11066=CARTESIAN_POINT ( 'NONE',  ( 107.9806159500837452, -17.79023661996872718, 4.339996101326005551 ) ) ;
#11070=( BOUNDED_SURFACE ( )  B_SPLINE_SURFACE ( 3, 2, ( 
 ( #31315, #26290, #13870 ),
 ( #23601, #5870, #3401 ),
 ( #23921, #31636, #6209 ),
 ( #19083, #23771, #885 ),
 ( #11062, #31461, #8540 ),
 ( #16392, #24077, #29270 ),
 ( #26604, #1207, #6357 ),
 ( #16552, #3882, #14057 ),
 ( #6707, #24764, #1695 ),
 ( #32464, #14872, #27093 ) ),
 .UNSPECIFIED., .F., .F., .F. ) 
 B_SPLINE_SURFACE_WITH_KNOTS ( ( 4, 2, 2, 2, 4 ),
 ( 3, 3 ),
 ( 0.01791456443260443579, 0.01997296323900674131, 0.02100216264220789580, 0.02151676234380847305, 0.02203136204540905030 ),
 ( 0.000000000000000000, 1.000000000000000000 ),
 .UNSPECIFIED. ) 
 GEOMETRIC_REPRESENTATION_ITEM ( )  RATIONAL_B_SPLINE_SURFACE ( (
 ( 1.000000000000000000, 0.8490876263417815872, 1.000000000000000000),
 ( 1.000000000000000000, 0.8789005871655674040, 1.000000000000000000),
 ( 1.000000000000000000, 0.9052476245296197099, 1.000000000000000000),
 ( 1.000000000000000000, 0.9409176603636237868, 1.000000000000000000),
 ( 1.000000000000000000, 0.9521522767065306869, 1.000000000000000000),
 ( 1.000000000000000000, 0.9681060328969361972, 1.000000000000000000),
 ( 1.000000000000000000, 0.9732806895434287231, 1.000000000000000000),
 ( 1.000000000000000000, 0.9832765258106581641, 1.000000000000000000),
 ( 1.000000000000000000, 0.9881226520953384496, 1.000000000000000000),
 ( 1.000000000000000000, 0.9925898118721221408, 1.000000000000000000) ) ) 
 REPRESENTATION_ITEM ( '' )  SURFACE ( )  );
#11077=CARTESIAN_POINT ( 'NONE',  ( 23.04481819307383716, -21.91824019632983678, -1.499999999999999556 ) ) ;
#11084=CARTESIAN_POINT ( 'NONE',  ( 107.9299262097015202, -17.06031696848630119, -2.839861482690292149 ) ) ;
#11090=CARTESIAN_POINT ( 'NONE',  ( -3.370691070153704949, -1.614088942876946264, 1.500000000000000000 ) ) ;
#11091=CARTESIAN_POINT ( 'NONE',  ( 2.535833972131079417, -0.1672301947041110182, 1.432210082195920720 ) ) ;
#11093=DIRECTION ( 'NONE',  ( 1.000000000000000000, -6.938893903907222067E-15, 0.000000000000000000 ) ) ;
#11100=CARTESIAN_POINT ( 'NONE',  ( 25.56776753627341137, -17.11417227705152655, 1.000000000000000000 ) ) ;
#11106=CARTESIAN_POINT ( 'NONE',  ( 24.36752972617610524, -17.44836528598952796, -1.442218785864573416 ) ) ;
#11110=B_SPLINE_CURVE_WITH_KNOTS ( 'NONE', 3,
 ( #6361, #22103, #21754, #11900, #8726, #19086, #31961, #13873, #26463, #16745, #24574, #14218 ),
 .UNSPECIFIED., .F., .F.,
 ( 4, 2, 2, 2, 2, 4 ),
 ( 4.661736504953698139E-16, 0.001666179614552203668, 0.002499269421828077386, 0.002915814325466020100, 0.003124086777284991890, 0.003332359229103963247 ),
 .UNSPECIFIED. ) ;
#11120=CARTESIAN_POINT ( 'NONE',  ( 108.0585218215646677, -18.91206178857411402, 4.613303170613168191 ) ) ;
#11122=CARTESIAN_POINT ( 'NONE',  ( 41.92799935455844462, -21.01937708447562159, -4.522129901861164925 ) ) ;
#11131=CARTESIAN_POINT ( 'NONE',  ( -32.85000000000000142, -10.96966150227469328, -1.499999999999999556 ) ) ;
#11136=DIRECTION ( 'NONE',  ( 1.000000000000000000, 0.000000000000000000, 0.000000000000000000 ) ) ;
#11142=CARTESIAN_POINT ( 'NONE',  ( 1.058168406056548605, -9.473510274387203722, 1.499999999999999778 ) ) ;
#11147=CARTESIAN_POINT ( 'NONE',  ( 24.34295195635817777, -17.38504247893911270, -1.375705049358364684 ) ) ;
#11149=FACE_OUTER_BOUND ( 'NONE', #24082, .T. ) ;
#11150=CARTESIAN_POINT ( 'NONE',  ( -31.18783180709124636, -21.43932300455417916, 1.500000000000000000 ) ) ;
#11164=CARTESIAN_POINT ( 'NONE',  ( 13.65718777917708415, -19.09288791508985028, 4.522129901861159595 ) ) ;
#11166=CARTESIAN_POINT ( 'NONE',  ( 25.43628654896618357, -17.54453578616538323, 1.025168090788791009 ) ) ;
#11181=CARTESIAN_POINT ( 'NONE',  ( 13.72001175370881221, -13.92748696968235578, -1.000000000000000000 ) ) ;
#11186=ORIENTED_EDGE ( 'NONE', *, *, #31875, .T. ) ;
#11187=EDGE_LOOP ( 'NONE', ( #3093, #6461, #17062 ) ) ;
#11188=DIRECTION ( 'NONE',  ( 0.000000000000000000, 0.000000000000000000, -1.000000000000000000 ) ) ;
#11190=CARTESIAN_POINT ( 'NONE',  ( 13.10266514559113205, -14.23637329403208263, 1.500000000000000000 ) ) ;
#11191=CARTESIAN_POINT ( 'NONE',  ( 1.997925886398103978, -1.624855788928872391, -1.500000000000000000 ) ) ;
#11233=CARTESIAN_POINT ( 'NONE',  ( -18.35000000000000142, -10.96966150227469505, 4.000000000000000000 ) ) ;
#11242=CARTESIAN_POINT ( 'NONE',  ( 7.650166299106958334, -9.403575859901817324, -1.000000000000000000 ) ) ;
#11243=CARTESIAN_POINT ( 'NONE',  ( 107.9811197705840016, -17.79749150983783323, -4.359573227107783389 ) ) ;
#11258=VECTOR ( 'NONE', #26410, 1000.000000000000000 ) ;
#11275=DIRECTION ( 'NONE',  ( 0.000000000000000000, -1.000000000000000000, 0.000000000000000000 ) ) ;
#11279=CARTESIAN_POINT ( 'NONE',  ( 107.5617723795404999, -18.98359893170737323, 4.522129901861158707 ) ) ;
#11282=ORIENTED_EDGE ( 'NONE', *, *, #18151, .F. ) ;
#11296=FACE_OUTER_BOUND ( 'NONE', #7465, .T. ) ;
#11298=CIRCLE ( 'NONE', #20894, 0.5000000000000004441 ) ;
#11310=CARTESIAN_POINT ( 'NONE',  ( 7.461135470892689803, -4.560857689779278523, 1.000000000000000000 ) ) ;
#11313=CIRCLE ( 'NONE', #1729, 0.4500000000000012879 ) ;
#11314=ORIENTED_EDGE ( 'NONE', *, *, #32445, .F. ) ;
#11315=CARTESIAN_POINT ( 'NONE',  ( 0.6388753366353405738, -7.663106119046291020, 1.499999999999999556 ) ) ;
#11335=CARTESIAN_POINT ( 'NONE',  ( -31.57659242536668742, -27.93932300454937590, -0.9999999999999981126 ) ) ;
#11337=VECTOR ( 'NONE', #5109, 999.9999999999998863 ) ;
#11339=CARTESIAN_POINT ( 'NONE',  ( -31.68476024375366862, -21.93625144121646642, 1.063946347602459319 ) ) ;
#11343=FACE_OUTER_BOUND ( 'NONE', #6323, .T. ) ;
#11350=CARTESIAN_POINT ( 'NONE',  ( 24.80306213860490061, -17.49230408913781787, -1.500000000000000000 ) ) ;
#11382=CARTESIAN_POINT ( 'NONE',  ( 11.72329880919066980, -20.06223657121697812, 1.500000000001569189 ) ) ;
#11383=CARTESIAN_POINT ( 'NONE',  ( 108.0981717737601997, -19.48301123670199075, -2.289311975395072363 ) ) ;
#11393=CARTESIAN_POINT ( 'NONE',  ( -4.179222253013961996, -3.233748670362141198, -1.499999999999999112 ) ) ;
#11401=EDGE_CURVE ( 'NONE', #17041, #31833, #4977, .T. ) ;
#11406=EDGE_LOOP ( 'NONE', ( #29705, #15226, #771, #28787 ) ) ;
#11419=ORIENTED_EDGE ( 'NONE', *, *, #27712, .F. ) ;
#11421=CARTESIAN_POINT ( 'NONE',  ( -3.657526656857886582, -9.739650026832221030, -1.743552401303936517 ) ) ;
#11422=CARTESIAN_POINT ( 'NONE',  ( 108.0688902883350693, -19.06136513089643714, -3.153541353326339891 ) ) ;
#11424=CARTESIAN_POINT ( 'NONE',  ( 7.168700581567057029, -6.410142746916854151, -1.500000000000142553 ) ) ;
#11427=EDGE_CURVE ( 'NONE', #21433, #12973, #32739, .T. ) ;
#11430=CARTESIAN_POINT ( 'NONE',  ( -3.616018626656801960, -10.49347358198851943, 1.500000000000000000 ) ) ;
#11437=ORIENTED_EDGE ( 'NONE', *, *, #26525, .T. ) ;
#11440=DIRECTION ( 'NONE',  ( -0.000000000000000000, 0.000000000000000000, 1.000000000000000000 ) ) ;
#11447=CARTESIAN_POINT ( 'NONE',  ( 25.33940588721724296, -17.54454932707515979, -1.176512215459074806 ) ) ;
#11449=VERTEX_POINT ( 'NONE', #12643 ) ;
#11462=CARTESIAN_POINT ( 'NONE',  ( 107.5625314920286399, -18.99452983251758553, 4.492264565199928228 ) ) ;
#11463=ADVANCED_FACE ( 'NONE', ( #22847 ), #6957, .T. ) ;
#11464=CARTESIAN_POINT ( 'NONE',  ( -0.5616989984784648282, -12.44624546261723985, -4.522129901861166701 ) ) ;
#11466=CARTESIAN_POINT ( 'NONE',  ( -31.35000000000000142, -10.96966150227469328, 4.000000000000000000 ) ) ;
#11467=DIRECTION ( 'NONE',  ( 1.000000000000000000, 0.000000000000000000, 0.000000000000000000 ) ) ;
#11479=CARTESIAN_POINT ( 'NONE',  ( -31.10918640827616244, -25.93932300454937945, 1.404595502311727362 ) ) ;
#11480=CARTESIAN_POINT ( 'NONE',  ( 6.800570610007250494, -8.349954097221042204, 1.500000000000000000 ) ) ;
#11484=CARTESIAN_POINT ( 'NONE',  ( 2.325079879153031825, -10.58907985611580216, 1.500000000000000444 ) ) ;
#11490=CARTESIAN_POINT ( 'NONE',  ( 23.72853298629051366, -17.37454644214605537, -1.486007232662901023 ) ) ;
#11493=CARTESIAN_POINT ( 'NONE',  ( 23.22234552117474848, -21.93639154742791675, -1.104776480646283643 ) ) ;
#11503=CARTESIAN_POINT ( 'NONE',  ( 107.6937183830913654, -18.97455548421143590, 4.522180808795155826 ) ) ;
#11506=CARTESIAN_POINT ( 'NONE',  ( 13.24595149388699511, -17.70232641593399947, 5.485967528433933538 ) ) ;
#11519=LINE ( 'NONE', #6982, #30582 ) ;
#11532=( BOUNDED_CURVE ( )  B_SPLINE_CURVE ( 3, ( #839, #15713, #6164, #23384 ),
 .UNSPECIFIED., .F., .F. ) 
 B_SPLINE_CURVE_WITH_KNOTS ( ( 4, 4 ),
 ( 1.570796326794896558, 3.141592653589793116 ),
 .UNSPECIFIED. ) 
 CURVE ( )  GEOMETRIC_REPRESENTATION_ITEM ( )  RATIONAL_B_SPLINE_CURVE ( ( 1.000000000000000000, 0.8047378541243649375, 0.8047378541243649375, 1.000000000000000000 ) ) 
 REPRESENTATION_ITEM ( '' )  );
#11544=EDGE_CURVE ( 'NONE', #4684, #11582, #19388, .T. ) ;
#11545=CARTESIAN_POINT ( 'NONE',  ( 24.80306213860341558, -17.49230408913766865, 1.499999999999999778 ) ) ;
#11561=DIRECTION ( 'NONE',  ( -0.000000000000000000, 0.000000000000000000, 1.000000000000000000 ) ) ;
#11564=ORIENTED_EDGE ( 'NONE', *, *, #29337, .T. ) ;
#11565=DIRECTION ( 'NONE',  ( -0.000000000000000000, 1.000000000000000000, 0.000000000000000000 ) ) ;
#11566=CARTESIAN_POINT ( 'NONE',  ( -4.075703125331459731, -9.746317125368902268, -1.500000000000000222 ) ) ;
#11567=VERTEX_POINT ( 'NONE', #5785 ) ;
#11571=CARTESIAN_POINT ( 'NONE',  ( 6.879500825888936077, -8.675028761530066745, -1.500000000000000000 ) ) ;
#11572=CARTESIAN_POINT ( 'NONE',  ( 108.0572303891428589, -18.89346548315845098, -4.650729098309561493 ) ) ;
#11575=EDGE_CURVE ( 'NONE', #9413, #993, #3387, .T. ) ;
#11582=VERTEX_POINT ( 'NONE', #23195 ) ;
#11583=CARTESIAN_POINT ( 'NONE',  ( -17.45597128428592981, -27.93932300454937590, 11.50000000000000000 ) ) ;
#11593=CARTESIAN_POINT ( 'NONE',  ( 3.744708216408842549, 0.000000000000000000, 1.000000000000000000 ) ) ;
#11604=CARTESIAN_POINT ( 'NONE',  ( -1.694237876703138967, -1.500727999663424184, 4.522129901861158707 ) ) ;
#11613=CARTESIAN_POINT ( 'NONE',  ( 108.0284409662735641, -18.47890495573541969, 4.354626199043353019 ) ) ;
#11629=CARTESIAN_POINT ( 'NONE',  ( 9.134478070377040737, -0.4075412271181343971, 1.000000000000000000 ) ) ;
#11631=CARTESIAN_POINT ( 'NONE',  ( 8.037025183208234225, -10.89872694351413784, -1.499999999999999778 ) ) ;
#11634=CARTESIAN_POINT ( 'NONE',  ( 3.866684586168369187, -11.79807535627656279, 1.500000000000000000 ) ) ;
#11644=CARTESIAN_POINT ( 'NONE',  ( -17.34999999999999787, -10.96966150227469505, -1.500000000000000000 ) ) ;
#11646=CARTESIAN_POINT ( 'NONE',  ( 23.27353278736381981, -21.94187821002792660, -1.000000000000000000 ) ) ;
#11648=DIRECTION ( 'NONE',  ( -1.000000000000000000, 0.000000000000000000, 0.000000000000000000 ) ) ;
#11650=DIRECTION ( 'NONE',  ( -0.000000000000000000, -0.000000000000000000, -1.000000000000000000 ) ) ;
#11652=CARTESIAN_POINT ( 'NONE',  ( -0.9232102171129827894, 0.000000000000000000, -4.522129901861166701 ) ) ;
#11676=ORIENTED_EDGE ( 'NONE', *, *, #9356, .T. ) ;
#11684=CARTESIAN_POINT ( 'NONE',  ( 3.640821217203817461, -12.13691508638171435, -1.758209645160216938 ) ) ;
#11699=CARTESIAN_POINT ( 'NONE',  ( -4.224514321812577577, -5.429116791541773956, -1.500000000000080602 ) ) ;
#11710=CARTESIAN_POINT ( 'NONE',  ( 0.000000000000000000, 0.000000000000000000, -1.000000000000000000 ) ) ;
#11714=CARTESIAN_POINT ( 'NONE',  ( 17.99869063401903446, -21.49583829453732875, 1.499999999999999556 ) ) ;
#11716=FACE_OUTER_BOUND ( 'NONE', #23661, .T. ) ;
#11729=CARTESIAN_POINT ( 'NONE',  ( 7.289999264625085296, -8.244573099997934307, -1.000000000000000000 ) ) ;
#11730=CARTESIAN_POINT ( 'NONE',  ( 108.0183420873304101, -18.33348361123931625, -4.566453197885271820 ) ) ;
#11733=AXIS2_PLACEMENT_3D ( 'NONE', #15764, #18441, #10911 ) ;
#11743=DIRECTION ( 'NONE',  ( 1.000000000000000000, 0.000000000000000000, 0.000000000000000000 ) ) ;
#11750=CARTESIAN_POINT ( 'NONE',  ( 7.452628691521980819, -4.595576623638184977, 1.000000000000000222 ) ) ;
#11765=DIRECTION ( 'NONE',  ( 0.1908089953765452762, -4.720536385445197917E-14, 0.9816271834476639757 ) ) ;
#11773=CARTESIAN_POINT ( 'NONE',  ( -1.824298235657398903, -2.866444442093540879, -5.485967528433938867 ) ) ;
#11780=CARTESIAN_POINT ( 'NONE',  ( 0.000000000000000000, 0.000000000000000000, 11.50000000000000000 ) ) ;
#11792=CARTESIAN_POINT ( 'NONE',  ( 7.192400642327566374, -7.644771086454712261, 1.500000000000285549 ) ) ;
#11797=CARTESIAN_POINT ( 'NONE',  ( 0.2521140843041953516, -7.034306361774945948, 1.499999999999964473 ) ) ;
#11803=CARTESIAN_POINT ( 'NONE',  ( 3.326350470277788407, -17.46743482665522151, 1.499999999999998446 ) ) ;
#11804=EDGE_CURVE ( 'NONE', #3232, #19511, #21014, .T. ) ;
#11810=CARTESIAN_POINT ( 'NONE',  ( 24.31705961742920863, -17.33693665021395347, -1.331050360515587005 ) ) ;
#11821=CARTESIAN_POINT ( 'NONE',  ( 0.3285611067768016147, -13.34342412962908320, -4.522129901861166701 ) ) ;
#11835=CARTESIAN_POINT ( 'NONE',  ( 25.29647035826949875, -17.54044501667244305, -1.294083318812917494 ) ) ;
#11838=CARTESIAN_POINT ( 'NONE',  ( -17.45597128428593336, -27.93932300454937590, 11.00000000000000000 ) ) ;
#11842=CARTESIAN_POINT ( 'NONE',  ( -31.43793636962776006, -25.49623161314221065, 1.500000000000015765 ) ) ;
#11856=VERTEX_POINT ( 'NONE', #4445 ) ;
#11863=CARTESIAN_POINT ( 'NONE',  ( 8.397335469007884967, -14.43511845646028391, -1.755102877586449450 ) ) ;
#11868=CARTESIAN_POINT ( 'NONE',  ( 25.56776753627337229, -17.11417227705151234, 1.000000000000000000 ) ) ;
#11869=CARTESIAN_POINT ( 'NONE',  ( -50.59999999999987352, -21.43932300454937945, 1.500000000000000000 ) ) ;
#11874=VERTEX_POINT ( 'NONE', #19994 ) ;
#11875=AXIS2_PLACEMENT_3D ( 'NONE', #31648, #24272, #9033 ) ;
#11886=TOROIDAL_SURFACE ( 'NONE', #6014, 10.46966150227468795, 0.5000000000000000000 ) ;
#11900=CARTESIAN_POINT ( 'NONE',  ( 22.99325939039831823, -17.14855239172962698, 1.466877076793034140 ) ) ;
#11903=DIRECTION ( 'NONE',  ( 0.1908089953765453595, -0.000000000000000000, 0.9816271834476638647 ) ) ;
#11912=CARTESIAN_POINT ( 'NONE',  ( -3.727414643486526291, -1.844583555841048828, -1.500000000000000222 ) ) ;
#11918=AXIS2_PLACEMENT_3D ( 'NONE', #9324, #29735, #6813 ) ;
#11919=CARTESIAN_POINT ( 'NONE',  ( 11.50505501463289626, -13.50304080202293555, -1.500000000000000000 ) ) ;
#11920=CARTESIAN_POINT ( 'NONE',  ( 107.4506475752643553, -17.36872507146703626, -4.544694954819969546 ) ) ;
#11929=CARTESIAN_POINT ( 'NONE',  ( 24.80306213860490061, -17.49230408913781787, -1.500000000000000000 ) ) ;
#11931=ORIENTED_EDGE ( 'NONE', *, *, #12794, .F. ) ;
#11937=ADVANCED_FACE ( 'NONE', ( #4756 ), #28356, .T. ) ;
#11941=AXIS2_PLACEMENT_3D ( 'NONE', #11479, #21673, #20775 ) ;
#11945=AXIS2_PLACEMENT_3D ( 'NONE', #17628, #11979, #4951 ) ;
#11948=CARTESIAN_POINT ( 'NONE',  ( -2.972652642344170371, -0.1886749676218029415, 1.397177942464156608 ) ) ;
#11950=EDGE_LOOP ( 'NONE', ( #4562, #1046, #31431, #5687 ) ) ;
#11955=CARTESIAN_POINT ( 'NONE',  ( 108.1300413742128228, -19.94772548867836193, -1.389623142575152848 ) ) ;
#11956=CARTESIAN_POINT ( 'NONE',  ( -4.317168503051449946, -7.715934794172482292, -1.500000000000000000 ) ) ;
#11957=DIRECTION ( 'NONE',  ( 1.000000000000000000, 0.000000000000000000, 0.000000000000000000 ) ) ;
#11965=CARTESIAN_POINT ( 'NONE',  ( -2.386718424894326063, -9.330009425477191698, -4.522129901861166701 ) ) ;
#11971=LINE ( 'NONE', #19324, #32164 ) ;
#11979=DIRECTION ( 'NONE',  ( -0.000000000000000000, 0.000000000000000000, 1.000000000000000000 ) ) ;
#11988=CARTESIAN_POINT ( 'NONE',  ( -4.547415420290301213, -6.122835645405422689, 1.499999999999999778 ) ) ;
#11991=CARTESIAN_POINT ( 'NONE',  ( -3.135269660805078740, -0.5000000000000000000, -1.500000000000000000 ) ) ;
#11992=ORIENTED_EDGE ( 'NONE', *, *, #22437, .F. ) ;
#11998=ORIENTED_EDGE ( 'NONE', *, *, #2496, .F. ) ;
#12008=CARTESIAN_POINT ( 'NONE',  ( 25.36146786571785583, -17.53026108976559527, -1.090855922821712731 ) ) ;
#12012=EDGE_CURVE ( 'NONE', #12213, #5578, #4892, .T. ) ;
#12021=ORIENTED_EDGE ( 'NONE', *, *, #21682, .T. ) ;
#12027=CARTESIAN_POINT ( 'NONE',  ( 107.4500593345382811, -17.36019228850094720, 4.522129901861156931 ) ) ;
#12035=CARTESIAN_POINT ( 'NONE',  ( 0.6082178693771017608, -7.500533726306640503, -1.499999999999999556 ) ) ;
#12041=CARTESIAN_POINT ( 'NONE',  ( 108.0597073579235570, -18.92913321739595744, -4.563813387244610276 ) ) ;
#12042=ORIENTED_EDGE ( 'NONE', *, *, #5574, .T. ) ;
#12051=CARTESIAN_POINT ( 'NONE',  ( 3.503099671769901224, -17.24542532612569445, -1.499999999999682920 ) ) ;
#12055=EDGE_LOOP ( 'NONE', ( #28678, #2556, #3942, #26905, #25896 ) ) ;
#12058=ORIENTED_EDGE ( 'NONE', *, *, #14434, .T. ) ;
#12065=CARTESIAN_POINT ( 'NONE',  ( 20.66542725970865746, -21.74162791314449805, 1.399019267719741499 ) ) ;
#12073=CARTESIAN_POINT ( 'NONE',  ( 107.4196074183075638, -16.92202192504116809, 3.623753903136544885 ) ) ;
#12077=CARTESIAN_POINT ( 'NONE',  ( -3.789033621533670182, -3.338956497497331366, 1.747105405493127428 ) ) ;
#12079=CARTESIAN_POINT ( 'NONE',  ( 107.9822453661852393, -17.81369980648333851, -4.398297061781460293 ) ) ;
#12088=ORIENTED_EDGE ( 'NONE', *, *, #3496, .T. ) ;
#12094=CARTESIAN_POINT ( 'NONE',  ( 40.91321928711694511, -19.30714377375492674, -0.9788672205888330202 ) ) ;
#12095=ORIENTED_EDGE ( 'NONE', *, *, #11023, .F. ) ;
#12114=CARTESIAN_POINT ( 'NONE',  ( 107.6648144168582775, -20.46701934092494568, 1.481717219550688913 ) ) ;
#12117=CARTESIAN_POINT ( 'NONE',  ( 42.67399297346870668, -22.27808837056542046, -5.485967528433938867 ) ) ;
#12119=CARTESIAN_POINT ( 'NONE',  ( 25.41068576271580781, -17.53965252855324053, 1.057866664602795437 ) ) ;
#12120=CARTESIAN_POINT ( 'NONE',  ( 17.84081991000783418, -19.48375781953046371, 5.485967528433935314 ) ) ;
#12137=CARTESIAN_POINT ( 'NONE',  ( 9.295344188488364523, -0.03282880342717523631, -1.183647805826461674 ) ) ;
#12140=CARTESIAN_POINT ( 'NONE',  ( -50.60000000000000142, -10.96966150227468972, 0.9999999999999991118 ) ) ;
#12142=( BOUNDED_SURFACE ( )  B_SPLINE_SURFACE ( 3, 2, ( 
 ( #11646, #14304, #4485 ),
 ( #22193, #16485, #24684 ),
 ( #10085, #1812, #6799 ),
 ( #16986, #27186, #24502 ),
 ( #1624, #9463, #22021 ),
 ( #19679, #6956, #14659 ),
 ( #24855, #2437, #30508 ),
 ( #8964, #32054, #19355 ),
 ( #2589, #28152, #21135 ),
 ( #28308, #15926, #13406 ),
 ( #28002, #18112, #30999 ),
 ( #8266, #28652, #5602 ) ),
 .UNSPECIFIED., .F., .F., .F. ) 
 B_SPLINE_SURFACE_WITH_KNOTS ( ( 4, 2, 2, 2, 2, 4 ),
 ( 3, 3 ),
 ( 0.01237460209466449690, 0.01250742172631360075, 0.01264024135796270286, 0.01290588062126090882, 0.01343715914785732247, 0.01449971620105014805 ),
 ( 0.000000000000000000, 1.000000000000000000 ),
 .UNSPECIFIED. ) 
 GEOMETRIC_REPRESENTATION_ITEM ( )  RATIONAL_B_SPLINE_SURFACE ( (
 ( 1.000000000000000000, 0.9985794324048127280, 1.000000000000000000),
 ( 1.000000000000000000, 0.9985649967291553297, 1.000000000000000000),
 ( 1.000000000000000000, 0.9977546568864327226, 1.000000000000000000),
 ( 1.000000000000000000, 0.9959318651690590718, 1.000000000000000000),
 ( 1.000000000000000000, 0.9948682866525003776, 1.000000000000000000),
 ( 1.000000000000000000, 0.9916149370760384274, 1.000000000000000000),
 ( 1.000000000000000000, 0.9892930324833787425, 1.000000000000000000),
 ( 1.000000000000000000, 0.9821212088646953386, 1.000000000000000000),
 ( 1.000000000000000000, 0.9771237707448936494, 1.000000000000000000),
 ( 1.000000000000000000, 0.9616790524996320366, 1.000000000000000000),
 ( 1.000000000000000000, 0.9507373671942048743, 1.000000000000000000),
 ( 1.000000000000000000, 0.9391581256477382622, 1.000000000000000000) ) ) 
 REPRESENTATION_ITEM ( '' )  SURFACE ( )  );
#12145=CARTESIAN_POINT ( 'NONE',  ( 21.47444597020330193, -21.75444421693962482, -1.464466272521893098 ) ) ;
#12151=CARTESIAN_POINT ( 'NONE',  ( -50.60000000000000142, 0.000000000000000000, 1.500000000000000000 ) ) ;
#12157=DIRECTION ( 'NONE',  ( 2.473959037481237219E-13, 1.000000000000000000, -0.000000000000000000 ) ) ;
#12168=CARTESIAN_POINT ( 'NONE',  ( 21.40255435829265451, -21.75563089608565903, 1.444450440414875692 ) ) ;
#12174=CARTESIAN_POINT ( 'NONE',  ( -23.35000000000000142, -10.96966150227469505, 4.500000000000000888 ) ) ;
#12181=CARTESIAN_POINT ( 'NONE',  ( 4.832428952779699749, -12.72822366752450307, -1.499999999999158451 ) ) ;
#12185=CARTESIAN_POINT ( 'NONE',  ( -29.85000000000000497, -10.96966150227469505, -11.00000000000000000 ) ) ;
#12197=CARTESIAN_POINT ( 'NONE',  ( 5.539315478094516187, -17.99457612246279936, -1.748481423779015609 ) ) ;
#12204=VERTEX_POINT ( 'NONE', #907 ) ;
#12213=VERTEX_POINT ( 'NONE', #30309 ) ;
#12223=CARTESIAN_POINT ( 'NONE',  ( -3.349881330687049630, -1.984754805279889345, 1.747784029808686412 ) ) ;
#12224=CARTESIAN_POINT ( 'NONE',  ( 9.134478070376893299, -0.4075412271184362112, -1.000000000000000000 ) ) ;
#12225=CARTESIAN_POINT ( 'NONE',  ( 107.9868730121348506, -17.88033675694570945, -4.506462841229693872 ) ) ;
#12231=ADVANCED_FACE ( 'NONE', ( #27468 ), #25863, .T. ) ;
#12233=CARTESIAN_POINT ( 'NONE',  ( -2.715612589025698131, -0.5453662152015711362, -1.748464016170166113 ) ) ;
#12239=B_SPLINE_CURVE_WITH_KNOTS ( 'NONE', 3,
 ( #19008, #16465, #29194, #28558, #13643, #23694 ),
 .UNSPECIFIED., .F., .F.,
 ( 4, 2, 4 ),
 ( 4.171616645832102339E-14, 0.0003905687335822774888, 0.0007811374671228388895 ),
 .UNSPECIFIED. ) ;
#12242=CARTESIAN_POINT ( 'NONE',  ( 2.632061376486627413, -0.5000000000000007772, -1.500000000000000444 ) ) ;
#12243=ORIENTED_EDGE ( 'NONE', *, *, #31252, .F. ) ;
#12255=ORIENTED_EDGE ( 'NONE', *, *, #2443, .T. ) ;
#12268=CARTESIAN_POINT ( 'NONE',  ( 25.33940588721780784, -17.54454932707527348, 1.176512215458641819 ) ) ;
#12279=VECTOR ( 'NONE', #3992, 1000.000000000000000 ) ;
#12281=CARTESIAN_POINT ( 'NONE',  ( 23.20536262852492726, -21.93817978746277220, -1.034581372269383293 ) ) ;
#12285=SHAPE_REPRESENTATION_RELATIONSHIP ( 'NONE' , 'NONE' ,  #5606, #18723 ) ;
#12293=CARTESIAN_POINT ( 'NONE',  ( 0.2308133903883674287, -15.52418313443756048, 1.500000000000000666 ) ) ;
#12299=ORIENTED_EDGE ( 'NONE', *, *, #7742, .T. ) ;
#12300=CARTESIAN_POINT ( 'NONE',  ( 21.73787281414312034, -21.77158151251076035, -1.493747827548021156 ) ) ;
#12306=PLANE ( 'NONE',  #25663 ) ;
#12307=CARTESIAN_POINT ( 'NONE',  ( -2.786590204610737587, -5.640011313469492471, -4.522129901861166701 ) ) ;
#12314=CARTESIAN_POINT ( 'NONE',  ( 23.13226153066085899, -21.93404782914829809, 1.074068642720903632 ) ) ;
#12320=AXIS2_PLACEMENT_3D ( 'NONE', #24163, #26375, #21814 ) ;
#12323=CARTESIAN_POINT ( 'NONE',  ( 14.53002800497467462, -16.11929632631086307, 1.753673441884563200 ) ) ;
#12325=ORIENTED_EDGE ( 'NONE', *, *, #4495, .T. ) ;
#12328=EDGE_CURVE ( 'NONE', #17825, #9859, #15711, .T. ) ;
#12338=CARTESIAN_POINT ( 'NONE',  ( 107.4500446874327935, -17.36019328965565123, 4.522129901861156931 ) ) ;
#12345=CARTESIAN_POINT ( 'NONE',  ( 3.164041846090267285, -11.65249415702359137, -1.500000000000000000 ) ) ;
#12353=EDGE_LOOP ( 'NONE', ( #12747, #4431, #32290 ) ) ;
#12366=CARTESIAN_POINT ( 'NONE',  ( 6.212874240570648965, -18.25778580431405018, -1.748739671137289342 ) ) ;
#12371=CARTESIAN_POINT ( 'NONE',  ( 107.9151932992832315, -16.84816672447076513, 3.542199815866853729 ) ) ;
#12384=ORIENTED_EDGE ( 'NONE', *, *, #14349, .T. ) ;
#12391=ORIENTED_EDGE ( 'NONE', *, *, #21793, .T. ) ;
#12397=EDGE_LOOP ( 'NONE', ( #26357, #25927, #17885, #32233 ) ) ;
#12404=AXIS2_PLACEMENT_3D ( 'NONE', #1984, #22039, #4148 ) ;
#12408=DIRECTION ( 'NONE',  ( 1.224646799147353207E-16, 1.000000000000000000, 0.000000000000000000 ) ) ;
#12409=CARTESIAN_POINT ( 'NONE',  ( 20.99695690729575048, -21.77932090203125526, -1.367431712678143008 ) ) ;
#12419=FACE_OUTER_BOUND ( 'NONE', #24385, .T. ) ;
#12421=CARTESIAN_POINT ( 'NONE',  ( 3.329122376115283277, 0.6654791810437885591, -0.9318852528018959358 ) ) ;
#12423=CARTESIAN_POINT ( 'NONE',  ( 9.057441432442507434, -0.5488979288031592407, 0.9999999999999997780 ) ) ;
#12442=DIRECTION ( 'NONE',  ( -0.000000000000000000, 0.000000000000000000, 1.000000000000000000 ) ) ;
#12443=CARTESIAN_POINT ( 'NONE',  ( 3.529609406779910419, -12.17998485103522199, 1.500000000000000000 ) ) ;
#12444=VERTEX_POINT ( 'NONE', #28271 ) ;
#12445=DIRECTION ( 'NONE',  ( -1.224646799147353207E-16, 1.000000000000000000, 0.000000000000000000 ) ) ;
#12447=CARTESIAN_POINT ( 'NONE',  ( -50.60000000000000142, -10.96966150227468972, 7.074999999999997513 ) ) ;
#12448=CARTESIAN_POINT ( 'NONE',  ( -50.60000000000000142, -0.5000000000000000000, 1.500000000000000000 ) ) ;
#12450=CARTESIAN_POINT ( 'NONE',  ( 24.83519197235663256, -17.49564329958969111, 1.498842795365988412 ) ) ;
#12472=CARTESIAN_POINT ( 'NONE',  ( 108.0243507582653280, -18.42000697793362107, 4.471835319414810606 ) ) ;
#12476=CARTESIAN_POINT ( 'NONE',  ( -2.962992063741595405, -11.77309494928644185, -1.499999999999999556 ) ) ;
#12478=CARTESIAN_POINT ( 'NONE',  ( -2.596515638727389330, -12.68063260205361154, 1.500000000000000666 ) ) ;
#12489=CARTESIAN_POINT ( 'NONE',  ( 21.41614545859222929, -21.75488722177052026, -1.449289482123008899 ) ) ;
#12492=DIRECTION ( 'NONE',  ( 0.5075624751249186994, 0.8616149568369075862, -1.660737436530807968E-15 ) ) ;
#12503=CARTESIAN_POINT ( 'NONE',  ( 23.22050010673017084, -21.93619796768861008, 1.062839084287792391 ) ) ;
#12513=ORIENTED_EDGE ( 'NONE', *, *, #29243, .T. ) ;
#12514=CARTESIAN_POINT ( 'NONE',  ( 21.36526493837866170, -21.76156136282174813, 1.423309099665599264 ) ) ;
#12520=CARTESIAN_POINT ( 'NONE',  ( 107.4500520110599240, -17.36019279015700079, 4.522129904808851464 ) ) ;
#12527=CARTESIAN_POINT ( 'NONE',  ( 21.04767255914890356, -17.06392231637721579, -1.499999999999999778 ) ) ;
#12528=CARTESIAN_POINT ( 'NONE',  ( 1.386174007446661749, -9.662292653395716968, 0.9788672205888330202 ) ) ;
#12534=VERTEX_POINT ( 'NONE', #5716 ) ;
#12544=CARTESIAN_POINT ( 'NONE',  ( 0.2700844563487312389, -15.55376400399037351, -1.499999999999999556 ) ) ;
#12552=FACE_OUTER_BOUND ( 'NONE', #19978, .T. ) ;
#12560=CARTESIAN_POINT ( 'NONE',  ( 74.30107678963170770, -22.79527490385382649, -1.500000000000000000 ) ) ;
#12568=CARTESIAN_POINT ( 'NONE',  ( -4.174653281524877357, -9.415293141582383285, 1.500000000000000000 ) ) ;
#12572=CARTESIAN_POINT ( 'NONE',  ( 108.0286247234065655, -18.48155101273792411, -4.347446253313675513 ) ) ;
#12588=CARTESIAN_POINT ( 'NONE',  ( 16.80274661516410006, -16.53680364986711737, -1.500000000000000444 ) ) ;
#12590=CARTESIAN_POINT ( 'NONE',  ( 8.770003503075953333, -11.01188172931930254, 1.000000000000000666 ) ) ;
#12594=CARTESIAN_POINT ( 'NONE',  ( -2.910169157841151488, 0.01692106641068897091, 0.9265120394742449861 ) ) ;
#12596=VERTEX_POINT ( 'NONE', #5569 ) ;
#12602=CARTESIAN_POINT ( 'NONE',  ( 0.5309851148689820333, -4.399114163800174282, -1.500000000000000000 ) ) ;
#12612=CARTESIAN_POINT ( 'NONE',  ( 24.79284380061039883, -17.49144841392520888, 1.371632250994630153 ) ) ;
#12613=CARTESIAN_POINT ( 'NONE',  ( -4.575445569744995389, -7.851872718544268714, 0.9788672205877712029 ) ) ;
#12633=CARTESIAN_POINT ( 'NONE',  ( 2.453127662067800863, -16.55897530748908153, 1.747541902167318861 ) ) ;
#12637=ORIENTED_EDGE ( 'NONE', *, *, #8798, .F. ) ;
#12640=EDGE_CURVE ( 'NONE', #21250, #31676, #30677, .T. ) ;
#12641=CARTESIAN_POINT ( 'NONE',  ( -31.09064165252238965, -25.43932300454937945, 1.500000000000000000 ) ) ;
#12643=CARTESIAN_POINT ( 'NONE',  ( -29.35000000000000853, -10.96966150227469505, -11.00000000000000000 ) ) ;
#12650=CARTESIAN_POINT ( 'NONE',  ( -15.54421513559356782, -25.44239456788696785, 1.499999999999999556 ) ) ;
#12651=CARTESIAN_POINT ( 'NONE',  ( 24.13073845333403966, -17.43243825926018786, -1.517345177934828815 ) ) ;
#12652=FACE_OUTER_BOUND ( 'NONE', #2506, .T. ) ;
#12661=CARTESIAN_POINT ( 'NONE',  ( -29.73484230743789070, 0.000000000000000000, 11.09540449768827308 ) ) ;
#12688=ORIENTED_EDGE ( 'NONE', *, *, #4583, .F. ) ;
#12694=CARTESIAN_POINT ( 'NONE',  ( -1.112385557803971414, -13.84060711329839322, -1.744598689557885551 ) ) ;
#12712=CARTESIAN_POINT ( 'NONE',  ( 3.566513200368869096, -17.47573827932033197, -1.500000000000000000 ) ) ;
#12720=CARTESIAN_POINT ( 'NONE',  ( -4.037246935524632541, -8.274097571364565695, 1.744146417483311451 ) ) ;
#12721=CARTESIAN_POINT ( 'NONE',  ( 2.632061376486628301, -0.5000000000000000000, 1.500000000000000000 ) ) ;
#12722=CARTESIAN_POINT ( 'NONE',  ( 108.0283028386853061, -18.47691595282699240, -4.359892190393998668 ) ) ;
#12729=FACE_OUTER_BOUND ( 'NONE', #29284, .T. ) ;
#12731=LINE ( 'NONE', #32344, #32717 ) ;
#12732=DIRECTION ( 'NONE',  ( 1.000000000000000000, 0.000000000000000000, 0.000000000000000000 ) ) ;
#12734=ORIENTED_EDGE ( 'NONE', *, *, #27156, .T. ) ;
#12737=CARTESIAN_POINT ( 'NONE',  ( 0.2678094507063553675, -7.640026513854723866, -1.500000000000000444 ) ) ;
#12738=CARTESIAN_POINT ( 'NONE',  ( 10.22928983298388772, -12.18097484234047201, 1.000000000000000000 ) ) ;
#12747=ORIENTED_EDGE ( 'NONE', *, *, #14839, .T. ) ;
#12752=VERTEX_POINT ( 'NONE', #20188 ) ;
#12753=CARTESIAN_POINT ( 'NONE',  ( 10.67617967751839458, -15.18094839191508960, -1.754323820777800025 ) ) ;
#12758=CARTESIAN_POINT ( 'NONE',  ( 1.302051718648536305, -9.310916516917917107, 1.499999999999999334 ) ) ;
#12766=ORIENTED_EDGE ( 'NONE', *, *, #30380, .F. ) ;
#12770=CARTESIAN_POINT ( 'NONE',  ( 20.55936702064902377, -21.63501724500277135, -1.474765012619939863 ) ) ;
#12780=CARTESIAN_POINT ( 'NONE',  ( 6.353200070539462452, -18.33841314941795986, 1.748782779367867191 ) ) ;
#12794=EDGE_CURVE ( 'NONE', #8778, #26510, #32811, .T. ) ;
#12798=CARTESIAN_POINT ( 'NONE',  ( -50.60000000000000142, -21.93932300454937945, 1.000000000000000000 ) ) ;
#12799=DIRECTION ( 'NONE',  ( 0.000000000000000000, 0.000000000000000000, 1.000000000000000000 ) ) ;
#12800=CARTESIAN_POINT ( 'NONE',  ( -29.24402871571405882, -25.93932300454937945, 11.50000000000000000 ) ) ;
#12810=CARTESIAN_POINT ( 'NONE',  ( 2.838906197121284336, 0.000000000000000000, -1.380701634710809200 ) ) ;
#12811=CARTESIAN_POINT ( 'NONE',  ( 7.650166298461252623, -9.403575860120110264, 1.500000000000000000 ) ) ;
#12816=CARTESIAN_POINT ( 'NONE',  ( -55.09999999999999432, -10.96966150227468972, 7.500000000000000000 ) ) ;
#12819=ADVANCED_FACE ( 'NONE', ( #19858 ), #15319, .T. ) ;
#12831=CARTESIAN_POINT ( 'NONE',  ( 12.23116174109277310, -15.17372397490200875, -1.500000000000000000 ) ) ;
#12833=CARTESIAN_POINT ( 'NONE',  ( 108.6155529559672885, -15.79924867777639186, 1.500000000000000444 ) ) ;
#12836=DIRECTION ( 'NONE',  ( -1.000000000000000000, 0.000000000000000000, -0.000000000000000000 ) ) ;
#12855=CARTESIAN_POINT ( 'NONE',  ( 107.9808716746042592, -17.79391898944832207, 4.343976358958649975 ) ) ;
#12856=ORIENTED_EDGE ( 'NONE', *, *, #21047, .T. ) ;
#12870=CARTESIAN_POINT ( 'NONE',  ( -3.889464452585704723, -3.181828567483031112, 1.500000000000000000 ) ) ;
#12880=CARTESIAN_POINT ( 'NONE',  ( 107.6540478345876579, -20.31198981111268864, 1.799433580832300761 ) ) ;
#12882=CARTESIAN_POINT ( 'NONE',  ( -1.898205096934858283, -13.58783804611283408, 1.500000000000000000 ) ) ;
#12884=VECTOR ( 'NONE', #11565, 1000.000000000000000 ) ;
#12887=ORIENTED_EDGE ( 'NONE', *, *, #1304, .F. ) ;
#12890=CARTESIAN_POINT ( 'NONE',  ( -31.18783180709124636, -25.44850941282521006, 1.500000000000000000 ) ) ;
#12897=ORIENTED_EDGE ( 'NONE', *, *, #26113, .T. ) ;
#12898=CARTESIAN_POINT ( 'NONE',  ( 108.0223665316818114, -18.39143460874491964, 4.509626086723559801 ) ) ;
#12901=CARTESIAN_POINT ( 'NONE',  ( 107.4997235041507793, -18.08180639291762404, -5.137882848214009535 ) ) ;
#12923=CARTESIAN_POINT ( 'NONE',  ( -32.85000000000000142, -10.96966150227469328, -1.499999999999999556 ) ) ;
#12924=CARTESIAN_POINT ( 'NONE',  ( 108.6155529559672885, -15.79924867777639186, 1.500000000000000000 ) ) ;
#12927=VERTEX_POINT ( 'NONE', #23500 ) ;
#12928=CARTESIAN_POINT ( 'NONE',  ( 8.787183276125896114, -14.57090831734663006, -1.754908492369190887 ) ) ;
#12937=VECTOR ( 'NONE', #2630, 999.9999999999998863 ) ;
#12938=DIRECTION ( 'NONE',  ( -0.000000000000000000, -0.000000000000000000, 1.000000000000000000 ) ) ;
#12945=CARTESIAN_POINT ( 'NONE',  ( 43.74661801760413482, -24.08792321988613594, 1.500000000000000000 ) ) ;
#12970=CARTESIAN_POINT ( 'NONE',  ( -4.062270432330101322, -5.105425442540494352, 1.745843391288832258 ) ) ;
#12973=VERTEX_POINT ( 'NONE', #5790 ) ;
#12978=CARTESIAN_POINT ( 'NONE',  ( 108.0379352182121835, -18.61561982177950725, 4.067192897739825952 ) ) ;
#12985=LINE ( 'NONE', #10316, #563 ) ;
#12994=CARTESIAN_POINT ( 'NONE',  ( 24.45151689496773173, -17.43764607375594977, 1.460555297092053895 ) ) ;
#13004=CARTESIAN_POINT ( 'NONE',  ( 2.893040194807178001, -11.59888121906014113, 1.759635999373791782 ) ) ;
#13005=CARTESIAN_POINT ( 'NONE',  ( 24.38441422957166083, -17.22282062799744295, 1.000000000000000000 ) ) ;
#13015=CIRCLE ( 'NONE', #11945, 4.999999999999997335 ) ;
#13025=CARTESIAN_POINT ( 'NONE',  ( 15.99600675134221106, -15.99419002640760290, -1.499999999999999778 ) ) ;
#13033=ORIENTED_EDGE ( 'NONE', *, *, #32671, .T. ) ;
#13036=B_SPLINE_CURVE_WITH_KNOTS ( 'NONE', 3,
 ( #8392, #21118, #31316, #8541, #3222, #2928, #18588, #26291, #5729, #20941, #3402, #8248 ),
 .UNSPECIFIED., .F., .F.,
 ( 4, 2, 2, 2, 2, 4 ),
 ( 0.000000000000000000, 0.0002268479045755578691, 0.0004536958091511157382, 0.0005671197614388945102, 0.0006805437137266734989, 0.0009073916183022310428 ),
 .UNSPECIFIED. ) ;
#13038=CARTESIAN_POINT ( 'NONE',  ( 24.35832023931450507, -17.33818253687174860, -1.317734466820339900 ) ) ;
#13045=DIRECTION ( 'NONE',  ( -0.000000000000000000, 0.000000000000000000, 1.000000000000000000 ) ) ;
#13063=CARTESIAN_POINT ( 'NONE',  ( 9.836026323043101982, -12.51705112700722822, 1.500000000000000222 ) ) ;
#13066=ORIENTED_EDGE ( 'NONE', *, *, #23946, .F. ) ;
#13069=CARTESIAN_POINT ( 'NONE',  ( -2.574648304754633799, -12.71113778305264752, 1.500000000000000000 ) ) ;
#13071=EDGE_CURVE ( 'NONE', #7539, #15957, #1330, .T. ) ;
#13073=CARTESIAN_POINT ( 'NONE',  ( 108.0612411924935827, -18.95122005363461071, -4.517344619987845533 ) ) ;
#13082=CARTESIAN_POINT ( 'NONE',  ( -3.226940125355887812, -1.840961572248389633E-05, -0.9957093966831331855 ) ) ;
#13086=LINE ( 'NONE', #28471, #25254 ) ;
#13091=CARTESIAN_POINT ( 'NONE',  ( 0.5309851148689820333, -4.399114163800174282, -1.500000000000000444 ) ) ;
#13093=CARTESIAN_POINT ( 'NONE',  ( 108.0130871940577748, -18.25781445536221526, 5.137726603835512940 ) ) ;
#13097=CARTESIAN_POINT ( 'NONE',  ( 107.5121035333901460, -18.26190534946589139, 5.137878862399732682 ) ) ;
#13103=CARTESIAN_POINT ( 'NONE',  ( 0.1962428234089072521, -6.885380501030516243, 1.500000000000000000 ) ) ;
#13105=LINE ( 'NONE', #25596, #2828 ) ;
#13110=CARTESIAN_POINT ( 'NONE',  ( -50.60000000000000142, -0.5000000000000000000, 1.500000000000000000 ) ) ;
#13113=CARTESIAN_POINT ( 'NONE',  ( 1.998490341989216379, -1.623810759619012778, 1.499999999999999112 ) ) ;
#13115=CARTESIAN_POINT ( 'NONE',  ( 107.4500373638804120, -17.36019379023677089, -4.522129901861164036 ) ) ;
#13116=CARTESIAN_POINT ( 'NONE',  ( 3.673334745432188075, 0.0007210401945645747868, 1.066984883846252341 ) ) ;
#13129=CARTESIAN_POINT ( 'NONE',  ( -4.365512850963738423, -6.230587388684557304, -1.499999999999999556 ) ) ;
#13132=DIRECTION ( 'NONE',  ( 1.000000000000000000, -2.498001805406599692E-13, 0.000000000000000000 ) ) ;
#13140=ADVANCED_FACE ( 'NONE', ( #6425 ), #27155, .F. ) ;
#13145=FACE_OUTER_BOUND ( 'NONE', #31697, .T. ) ;
#13148=CARTESIAN_POINT ( 'NONE',  ( 23.09505357366878897, -21.93193652582860409, 1.086920924784747777 ) ) ;
#13158=CARTESIAN_POINT ( 'NONE',  ( 10.63777812034810566, -12.44241537516270490, 1.000000000000000000 ) ) ;
#13162=EDGE_LOOP ( 'NONE', ( #26009, #5816, #10532, #11931, #1937 ) ) ;
#13169=CARTESIAN_POINT ( 'NONE',  ( 42.35322304605574573, -22.56891886512037360, 4.522129901861158707 ) ) ;
#13176=ORIENTED_EDGE ( 'NONE', *, *, #19820, .T. ) ;
#13183=CARTESIAN_POINT ( 'NONE',  ( 108.1296380701673598, -19.93611807713457651, 1.386936492588066949 ) ) ;
#13185=FACE_OUTER_BOUND ( 'NONE', #22100, .T. ) ;
#13189=ORIENTED_EDGE ( 'NONE', *, *, #1663, .T. ) ;
#13196=LINE ( 'NONE', #31285, #5570 ) ;
#13203=CARTESIAN_POINT ( 'NONE',  ( -0.7739934281325309140, -8.972773999336983053, -4.522129901861164925 ) ) ;
#13212=EDGE_CURVE ( 'NONE', #11449, #30719, #1099, .T. ) ;
#13213=CARTESIAN_POINT ( 'NONE',  ( -4.224498304150544392, -5.428959277710454501, 1.500000000000239808 ) ) ;
#13215=CARTESIAN_POINT ( 'NONE',  ( 2.808958353948056264, -0.3589573147998340596, 1.483919649041820499 ) ) ;
#13219=B_SPLINE_CURVE_WITH_KNOTS ( 'NONE', 3,
 ( #1391, #18946, #13885, #11077, #29136, #29460 ),
 .UNSPECIFIED., .F., .F.,
 ( 4, 2, 4 ),
 ( 0.01682075285868000689, 0.5000000000000000000, 0.5131349204668804731 ),
 .UNSPECIFIED. ) ;
#13222=ADVANCED_FACE ( 'NONE', ( #11296 ), #6271, .T. ) ;
#13227=CARTESIAN_POINT ( 'NONE',  ( 107.9802527803230419, -17.78500706576073753, 4.325704939602341703 ) ) ;
#13234=CARTESIAN_POINT ( 'NONE',  ( 0.8407900506754626413, -11.56055812333295130, -4.522129901861164925 ) ) ;
#13236=CARTESIAN_POINT ( 'NONE',  ( 107.9811281649432289, -17.79761238652359978, 4.359937231691887405 ) ) ;
#13237=ADVANCED_FACE ( 'NONE', ( #30347 ), #30322, .F. ) ;
#13238=EDGE_LOOP ( 'NONE', ( #16469, #14259, #24681, #25429 ) ) ;
#13239=LINE ( 'NONE', #21428, #29403 ) ;
#13241=CARTESIAN_POINT ( 'NONE',  ( -3.105859910356985054, -0.009789559233381405975, 1.118159719381635497 ) ) ;
#13246=LINE ( 'NONE', #12923, #31074 ) ;
#13257=CARTESIAN_POINT ( 'NONE',  ( 3.326374039432143270, -11.41640325077553975, 1.499999999999999778 ) ) ;
#13262=DIRECTION ( 'NONE',  ( 0.000000000000000000, 0.000000000000000000, 1.000000000000000000 ) ) ;
#13288=ADVANCED_FACE ( 'NONE', ( #14780 ), #4605, .F. ) ;
#13292=CARTESIAN_POINT ( 'NONE',  ( 0.9232102171129937807, 0.000000000000000000, -4.522129901861164925 ) ) ;
#13298=CARTESIAN_POINT ( 'NONE',  ( 21.65220420020007097, -21.84595744892845559, 1.292937544721791898 ) ) ;
#13304=FACE_OUTER_BOUND ( 'NONE', #10334, .T. ) ;
#13306=CARTESIAN_POINT ( 'NONE',  ( 11.72844749915270413, -13.05523934215238313, 1.500000000000280220 ) ) ;
#13319=CARTESIAN_POINT ( 'NONE',  ( 9.295344188488364523, -0.03282880342717511835, 1.183647805826461674 ) ) ;
#13321=CARTESIAN_POINT ( 'NONE',  ( 0.4474568012433104425, -7.410208993127077370, 0.9788672205888330202 ) ) ;
#13334=EDGE_CURVE ( 'NONE', #9983, #27584, #31340, .T. ) ;
#13339=CARTESIAN_POINT ( 'NONE',  ( 2.808958353948056708, -0.3589573147998343372, -1.483919649041820721 ) ) ;
#13341=VERTEX_POINT ( 'NONE', #23633 ) ;
#13358=CARTESIAN_POINT ( 'NONE',  ( 7.565496255526879210, -10.23852490753181499, 1.500000000000000222 ) ) ;
#13360=CARTESIAN_POINT ( 'NONE',  ( -29.24402871571405882, -27.93932300454937590, 11.00000000000000000 ) ) ;
#13364=CARTESIAN_POINT ( 'NONE',  ( 6.212730774181275173, -18.25773092725300728, 1.748739615172814732 ) ) ;
#13365=CARTESIAN_POINT ( 'NONE',  ( 17.33093461831547444, -21.43932300456618378, -1.500000000000000000 ) ) ;
#13378=FACE_OUTER_BOUND ( 'NONE', #4509, .T. ) ;
#13386=CARTESIAN_POINT ( 'NONE',  ( 108.0347112123201612, -18.56919493900439377, 5.017201665671134236 ) ) ;
#13387=ORIENTED_EDGE ( 'NONE', *, *, #29412, .T. ) ;
#13389=VECTOR ( 'NONE', #23055, 1000.000000000000000 ) ;
#13393=CARTESIAN_POINT ( 'NONE',  ( 21.34939358370785101, -21.78237682584212465, -1.377397332511757444 ) ) ;
#13404=CARTESIAN_POINT ( 'NONE',  ( 10.46141283585619242, -19.61934161334578519, -1.750340053724213973 ) ) ;
#13406=CARTESIAN_POINT ( 'NONE',  ( 21.99035326630345466, -21.86692099231494879, -1.263015267642259243 ) ) ;
#13412=CARTESIAN_POINT ( 'NONE',  ( 0.5441968595407785658, -6.194664530687079562, 1.500000000000000666 ) ) ;
#13418=CARTESIAN_POINT ( 'NONE',  ( -4.365512850963738423, -6.230587388684557304, 1.500000000000000000 ) ) ;
#13423=DIRECTION ( 'NONE',  ( -0.1908089953765452762, 0.000000000000000000, -0.9816271834476639757 ) ) ;
#13431=CARTESIAN_POINT ( 'NONE',  ( 1.302476151998225973, -9.311590272907336541, -1.500000000000000222 ) ) ;
#13466=CARTESIAN_POINT ( 'NONE',  ( 22.46520412490106722, -21.85309540019774843, 1.407654271148356395 ) ) ;
#13468=CARTESIAN_POINT ( 'NONE',  ( 21.67755997557343406, -21.76174915994640102, 1.411535641067431124 ) ) ;
#13470=CIRCLE ( 'NONE', #12404, 7.144028715714068056 ) ;
#13474=ORIENTED_EDGE ( 'NONE', *, *, #22237, .T. ) ;
#13482=CARTESIAN_POINT ( 'NONE',  ( 9.851448551970788614, -11.91728849095426135, 1.499999999999785283 ) ) ;
#13483=AXIS2_PLACEMENT_3D ( 'NONE', #32715, #22829, #25501 ) ;
#13487=EDGE_CURVE ( 'NONE', #29313, #28440, #1404, .T. ) ;
#13498=PLANE ( 'NONE',  #17309 ) ;
#13510=VERTEX_POINT ( 'NONE', #6734 ) ;
#13513=CARTESIAN_POINT ( 'NONE',  ( 107.6648144168582348, -20.46701934092476449, -1.481717219551038411 ) ) ;
#13514=CARTESIAN_POINT ( 'NONE',  ( -1.671916146696592831, -10.12145986844939927, 5.485967528433935314 ) ) ;
#13524=CARTESIAN_POINT ( 'NONE',  ( -2.767073886773233848, -0.6621507858625358400, 1.748408842879327851 ) ) ;
#13532=CARTESIAN_POINT ( 'NONE',  ( -3.135269660805080516, -0.5000000000000000000, 1.500000000000000000 ) ) ;
#13535=ORIENTED_EDGE ( 'NONE', *, *, #5693, .T. ) ;
#13537=CARTESIAN_POINT ( 'NONE',  ( -15.26206363037219838, -21.68942756709465769, 1.499999999999998668 ) ) ;
#13540=CARTESIAN_POINT ( 'NONE',  ( 14.08105513877605652, -14.60666186089171603, 1.499999999999999556 ) ) ;
#13548=CARTESIAN_POINT ( 'NONE',  ( 15.97646010100271496, -20.81270992525872288, 1.751026346556933344 ) ) ;
#13551=CARTESIAN_POINT ( 'NONE',  ( 24.39659513448239991, -17.41072360183627055, 1.416990234759656575 ) ) ;
#13557=CARTESIAN_POINT ( 'NONE',  ( 25.52557118915448342, -17.56218954043521663, 1.078818518451832409 ) ) ;
#13559=DIRECTION ( 'NONE',  ( -0.1908089953765453595, -4.729706814396277527E-15, 0.9816271834476638647 ) ) ;
#13566=LINE ( 'NONE', #14059, #17815 ) ;
#13568=CARTESIAN_POINT ( 'NONE',  ( 107.4502445245915254, -17.36287206927810089, 4.529451243851331910 ) ) ;
#13571=ORIENTED_EDGE ( 'NONE', *, *, #3964, .F. ) ;
#13572=DIRECTION ( 'NONE',  ( -1.000000000000000000, 0.000000000000000000, 0.000000000000000000 ) ) ;
#13580=EDGE_CURVE ( 'NONE', #26388, #7529, #31489, .T. ) ;
#13581=CARTESIAN_POINT ( 'NONE',  ( -50.60000000000000142, -10.96966150227468972, 7.500000000000000000 ) ) ;
#13582=CARTESIAN_POINT ( 'NONE',  ( 0.000000000000000000, -0.5000000000000000000, -1.000000000000000000 ) ) ;
#13587=CARTESIAN_POINT ( 'NONE',  ( 19.32480846800323349, -16.28061487828787790, -1.500000000000000000 ) ) ;
#13588=CARTESIAN_POINT ( 'NONE',  ( 107.4498871846200814, -17.35770398095254663, -4.515330059624638182 ) ) ;
#13594=CARTESIAN_POINT ( 'NONE',  ( 13.65718777918027271, -19.09288791508984673, 4.522129901861158707 ) ) ;
#13595=CARTESIAN_POINT ( 'NONE',  ( 2.281627749324421917, -0.2935656086769610207, 1.757435426329174488 ) ) ;
#13598=CARTESIAN_POINT ( 'NONE',  ( 107.3983896896722570, -16.61650204647006390, -2.997325617849243784 ) ) ;
#13603=CARTESIAN_POINT ( 'NONE',  ( -23.35000000000000142, -10.96966150227469505, 4.000000000000000000 ) ) ;
#13605=CARTESIAN_POINT ( 'NONE',  ( 0.6160563202711623054, -5.544449031061736477, -1.499999999999999556 ) ) ;
#13618=ORIENTED_EDGE ( 'NONE', *, *, #29243, .F. ) ;
#13627=CARTESIAN_POINT ( 'NONE',  ( 108.0616230038786796, -18.95671804260016913, 4.502323035491692771 ) ) ;
#13643=CARTESIAN_POINT ( 'NONE',  ( 107.9719557256307354, -17.66553154178031093, 4.376786827539821623 ) ) ;
#13645=CARTESIAN_POINT ( 'NONE',  ( 9.283830569141708011, -0.1241467202049961749, 1.000000000000000000 ) ) ;
#13646=ORIENTED_EDGE ( 'NONE', *, *, #7148, .F. ) ;
#13649=CARTESIAN_POINT ( 'NONE',  ( 4.969883781861252459, -12.47903377700913907, 1.500000000000000000 ) ) ;
#13655=CARTESIAN_POINT ( 'NONE',  ( 23.86874014608191175, -17.38228585591196307, -1.471223822905572076 ) ) ;
#13670=CARTESIAN_POINT ( 'NONE',  ( 107.8192872773860245, -18.91580487786033515, 4.500888494199039691 ) ) ;
#13671=( BOUNDED_SURFACE ( )  B_SPLINE_SURFACE ( 3, 2, ( 
 ( #1420, #21792, #1076 ),
 ( #5923, #18804, #31506 ),
 ( #21160, #18629, #21477 ),
 ( #3601, #26813, #6406 ),
 ( #24453, #11447, #16115 ),
 ( #31999, #24135, #18977 ),
 ( #6251, #28825, #26500 ),
 ( #16604, #8591, #24308 ),
 ( #16437, #1263, #21641 ),
 ( #29010, #11106, #6108 ) ),
 .UNSPECIFIED., .F., .F., .F. ) 
 B_SPLINE_SURFACE_WITH_KNOTS ( ( 4, 2, 2, 2, 4 ),
 ( 3, 3 ),
 ( 0.01348603581696579921, 0.01365687529134765321, 0.01382771476572950548, 0.01416939371449321000, 0.01485275161202062079 ),
 ( 0.000000000000000000, 1.000000000000000000 ),
 .UNSPECIFIED. ) 
 GEOMETRIC_REPRESENTATION_ITEM ( )  RATIONAL_B_SPLINE_SURFACE ( (
 ( 1.000000000000000000, 0.9948736491435667961, 1.000000000000000000),
 ( 1.000000000000000000, 0.9948794564610742297, 1.000000000000000000),
 ( 1.000000000000000000, 0.9935082075948258318, 1.000000000000000000),
 ( 1.000000000000000000, 0.9898246045860391584, 1.000000000000000000),
 ( 1.000000000000000000, 0.9875779995959506063, 1.000000000000000000),
 ( 1.000000000000000000, 0.9804235948790372968, 1.000000000000000000),
 ( 1.000000000000000000, 0.9752522326728655377, 1.000000000000000000),
 ( 1.000000000000000000, 0.9593679678191086024, 1.000000000000000000),
 ( 1.000000000000000000, 0.9482314950096560890, 1.000000000000000000),
 ( 1.000000000000000000, 0.9372872368324044468, 1.000000000000000000) ) ) 
 REPRESENTATION_ITEM ( '' )  SURFACE ( )  );
#13675=DIRECTION ( 'NONE',  ( -0.000000000000000000, 0.000000000000000000, 1.000000000000000000 ) ) ;
#13676=CARTESIAN_POINT ( 'NONE',  ( -15.51216819290874227, -25.44850941282521006, 1.500000000000000000 ) ) ;
#13691=CARTESIAN_POINT ( 'NONE',  ( -2.681117189733320139, -7.739668020571214980E-17, -1.353799989032657303 ) ) ;
#13694=CARTESIAN_POINT ( 'NONE',  ( 6.220890055307039646, -15.20372210278347680, -4.522129901861164925 ) ) ;
#13698=CARTESIAN_POINT ( 'NONE',  ( 0.1307775883147231089, -6.173461807542353519, -1.772482830384789265 ) ) ;
#13706=CARTESIAN_POINT ( 'NONE',  ( 23.71271855738436329, -17.43088677775550011, 1.604577790254628100 ) ) ;
#13713=CARTESIAN_POINT ( 'NONE',  ( -3.349888966845140370, -1.984772134521467502, -1.747784021618837835 ) ) ;
#13724=CARTESIAN_POINT ( 'NONE',  ( 107.9478747612858882, -17.31877164626198251, 4.502019023796631103 ) ) ;
#13729=CARTESIAN_POINT ( 'NONE',  ( 24.35832023931602208, -17.33818253687209676, 1.317734466820223549 ) ) ;
#13730=ORIENTED_EDGE ( 'NONE', *, *, #7486, .T. ) ;
#13739=CARTESIAN_POINT ( 'NONE',  ( 13.44509804349893933, -13.81913516303328393, -1.000000000000000000 ) ) ;
#13740=CARTESIAN_POINT ( 'NONE',  ( 107.9809898003504003, -17.79561997080629254, -4.354661406389237044 ) ) ;
#13744=CARTESIAN_POINT ( 'NONE',  ( 3.238981242682539285, 0.6371288015966363183, 1.059614580210928025 ) ) ;
#13753=CARTESIAN_POINT ( 'NONE',  ( -15.02135460118491217, -25.93932300454937945, 1.095404497688272638 ) ) ;
#13754=CARTESIAN_POINT ( 'NONE',  ( 21.39621122230721539, -21.77804412735442696, -1.397661460514420195 ) ) ;
#13756=CARTESIAN_POINT ( 'NONE',  ( 14.72442999747527637, -15.74550703336688784, -1.499999999999999334 ) ) ;
#13768=CARTESIAN_POINT ( 'NONE',  ( 71.84273455769063332, -21.42499078636442178, 4.522129901861158707 ) ) ;
#13779=EDGE_CURVE ( 'NONE', #6331, #2424, #17394, .T. ) ;
#13782=CARTESIAN_POINT ( 'NONE',  ( 107.3476768466458253, -15.88628154573095586, -1.500000000000000000 ) ) ;
#13789=LINE ( 'NONE', #6139, #1252 ) ;
#13790=CARTESIAN_POINT ( 'NONE',  ( 6.666829201526833337, -7.372062170298320005, 1.500000000000000000 ) ) ;
#13794=CARTESIAN_POINT ( 'NONE',  ( 6.604407424131250259, -13.59569599788273031, 1.499999999999154898 ) ) ;
#13798=CARTESIAN_POINT ( 'NONE',  ( 21.08401840680132011, -16.78474387324121153, -1.499999999999999556 ) ) ;
#13800=B_SPLINE_CURVE_WITH_KNOTS ( 'NONE', 3,
 ( #4076, #31985, #14242, #22439, #29655, #9053, #17428, #6736, #16926, #11929 ),
 .UNSPECIFIED., .F., .F.,
 ( 4, 2, 2, 2, 4 ),
 ( 0.000000000000000000, 5.472672424563606967E-05, 0.0001094534484912721393, 0.0002189068969825542805, 0.0004378137939651184814 ),
 .UNSPECIFIED. ) ;
#13815=CARTESIAN_POINT ( 'NONE',  ( -2.786590204610741583, -5.640011313470056464, 4.522129901861159595 ) ) ;
#13828=FACE_OUTER_BOUND ( 'NONE', #13162, .T. ) ;
#13831=EDGE_LOOP ( 'NONE', ( #8004, #17535 ) ) ;
#13834=ADVANCED_FACE ( 'NONE', ( #29553 ), #31584, .F. ) ;
#13841=CARTESIAN_POINT ( 'NONE',  ( -1.170068671574743036, -6.059534462705075342, -4.522129901861164925 ) ) ;
#13844=CARTESIAN_POINT ( 'NONE',  ( 1.184589434306864364, -2.669489141080311434, -1.500000000000000222 ) ) ;
#13857=ADVANCED_FACE ( 'NONE', ( #29715 ), #22487, .F. ) ;
#13870=CARTESIAN_POINT ( 'NONE',  ( 17.33093461831347781, -21.43932300456618378, 1.499999999999999112 ) ) ;
#13873=CARTESIAN_POINT ( 'NONE',  ( 24.01922593961334940, -17.30645187339506563, 1.384626276794619137 ) ) ;
#13885=CARTESIAN_POINT ( 'NONE',  ( 43.06800534735074137, -24.01680020629799728, -1.499999999999999556 ) ) ;
#13890=CARTESIAN_POINT ( 'NONE',  ( 12.23764924856644143, -13.51220073293806223, -1.000000000000000000 ) ) ;
#13893=CARTESIAN_POINT ( 'NONE',  ( 8.789577373537829530, -11.69574158658589091, -1.500000000000000000 ) ) ;
#13894=CARTESIAN_POINT ( 'NONE',  ( 107.9755271014895754, -17.71695846615960335, -4.186189698420959004 ) ) ;
#13911=CARTESIAN_POINT ( 'NONE',  ( -15.35000000000000320, -10.96966150227469505, 4.500000000000000888 ) ) ;
#13924=CARTESIAN_POINT ( 'NONE',  ( 0.3285611067768013926, -13.34342412962908497, 4.522129901861158707 ) ) ;
#13925=DIRECTION ( 'NONE',  ( 1.000000000000000000, -2.473959037481237219E-13, 0.000000000000000000 ) ) ;
#13930=VECTOR ( 'NONE', #22483, 1000.000000000000000 ) ;
#13936=CARTESIAN_POINT ( 'NONE',  ( 108.0288187330202732, -18.48434470291169873, 4.339809795830553263 ) ) ;
#13939=CARTESIAN_POINT ( 'NONE',  ( 3.554613218822866738, -15.76807188677689275, -4.522129901861166701 ) ) ;
#13943=VECTOR ( 'NONE', #26462, 1000.000000000000000 ) ;
#13945=DIRECTION ( 'NONE',  ( -0.000000000000000000, 0.000000000000000000, 1.000000000000000000 ) ) ;
#13956=CARTESIAN_POINT ( 'NONE',  ( 8.845957756505406167, -0.9823800962678642668, 1.000000000000000000 ) ) ;
#13957=ORIENTED_EDGE ( 'NONE', *, *, #21383, .F. ) ;
#13962=CARTESIAN_POINT ( 'NONE',  ( 0.3143644610611543433, -7.550156354830646954, 1.500000000000071720 ) ) ;
#13970=CARTESIAN_POINT ( 'NONE',  ( 23.02255580926556178, -17.31849206757231840, -1.529834177132233686 ) ) ;
#13973=EDGE_LOOP ( 'NONE', ( #9567, #9215, #29950, #460 ) ) ;
#13981=ORIENTED_EDGE ( 'NONE', *, *, #25725, .T. ) ;
#13984=B_SPLINE_SURFACE_WITH_KNOTS ( 'NONE', 1, 3, ( 
 ( #4831, #7338, #10355, #5174, #2663, #25233, #32599, #27418, #32780, #17382, #22884, #33088, #2162, #25402, #27576, #10009 ),
 ( #12833, #30604, #9671, #19899, #20566, #4524, #24897, #23048, #172, #17212, #7686, #30113, #20220, #30415, #4675, #14845 ),
 ( #25044, #9858, #5022, #15200, #2512, #27722, #2353, #12528, #22735, #13321, #8334, #30922, #28400, #16181, #31087, #8480 ) ),
 .UNSPECIFIED., .F., .F., .F.,
 ( 2, 1, 2 ),
 ( 4, 2, 2, 2, 2, 2, 2, 4 ),
 ( 0.000000000000000000, 1.000000000000000000, 1.172438907768402538 ),
 ( 0.000000000000000000, 0.5000000000000000000, 0.6250000000000000000, 0.7500000000000000000, 0.8125000000000000000, 0.8750000000000000000, 0.9375000000000000000, 1.000000000000000000 ),
 .UNSPECIFIED. ) ;
#13989=DIRECTION ( 'NONE',  ( 1.000000000000000000, 0.000000000000000000, 0.000000000000000000 ) ) ;
#13990=AXIS2_PLACEMENT_3D ( 'NONE', #24869, #19036, #21853 ) ;
#13996=CARTESIAN_POINT ( 'NONE',  ( 0.3285611067768007265, -13.34342412962908853, 4.522129901861159595 ) ) ;
#14024=ORIENTED_EDGE ( 'NONE', *, *, #11032, .F. ) ;
#14028=DIRECTION ( 'NONE',  ( -1.000000000000000000, 0.000000000000000000, 0.000000000000000000 ) ) ;
#14048=CARTESIAN_POINT ( 'NONE',  ( -4.433175167559320506, -8.339139981106209021, -1.500000000000000000 ) ) ;
#14057=CARTESIAN_POINT ( 'NONE',  ( 21.02910828058395865, -21.78322936331010595, 1.363801422436717870 ) ) ;
#14059=CARTESIAN_POINT ( 'NONE',  ( -29.23615344119660264, -25.43932300454937945, 11.04051477514566315 ) ) ;
#14061=CARTESIAN_POINT ( 'NONE',  ( 107.9480651260689967, -17.32151285178439437, 4.509510090909671476 ) ) ;
#14071=EDGE_CURVE ( 'NONE', #12752, #11856, #117, .T. ) ;
#14079=CARTESIAN_POINT ( 'NONE',  ( 25.43628654896041397, -17.54453578616353582, -1.000000000000000000 ) ) ;
#14083=CARTESIAN_POINT ( 'NONE',  ( 12.29359088965170521, -13.32350402071905471, -1.000000000000000000 ) ) ;
#14085=CARTESIAN_POINT ( 'NONE',  ( 107.9811858922438006, -17.79844364529119716, -4.362021580293085954 ) ) ;
#14095=VERTEX_POINT ( 'NONE', #25769 ) ;
#14098=DIRECTION ( 'NONE',  ( 2.473959037481237219E-13, 1.000000000000000000, -0.000000000000000000 ) ) ;
#14101=CARTESIAN_POINT ( 'NONE',  ( 21.37217251140765484, -21.79767279465048802, -1.352145825573628279 ) ) ;
#14103=ORIENTED_EDGE ( 'NONE', *, *, #22795, .F. ) ;
#14104=CARTESIAN_POINT ( 'NONE',  ( 9.130836792357447607, -14.25899304337494478, -1.499999999999999112 ) ) ;
#14114=ORIENTED_EDGE ( 'NONE', *, *, #2811, .T. ) ;
#14117=VECTOR ( 'NONE', #16808, 1000.000000000000000 ) ;
#14126=CARTESIAN_POINT ( 'NONE',  ( 17.97422212135272446, -19.86246923125032282, -4.522129901861166701 ) ) ;
#14132=FACE_OUTER_BOUND ( 'NONE', #8319, .T. ) ;
#14134=DIRECTION ( 'NONE',  ( -0.000000000000000000, -0.000000000000000000, -1.000000000000000000 ) ) ;
#14138=CARTESIAN_POINT ( 'NONE',  ( 22.45654429440861222, -21.89488324759587101, -1.207178455809153395 ) ) ;
#14140=CARTESIAN_POINT ( 'NONE',  ( 9.437548970008970528, 0.1642588933130853524, 1.500000000000000000 ) ) ;
#14142=CARTESIAN_POINT ( 'NONE',  ( 11.67286638378758745, -13.57952815233258903, -1.499999999999999778 ) ) ;
#14145=CARTESIAN_POINT ( 'NONE',  ( 0.1995908835383632951, -7.569794710591879472, 1.774175096175876432 ) ) ;
#14149=ORIENTED_EDGE ( 'NONE', *, *, #23196, .T. ) ;
#14153=CARTESIAN_POINT ( 'NONE',  ( 24.05790257984022062, -17.31116499701210287, -1.379149890413408963 ) ) ;
#14159=FACE_OUTER_BOUND ( 'NONE', #1365, .T. ) ;
#14187=ORIENTED_EDGE ( 'NONE', *, *, #25064, .F. ) ;
#14191=CARTESIAN_POINT ( 'NONE',  ( 0.4785084283111751269, -8.598468463561344421, -1.771410369227642834 ) ) ;
#14198=CARTESIAN_POINT ( 'NONE',  ( -14.83051435581985444, -21.73221622337167958, -1.500000000000000000 ) ) ;
#14200=CARTESIAN_POINT ( 'NONE',  ( -15.00280984543113583, -21.93932300455818307, 1.000000000000000000 ) ) ;
#14211=CARTESIAN_POINT ( 'NONE',  ( 107.3477315916820913, -15.88627780335592732, 1.500000000000000000 ) ) ;
#14218=CARTESIAN_POINT ( 'NONE',  ( 24.35832023931602208, -17.33818253687209676, 1.317734466820223549 ) ) ;
#14229=CARTESIAN_POINT ( 'NONE',  ( -3.368835499171254799, -11.43153892038626829, -1.500000000000000888 ) ) ;
#14235=CARTESIAN_POINT ( 'NONE',  ( 8.323087564152283235, -11.23204384871575812, -1.500000000000000000 ) ) ;
#14236=CARTESIAN_POINT ( 'NONE',  ( 107.4512831466929583, -17.37794483578546689, -4.567559570125502511 ) ) ;
#14242=CARTESIAN_POINT ( 'NONE',  ( 24.41748882719689107, -17.42561905328290095, -1.443068816866804882 ) ) ;
#14259=ORIENTED_EDGE ( 'NONE', *, *, #7015, .T. ) ;
#14273=CARTESIAN_POINT ( 'NONE',  ( 13.24595149388380300, -17.70232641594038014, -5.485967528433937979 ) ) ;
#14275=DIRECTION ( 'NONE',  ( 1.224646799147353207E-16, 1.000000000000000000, 0.000000000000000000 ) ) ;
#14276=EDGE_CURVE ( 'NONE', #15410, #28448, #20216, .T. ) ;
#14288=CARTESIAN_POINT ( 'NONE',  ( 7.594557537342751630, -2.555973540832573665, 1.500000000000000000 ) ) ;
#14291=CARTESIAN_POINT ( 'NONE',  ( 5.414493835220194562, -13.03402177297271791, 1.500000000000845324 ) ) ;
#14295=CARTESIAN_POINT ( 'NONE',  ( -0.6222850063875347004, -14.83242053952924522, 1.500000000000000000 ) ) ;
#14299=CARTESIAN_POINT ( 'NONE',  ( -2.673784117434885310, -0.4252644786298063750, 1.725835304028459527 ) ) ;
#14304=CARTESIAN_POINT ( 'NONE',  ( 23.24965750580003387, -21.93932300456764395, -1.000000000000000000 ) ) ;
#14309=CARTESIAN_POINT ( 'NONE',  ( -31.18783180709124636, -21.43932300455417916, 1.500000000000000000 ) ) ;
#14315=CARTESIAN_POINT ( 'NONE',  ( 25.02103040602151651, -17.46523595225292880, -1.208340562988329037 ) ) ;
#14318=ORIENTED_EDGE ( 'NONE', *, *, #27986, .T. ) ;
#14338=CARTESIAN_POINT ( 'NONE',  ( 7.214435349459066060, -13.85197079645077878, -1.500000000000000444 ) ) ;
#14340=ORIENTED_EDGE ( 'NONE', *, *, #18545, .F. ) ;
#14349=EDGE_CURVE ( 'NONE', #2520, #19511, #20563, .T. ) ;
#14355=DIRECTION ( 'NONE',  ( 0.000000000000000000, -0.000000000000000000, -1.000000000000000000 ) ) ;
#14368=CARTESIAN_POINT ( 'NONE',  ( 21.16281565822857758, -21.79884031534714595, 1.349901004997127396 ) ) ;
#14372=ORIENTED_EDGE ( 'NONE', *, *, #16988, .T. ) ;
#14377=CARTESIAN_POINT ( 'NONE',  ( -3.686555117304171070, -10.77456164543319161, -1.500000000000000444 ) ) ;
#14381=CARTESIAN_POINT ( 'NONE',  ( -3.467098320250194821, -1.941669238915278983, 1.500000000001435296 ) ) ;
#14382=CARTESIAN_POINT ( 'NONE',  ( 7.230698034991824841, -5.790874021893237966, -1.499999999999857225 ) ) ;
#14383=CARTESIAN_POINT ( 'NONE',  ( 108.0598553040188534, -18.93126360436130895, -4.568634059891971688 ) ) ;
#14394=ORIENTED_EDGE ( 'NONE', *, *, #14562, .T. ) ;
#14401=CARTESIAN_POINT ( 'NONE',  ( 3.393608999705061802, -0.06500480712390584170, -1.255126411524210450 ) ) ;
#14411=CARTESIAN_POINT ( 'NONE',  ( 20.06012370291166391, -21.48645126995948829, -1.642756992391330773 ) ) ;
#14420=CARTESIAN_POINT ( 'NONE',  ( -31.60000000000018971, -21.93932300455407969, 1.499999999998983480 ) ) ;
#14421=CARTESIAN_POINT ( 'NONE',  ( -50.60000000000000142, -10.96966150227468972, 1.000000000000000000 ) ) ;
#14430=CARTESIAN_POINT ( 'NONE',  ( 0.4398628304357228846, -12.95602692781729282, -5.485967528433938867 ) ) ;
#14434=EDGE_CURVE ( 'NONE', #140, #16376, #32115, .T. ) ;
#14436=FACE_OUTER_BOUND ( 'NONE', #25513, .T. ) ;
#14442=ORIENTED_EDGE ( 'NONE', *, *, #28160, .T. ) ;
#14453=CARTESIAN_POINT ( 'NONE',  ( 18.48762451651099781, -16.70791404657606094, 1.499999999999163558 ) ) ;
#14458=CARTESIAN_POINT ( 'NONE',  ( -0.3439025151734569907, -15.06911885298311304, 1.500000000000000444 ) ) ;
#14460=CIRCLE ( 'NONE', #1680, 0.4499999999999999556 ) ;
#14470=CARTESIAN_POINT ( 'NONE',  ( -2.681019058075245542, 0.000000000000000000, 1.353976854744275871 ) ) ;
#14484=CARTESIAN_POINT ( 'NONE',  ( -29.24402871571406237, -28.43932300454937590, 11.00000000000000000 ) ) ;
#14486=CARTESIAN_POINT ( 'NONE',  ( 23.27353278736381981, -21.94187821002792660, 1.000000000000000000 ) ) ;
#14502=VERTEX_POINT ( 'NONE', #11150 ) ;
#14522=CARTESIAN_POINT ( 'NONE',  ( 2.896241209900578539, -11.44832573956215249, -1.500000000000036637 ) ) ;
#14526=CIRCLE ( 'NONE', #143, 2.099999999999997868 ) ;
#14541=CARTESIAN_POINT ( 'NONE',  ( 0.7299402604449777288, -15.54820927731847569, -1.500000000000079270 ) ) ;
#14562=EDGE_CURVE ( 'NONE', #19632, #9004, #3291, .T. ) ;
#14564=CARTESIAN_POINT ( 'NONE',  ( -29.24402871571405882, -25.93932300454937945, 11.00000000000000000 ) ) ;
#14573=CARTESIAN_POINT ( 'NONE',  ( 107.4297505511455313, -17.06807598898313927, 3.923214148221579656 ) ) ;
#14581=CARTESIAN_POINT ( 'NONE',  ( 6.784984840995218924, -5.399320162307486903, -1.500000000000000000 ) ) ;
#14582=CARTESIAN_POINT ( 'NONE',  ( 107.5536565100458830, -18.86584003217233629, -4.757788453915527960 ) ) ;
#14584=DIRECTION ( 'NONE',  ( -0.000000000000000000, 0.000000000000000000, 1.000000000000000000 ) ) ;
#14596=CARTESIAN_POINT ( 'NONE',  ( -5.427698642335591239E-12, -21.93932300456189566, 1.500000000000000000 ) ) ;
#14599=CARTESIAN_POINT ( 'NONE',  ( 108.4615897723380868, -15.55450498649102720, -0.9788672205888330202 ) ) ;
#14610=ORIENTED_EDGE ( 'NONE', *, *, #1746, .T. ) ;
#14619=DIRECTION ( 'NONE',  ( -1.000000000000000000, -0.000000000000000000, 1.387778780781444256E-14 ) ) ;
#14621=CARTESIAN_POINT ( 'NONE',  ( 108.1293191352079361, -19.93152549158542897, 2.509206947344208238 ) ) ;
#14624=CARTESIAN_POINT ( 'NONE',  ( -0.7867377105085294753, -2.707992247746929149, -5.485967528433937979 ) ) ;
#14629=CARTESIAN_POINT ( 'NONE',  ( 110.2779561444949223, -18.44184597392422020, 5.485967528433935314 ) ) ;
#14641=FACE_OUTER_BOUND ( 'NONE', #11406, .T. ) ;
#14652=CARTESIAN_POINT ( 'NONE',  ( -29.24402871571405882, -27.93932300454937590, 11.00000000000000000 ) ) ;
#14659=CARTESIAN_POINT ( 'NONE',  ( 22.98163386837276434, -21.92547295135298313, -1.118948288781295153 ) ) ;
#14664=LINE ( 'NONE', #12151, #6413 ) ;
#14682=CARTESIAN_POINT ( 'NONE',  ( 2.281627749324421917, -0.2935656086769610207, 1.757435426329174044 ) ) ;
#14683=ORIENTED_EDGE ( 'NONE', *, *, #12640, .F. ) ;
#14698=CARTESIAN_POINT ( 'NONE',  ( 0.1512968795556346446, -7.218651089666939136, -1.774506416594164637 ) ) ;
#14706=CARTESIAN_POINT ( 'NONE',  ( -15.02135460118491217, -21.93013659628234890, 1.095404497688272638 ) ) ;
#14713=CARTESIAN_POINT ( 'NONE',  ( 0.8027523773784053240, -15.44646927475563913, -1.746109446251894681 ) ) ;
#14715=ADVANCED_FACE ( 'NONE', ( #3990 ), #12142, .F. ) ;
#14726=CARTESIAN_POINT ( 'NONE',  ( 107.6641398346957033, -20.45810202417174750, 1.500000000000000000 ) ) ;
#14728=FACE_OUTER_BOUND ( 'NONE', #26731, .T. ) ;
#14736=CARTESIAN_POINT ( 'NONE',  ( -4.555597372409920354, -6.492899504186820714, -1.500000000000000666 ) ) ;
#14737=ORIENTED_EDGE ( 'NONE', *, *, #13212, .F. ) ;
#14740=CARTESIAN_POINT ( 'NONE',  ( -17.45597128428593336, -27.93932300454937590, 11.00000000000000000 ) ) ;
#14741=CARTESIAN_POINT ( 'NONE',  ( 8.060276137098751903, -2.738905750062150535, -1.000000000000000000 ) ) ;
#14742=CARTESIAN_POINT ( 'NONE',  ( 107.9496129882747937, -17.34380168244590337, -4.567365599077690241 ) ) ;
#14746=DIRECTION ( 'NONE',  ( -0.000000000000000000, -0.000000000000000000, -1.000000000000000000 ) ) ;
#14755=DIRECTION ( 'NONE',  ( -0.000000000000000000, 0.000000000000000000, 1.000000000000000000 ) ) ;
#14759=CARTESIAN_POINT ( 'NONE',  ( 2.454674724652319728, -0.02938977324472418981, -1.729574810602341861 ) ) ;
#14765=CARTESIAN_POINT ( 'NONE',  ( -15.02135460118491217, -21.93013659628234890, 1.095404497688272638 ) ) ;
#14767=ORIENTED_EDGE ( 'NONE', *, *, #16195, .F. ) ;
#14780=FACE_OUTER_BOUND ( 'NONE', #3045, .T. ) ;
#14796=CARTESIAN_POINT ( 'NONE',  ( 0.000000000000000000, 0.000000000000000000, 0.000000000000000000 ) ) ;
#14797=ORIENTED_EDGE ( 'NONE', *, *, #11804, .T. ) ;
#14804=DIRECTION ( 'NONE',  ( 0.000000000000000000, -1.000000000000000000, 0.000000000000000000 ) ) ;
#14809=CARTESIAN_POINT ( 'NONE',  ( 22.80257615841729191, -21.89069152845288713, -1.310091664434587022 ) ) ;
#14811=EDGE_CURVE ( 'NONE', #9859, #6440, #23451, .T. ) ;
#14839=EDGE_CURVE ( 'NONE', #24091, #19481, #27853, .T. ) ;
#14844=CARTESIAN_POINT ( 'NONE',  ( 0.5290670167336711804, -6.525914665286372873, -1.500000000000000444 ) ) ;
#14845=CARTESIAN_POINT ( 'NONE',  ( 2.600000000000000089, 0.000000000000000000, 1.500000000000000444 ) ) ;
#14853=CARTESIAN_POINT ( 'NONE',  ( 24.14342515508168674, -17.38895391569510807, 1.425886477552664289 ) ) ;
#14862=CARTESIAN_POINT ( 'NONE',  ( -3.308580754637445498, -10.64006648303969271, -1.743554639575954690 ) ) ;
#14867=ORIENTED_EDGE ( 'NONE', *, *, #16934, .F. ) ;
#14870=EDGE_CURVE ( 'NONE', #31289, #28214, #6565, .T. ) ;
#14872=CARTESIAN_POINT ( 'NONE',  ( 21.37217251140774721, -21.79767279465052709, 1.352145825573594307 ) ) ;
#14881=ORIENTED_EDGE ( 'NONE', *, *, #8916, .T. ) ;
#14886=CARTESIAN_POINT ( 'NONE',  ( -17.45597128428592981, -27.93932300454937590, 11.00000000000000000 ) ) ;
#14888=CARTESIAN_POINT ( 'NONE',  ( -4.458006279114910875, -5.037799543062196683, 1.500000000000000000 ) ) ;
#14890=CARTESIAN_POINT ( 'NONE',  ( 107.3477315916820913, -15.88627780335592732, 1.500000000000000000 ) ) ;
#14891=CARTESIAN_POINT ( 'NONE',  ( 108.0616218773274824, -18.95670182053928698, -4.502367357316522600 ) ) ;
#14899=CARTESIAN_POINT ( 'NONE',  ( 20.00016891673655195, -21.67414139014265473, -1.443203664631054428 ) ) ;
#14905=ADVANCED_FACE ( 'NONE', ( #18773 ), #16414, .T. ) ;
#14912=ORIENTED_EDGE ( 'NONE', *, *, #15920, .T. ) ;
#14917=ORIENTED_EDGE ( 'NONE', *, *, #16796, .F. ) ;
#14920=EDGE_CURVE ( 'NONE', #15578, #10646, #2305, .T. ) ;
#14924=CARTESIAN_POINT ( 'NONE',  ( 3.529609406779910419, -12.17998485103522199, -1.500000000000000000 ) ) ;
#14929=CARTESIAN_POINT ( 'NONE',  ( 107.5603894785017047, -18.96336710931705838, 4.563597971275775933 ) ) ;
#14933=CARTESIAN_POINT ( 'NONE',  ( 107.8460215217088631, -15.85211033425179039, -1.499787059522396326 ) ) ;
#14937=CARTESIAN_POINT ( 'NONE',  ( -1.170068671574867158, -6.059534462705557623, 4.522129901861156931 ) ) ;
#14949=CARTESIAN_POINT ( 'NONE',  ( -50.60000000000000142, -10.96966150227468972, -1.500000000000000000 ) ) ;
#14950=CARTESIAN_POINT ( 'NONE',  ( 107.5411459829244052, -18.68417316270920026, 4.956489308412717065 ) ) ;
#14953=CARTESIAN_POINT ( 'NONE',  ( 6.555498503425793544, -13.70794208679299153, 1.755773382248213110 ) ) ;
#14957=CARTESIAN_POINT ( 'NONE',  ( 15.88616825581402203, -21.20699617082199850, 1.500000000000000000 ) ) ;
#14970=ORIENTED_EDGE ( 'NONE', *, *, #17900, .T. ) ;
#14971=AXIS2_PLACEMENT_3D ( 'NONE', #14421, #24630, #11957 ) ;
#14979=CARTESIAN_POINT ( 'NONE',  ( 23.24965665534722348, -21.93932291342295215, 1.034606501594972583 ) ) ;
#14988=CARTESIAN_POINT ( 'NONE',  ( 3.519433398973329297, -1.626303258728258623E-15, -1.098451328137469929 ) ) ;
#15007=CARTESIAN_POINT ( 'NONE',  ( 108.0291781248180598, -18.48951985539477505, -4.325670280508457921 ) ) ;
#15010=CARTESIAN_POINT ( 'NONE',  ( 15.92126372259303224, -16.39212668776233883, -1.753532113938507608 ) ) ;
#15016=CARTESIAN_POINT ( 'NONE',  ( -55.59999999999999432, -10.96966150227468972, 6.999999999999999112 ) ) ;
#15019=CARTESIAN_POINT ( 'NONE',  ( 21.59695500784411593, -17.14749606024852469, 1.524646196218438110 ) ) ;
#15024=VECTOR ( 'NONE', #10263, 1000.000000000000000 ) ;
#15030=CARTESIAN_POINT ( 'NONE',  ( -0.4073435738283839314, -14.65433346320568653, -1.499999999999723110 ) ) ;
#15038=CIRCLE ( 'NONE', #10340, 6.000000000000001776 ) ;
#15041=DIRECTION ( 'NONE',  ( -1.000000000000000000, 2.498001805406600196E-13, 0.000000000000000000 ) ) ;
#15046=ORIENTED_EDGE ( 'NONE', *, *, #27813, .F. ) ;
#15049=ORIENTED_EDGE ( 'NONE', *, *, #2150, .T. ) ;
#15052=AXIS2_PLACEMENT_3D ( 'NONE', #29413, #21577, #14028 ) ;
#15053=DIRECTION ( 'NONE',  ( -0.000000000000000000, -0.000000000000000000, -1.000000000000000000 ) ) ;
#15060=CARTESIAN_POINT ( 'NONE',  ( 21.08401840680159367, -16.78474387324287775, 1.500000000000000000 ) ) ;
#15064=CARTESIAN_POINT ( 'NONE',  ( 7.461135469111495944, -4.560857689424945960, -1.500000000000000000 ) ) ;
#15066=ORIENTED_EDGE ( 'NONE', *, *, #25949, .F. ) ;
#15068=AXIS2_PLACEMENT_3D ( 'NONE', #29884, #30236, #6808 ) ;
#15082=AXIS2_PLACEMENT_3D ( 'NONE', #16361, #498, #26569 ) ;
#15087=FACE_OUTER_BOUND ( 'NONE', #30573, .T. ) ;
#15089=ADVANCED_FACE ( 'NONE', ( #27767 ), #4565, .T. ) ;
#15090=CARTESIAN_POINT ( 'NONE',  ( 6.013832568680315127, -13.53405802968792848, -1.500000000000000444 ) ) ;
#15094=ORIENTED_EDGE ( 'NONE', *, *, #22241, .T. ) ;
#15098=CARTESIAN_POINT ( 'NONE',  ( -2.767073886773234292, -0.6621507858625358400, 1.748408842879327629 ) ) ;
#15101=CARTESIAN_POINT ( 'NONE',  ( -3.029131898378900623, -0.04852093894418087194, 1.223527895085199768 ) ) ;
#15110=CARTESIAN_POINT ( 'NONE',  ( 2.600000000000000089, 0.000000000000000000, 1.500000000000000000 ) ) ;
#15115=CARTESIAN_POINT ( 'NONE',  ( 108.1329823800173671, -19.98427530701536270, 1.262026545339602679 ) ) ;
#15119=CARTESIAN_POINT ( 'NONE',  ( 25.45368006873450994, -17.55541207042479712, 1.083666005367639018 ) ) ;
#15140=CARTESIAN_POINT ( 'NONE',  ( -29.73484230743789070, -27.93932300454937590, 11.09540449768827308 ) ) ;
#15148=CARTESIAN_POINT ( 'NONE',  ( -4.027742607708217015, -8.337697986505625991, 1.744154148835437956 ) ) ;
#15149=ADVANCED_FACE ( 'NONE', ( #1904 ), #15561, .F. ) ;
#15152=CARTESIAN_POINT ( 'NONE',  ( 107.9812533011594269, -17.79941431690619069, -4.365076636216545403 ) ) ;
#15158=CARTESIAN_POINT ( 'NONE',  ( 108.1288400433390393, -19.92462668933127290, 1.384270303710046335 ) ) ;
#15161=DIRECTION ( 'NONE',  ( 0.000000000000000000, -0.000000000000000000, -1.000000000000000000 ) ) ;
#15170=CARTESIAN_POINT ( 'NONE',  ( 23.85324836636416634, -17.43424264171716231, -1.580747861890610562 ) ) ;
#15181=LINE ( 'NONE', #12661, #5533 ) ;
#15192=DIRECTION ( 'NONE',  ( 0.000000000000000000, 1.000000000000000000, 0.000000000000000000 ) ) ;
#15200=CARTESIAN_POINT ( 'NONE',  ( 16.70660563660005593, -16.26387199940855410, 0.9788672205888330202 ) ) ;
#15208=CARTESIAN_POINT ( 'NONE',  ( 24.07542780980101682, -17.38801686517350475, 1.438486003925011136 ) ) ;
#15216=CARTESIAN_POINT ( 'NONE',  ( 11.65799190157298781, -20.33406113955203409, -1.499999999999997780 ) ) ;
#15226=ORIENTED_EDGE ( 'NONE', *, *, #21793, .F. ) ;
#15230=ORIENTED_EDGE ( 'NONE', *, *, #14276, .F. ) ;
#15239=CARTESIAN_POINT ( 'NONE',  ( 3.503000659536867900, -17.24537520706771687, 1.500000000000951017 ) ) ;
#15240=CARTESIAN_POINT ( 'NONE',  ( 7.278212735265215727, -5.482579124930866854, -1.000000000000000000 ) ) ;
#15245=B_SPLINE_CURVE_WITH_KNOTS ( 'NONE', 3,
 ( #11279, #13768, #13169, #19130, #24146, #1273, #1428, #13924, #21489, #26648, #31701, #8779, #18984, #29170, #11604, #18372 ),
 .UNSPECIFIED., .F., .F.,
 ( 4, 2, 2, 2, 2, 2, 2, 4 ),
 ( 0.01324599089036895827, 0.5000000000000000000, 0.6250000000000000000, 0.7500000000000000000, 0.8125000000000000000, 0.8749999999999998890, 0.9375000000000000000, 1.000000000000000000 ),
 .UNSPECIFIED. ) ;
#15248=CARTESIAN_POINT ( 'NONE',  ( 5.139557470515282267E-15, 0.000000000000000000, -4.137834579201380869 ) ) ;
#15250=CARTESIAN_POINT ( 'NONE',  ( -2.672624763096117739, -0.4219952926969700591, -1.725256589882067093 ) ) ;
#15258=ADVANCED_FACE ( 'NONE', ( #21246 ), #8522, .T. ) ;
#15259=CARTESIAN_POINT ( 'NONE',  ( 41.06247019076344884, -19.55897407381494091, -1.500000000000000444 ) ) ;
#15261=CARTESIAN_POINT ( 'NONE',  ( 10.75691143517498283, -12.51424465391554719, 1.000000000000000000 ) ) ;
#15269=VERTEX_POINT ( 'NONE', #27074 ) ;
#15271=VERTEX_POINT ( 'NONE', #11869 ) ;
#15273=CARTESIAN_POINT ( 'NONE',  ( 0.8174570305809125692, -9.170357625429589987, -1.500000000000000000 ) ) ;
#15282=CARTESIAN_POINT ( 'NONE',  ( 25.34157222223575445, -17.52646456585306822, 1.103933258152489882 ) ) ;
#15285=CARTESIAN_POINT ( 'NONE',  ( 18.53175858344379634, -21.44524224917989130, 1.500000000000000000 ) ) ;
#15303=ORIENTED_EDGE ( 'NONE', *, *, #7148, .T. ) ;
#15305=CARTESIAN_POINT ( 'NONE',  ( 0.08995365929913461123, -14.90597059099496136, 1.745535636305011629 ) ) ;
#15307=CARTESIAN_POINT ( 'NONE',  ( 108.0223616456019471, -18.39136425041039402, -4.509695625108203210 ) ) ;
#15308=CARTESIAN_POINT ( 'NONE',  ( -2.767073886773233848, -0.6621507858625358400, 1.748408842879327851 ) ) ;
#15313=CARTESIAN_POINT ( 'NONE',  ( 22.00639167669224960, -21.80013755708282730, -1.499999999999999556 ) ) ;
#15319=PLANE ( 'NONE',  #3973 ) ;
#15332=CARTESIAN_POINT ( 'NONE',  ( 0.2210079091045983601, -7.685141149027079344, 1.773955204205442060 ) ) ;
#15333=CARTESIAN_POINT ( 'NONE',  ( 11.50505501463784697, -13.50304080202605306, 1.500000000000000000 ) ) ;
#15343=DIRECTION ( 'NONE',  ( 0.000000000000000000, 0.000000000000000000, 1.000000000000000000 ) ) ;
#15346=ORIENTED_EDGE ( 'NONE', *, *, #20919, .T. ) ;
#15353=ORIENTED_EDGE ( 'NONE', *, *, #9196, .T. ) ;
#15368=CARTESIAN_POINT ( 'NONE',  ( 107.9462823452557814, -17.29584125157287744, 3.322807143010101605 ) ) ;
#15381=CARTESIAN_POINT ( 'NONE',  ( 6.655951778521610684, -18.71196003547629516, 1.500000000000000000 ) ) ;
#15385=CARTESIAN_POINT ( 'NONE',  ( 107.5719395156074540, -19.12968270266287618, -4.222684948861750165 ) ) ;
#15390=CARTESIAN_POINT ( 'NONE',  ( -3.806139276275473105, -9.688921910891492573, 1.499999999999999112 ) ) ;
#15401=VERTEX_POINT ( 'NONE', #20571 ) ;
#15402=CARTESIAN_POINT ( 'NONE',  ( 43.06800534735074137, -24.01680020629799728, 1.500000000000000000 ) ) ;
#15404=CARTESIAN_POINT ( 'NONE',  ( 107.4616189337527885, -17.52789370703686345, -4.846792217672044600 ) ) ;
#15408=CARTESIAN_POINT ( 'NONE',  ( 3.529609406779910419, -12.17998485103522199, -1.500000000000000444 ) ) ;
#15410=VERTEX_POINT ( 'NONE', #15016 ) ;
#15414=CARTESIAN_POINT ( 'NONE',  ( 107.4500593345382811, -17.36019228850094720, 4.522129901861156931 ) ) ;
#15415=DIRECTION ( 'NONE',  ( 0.000000000000000000, 0.000000000000000000, 1.000000000000000000 ) ) ;
#15418=ORIENTED_EDGE ( 'NONE', *, *, #9574, .T. ) ;
#15424=CARTESIAN_POINT ( 'NONE',  ( 41.06247019076344884, -19.55897407381494091, -1.500000000000000000 ) ) ;
#15427=CARTESIAN_POINT ( 'NONE',  ( 1.067267558240149850, -2.636048217392937154, -1.760945737653910825 ) ) ;
#15429=CARTESIAN_POINT ( 'NONE',  ( 15.81086013898703690, -14.68957282009552756, -1.500000000000274447 ) ) ;
#15433=CARTESIAN_POINT ( 'NONE',  ( 14.72414172255109222, -15.74544918409871741, 1.500000000000000444 ) ) ;
#15436=CARTESIAN_POINT ( 'NONE',  ( 111.5384102276623395, -20.44549501350944709, 0.9788672205877712029 ) ) ;
#15443=CARTESIAN_POINT ( 'NONE',  ( -17.45597128428592981, -25.93932300454937945, 11.00000000000000000 ) ) ;
#15449=ORIENTED_EDGE ( 'NONE', *, *, #3496, .F. ) ;
#15462=ORIENTED_EDGE ( 'NONE', *, *, #2402, .T. ) ;
#15473=PLANE ( 'NONE',  #22441 ) ;
#15474=LINE ( 'NONE', #25686, #24150 ) ;
#15477=EDGE_CURVE ( 'NONE', #9323, #28886, #29483, .T. ) ;
#15478=CARTESIAN_POINT ( 'NONE',  ( 24.43238093800358968, -17.43085383294892665, 1.450662971657243006 ) ) ;
#15481=CARTESIAN_POINT ( 'NONE',  ( 23.22564502775751194, -21.93932300456764040, 1.023882905580708380 ) ) ;
#15489=CARTESIAN_POINT ( 'NONE',  ( 10.69474453358853872, -15.18614050023080608, 1.754319658296275009 ) ) ;
#15490=CARTESIAN_POINT ( 'NONE',  ( 12.08436850396594409, -13.77779907615654231, 1.500000000000000000 ) ) ;
#15493=B_SPLINE_CURVE_WITH_KNOTS ( 'NONE', 3,
 ( #3889, #14368, #31963, #12065, #9211, #24576, #19440, #26770, #11714, #19745 ),
 .UNSPECIFIED., .F., .F.,
 ( 4, 2, 2, 2, 4 ),
 ( 0.000000000000000000, 0.0005028294029233987402, 0.001005658805846797480, 0.002011317611693595828, 0.004022635223387192524 ),
 .UNSPECIFIED. ) ;
#15495=CARTESIAN_POINT ( 'NONE',  ( 1.184669658563290984, -2.669308969140904431, 1.499999999999999334 ) ) ;
#15506=ORIENTED_EDGE ( 'NONE', *, *, #2402, .F. ) ;
#15513=CIRCLE ( 'NONE', #1084, 0.4500000000000000111 ) ;
#15518=DIRECTION ( 'NONE',  ( 1.000000000000000000, 0.000000000000000000, 0.000000000000000000 ) ) ;
#15561=( BOUNDED_SURFACE ( )  B_SPLINE_SURFACE ( 3, 2, ( 
 ( #16917, #27111, #4211 ),
 ( #12223, #14381, #17065 ),
 ( #12077, #24592, #32643 ),
 ( #29802, #7053, #14888 ),
 ( #27463, #13213, #28267 ),
 ( #32980, #31140, #10547 ),
 ( #25947, #519, #15745 ),
 ( #10704, #5213, #2553 ),
 ( #12720, #10048, #373 ),
 ( #20262, #23413, #12568 ),
 ( #20920, #15390, #5374 ),
 ( #20758, #5709, #2707 ),
 ( #22922, #30, #30814 ),
 ( #22774, #10215, #20437 ),
 ( #8225, #30656, #30958 ),
 ( #15562, #8040, #7733 ),
 ( #25779, #18074, #13069 ),
 ( #17925, #18425, #12882 ),
 ( #2906, #28615, #30461 ),
 ( #25598, #15889, #23101 ),
 ( #27958, #26099, #28116 ),
 ( #7543, #18238, #28451 ),
 ( #5563, #20607, #17748 ),
 ( #23270, #5062, #3057 ),
 ( #222, #15239, #10398 ),
 ( #25442, #7882, #16230 ),
 ( #13364, #23577, #16035 ),
 ( #29107, #9007, #31788 ),
 ( #5852, #26447, #3860 ),
 ( #8859, #3203, #1184 ),
 ( #31942, #11382, #6196 ),
 ( #8373, #19068, #26588 ),
 ( #13548, #869, #6341 ),
 ( #3545, #18569, #701 ) ),
 .UNSPECIFIED., .F., .F., .F. ) 
 B_SPLINE_SURFACE_WITH_KNOTS ( ( 4, 2, 2, 2, 2, 2, 2, 2, 2, 2, 2, 2, 2, 2, 2, 2, 4 ),
 ( 3, 3 ),
 ( 0.000000000000000000, 0.004360647101759708780, 0.005450808877199635541, 0.006540970652639563170, 0.008721294203519417559, 0.009811455978959344321, 0.01090161775439927108, 0.01199177952983919784, 0.01308194130527912634, 0.01526226485615898160, 0.01635242663159890836, 0.01744258840703883512, 0.02180323550879854216, 0.02398355905967839569, 0.02616388261055825268, 0.03052452971231796319, 0.03488517681407767024 ),
 ( 0.000000000000000000, 1.000000000000000000 ),
 .UNSPECIFIED. ) 
 GEOMETRIC_REPRESENTATION_ITEM ( )  RATIONAL_B_SPLINE_SURFACE ( (
 ( 1.000000000000000000, 0.8508761217583463710, 1.000000000000000000),
 ( 1.000000000000000000, 0.8513495319938002570, 1.000000000000000000),
 ( 1.000000000000000000, 0.8517269884644930178, 1.000000000000000000),
 ( 1.000000000000000000, 0.8525421454182948722, 1.000000000000000000),
 ( 1.000000000000000000, 0.8526809326693643998, 1.000000000000000000),
 ( 1.000000000000000000, 0.8529405002960604998, 1.000000000000000000),
 ( 1.000000000000000000, 0.8530607137251564609, 1.000000000000000000),
 ( 1.000000000000000000, 0.8534148190580183035, 1.000000000000000000),
 ( 1.000000000000000000, 0.8536546399906833615, 1.000000000000000000),
 ( 1.000000000000000000, 0.8539619561405888959, 1.000000000000000000),
 ( 1.000000000000000000, 0.8540316006964270290, 1.000000000000000000),
 ( 1.000000000000000000, 0.8540602160990389269, 1.000000000000000000),
 ( 1.000000000000000000, 0.8540396656596365155, 1.000000000000000000),
 ( 1.000000000000000000, 0.8539811480365533392, 1.000000000000000000),
 ( 1.000000000000000000, 0.8539432201616324880, 1.000000000000000000),
 ( 1.000000000000000000, 0.8538670549725509984, 1.000000000000000000),
 ( 1.000000000000000000, 0.8538286323939511258, 1.000000000000000000),
 ( 1.000000000000000000, 0.8536850005030293120, 1.000000000000000000),
 ( 1.000000000000000000, 0.8533603115986116983, 1.000000000000000000),
 ( 1.000000000000000000, 0.8529655131887596831, 1.000000000000000000),
 ( 1.000000000000000000, 0.8528244803202271740, 1.000000000000000000),
 ( 1.000000000000000000, 0.8525300428278739240, 1.000000000000000000),
 ( 1.000000000000000000, 0.8523762152465480524, 1.000000000000000000),
 ( 1.000000000000000000, 0.8516129968056589394, 1.000000000000000000),
 ( 1.000000000000000000, 0.8513036313371858954, 1.000000000000000000),
 ( 1.000000000000000000, 0.8508287765237684264, 1.000000000000000000),
 ( 1.000000000000000000, 0.8506601442286274573, 1.000000000000000000),
 ( 1.000000000000000000, 0.8503078737455993519, 1.000000000000000000),
 ( 1.000000000000000000, 0.8501262971080763009, 1.000000000000000000),
 ( 1.000000000000000000, 0.8496349502455389224, 1.000000000000000000),
 ( 1.000000000000000000, 0.8494863746679542915, 1.000000000000000000),
 ( 1.000000000000000000, 0.8492518789947639535, 1.000000000000000000),
 ( 1.000000000000000000, 0.8491664934843269341, 1.000000000000000000),
 ( 1.000000000000000000, 0.8490876263417839187, 1.000000000000000000) ) ) 
 REPRESENTATION_ITEM ( '' )  SURFACE ( )  );
#15562=CARTESIAN_POINT ( 'NONE',  ( -2.454858791982045041, -12.18258820806518372, 1.743819948486679206 ) ) ;
#15566=CARTESIAN_POINT ( 'NONE',  ( -23.35000000000000142, -10.96966150227469505, 4.000000000000000000 ) ) ;
#15578=VERTEX_POINT ( 'NONE', #3336 ) ;
#15579=CARTESIAN_POINT ( 'NONE',  ( 108.0281774240363717, -18.47511001308152601, 4.365040738911419638 ) ) ;
#15584=AXIS2_PLACEMENT_3D ( 'NONE', #25528, #10323, #5146 ) ;
#15590=CARTESIAN_POINT ( 'NONE',  ( -1.033057378353439804, -8.048844657541355474, -4.522129901861164925 ) ) ;
#15593=CARTESIAN_POINT ( 'NONE',  ( 107.9808062360839216, -17.79297669103587154, 4.347487705976786465 ) ) ;
#15599=CARTESIAN_POINT ( 'NONE',  ( -3.018833153847216622, -0.05660549560302519101, 1.240144350321864763 ) ) ;
#15609=CARTESIAN_POINT ( 'NONE',  ( 11.95049951519663978, -15.52103481658239659, -1.754067188414264233 ) ) ;
#15612=CARTESIAN_POINT ( 'NONE',  ( 108.1300413742128228, -19.95926608421481063, -1.392287898180229133 ) ) ;
#15620=CARTESIAN_POINT ( 'NONE',  ( 1.134906995224885584, -9.027104445734691396, 1.499999999999999334 ) ) ;
#15626=DIRECTION ( 'NONE',  ( -0.000000000000000000, -0.000000000000000000, 1.000000000000000000 ) ) ;
#15646=CARTESIAN_POINT ( 'NONE',  ( 110.4915906369627123, -18.78144465615449832, -4.522129901861166701 ) ) ;
#15647=ORIENTED_EDGE ( 'NONE', *, *, #9943, .F. ) ;
#15649=CARTESIAN_POINT ( 'NONE',  ( -2.767073886773233848, -0.6621507858625358400, 1.748408842879327851 ) ) ;
#15656=CARTESIAN_POINT ( 'NONE',  ( 108.1072762316657219, -19.61411316563674134, 2.020652039824201829 ) ) ;
#15657=DIRECTION ( 'NONE',  ( -0.000000000000000000, -0.000000000000000000, -1.000000000000000000 ) ) ;
#15670=CARTESIAN_POINT ( 'NONE',  ( 24.62503378732304071, -17.47108153024710475, 1.492984249781206474 ) ) ;
#15683=CARTESIAN_POINT ( 'NONE',  ( 9.126991456845855666, -11.32614230912692577, 1.000000000000000000 ) ) ;
#15692=VECTOR ( 'NONE', #10285, 1000.000000000000114 ) ;
#15694=CARTESIAN_POINT ( 'NONE',  ( 2.342933509396897929, -0.1895978275999547213, -1.757325986342923363 ) ) ;
#15695=CARTESIAN_POINT ( 'NONE',  ( 24.80306213860490061, -17.49230408913781787, -1.500000000000000000 ) ) ;
#15703=CARTESIAN_POINT ( 'NONE',  ( 24.35832023931450507, -17.33818253687174860, -1.317734466820339900 ) ) ;
#15711=CIRCLE ( 'NONE', #27449, 0.9999999999999983347 ) ;
#15713=CARTESIAN_POINT ( 'NONE',  ( -31.86948564418014485, -21.73221622336745895, -1.500000000000000000 ) ) ;
#15729=CARTESIAN_POINT ( 'NONE',  ( -31.85000000000000497, -10.96966150227469505, 1.500000000000000000 ) ) ;
#15735=CARTESIAN_POINT ( 'NONE',  ( -17.45597128428592981, -25.93932300454937945, 11.50000000000000000 ) ) ;
#15740=DIRECTION ( 'NONE',  ( -0.000000000000000000, 0.000000000000000000, 1.000000000000000000 ) ) ;
#15745=CARTESIAN_POINT ( 'NONE',  ( -4.555723071052306672, -6.510850216547120262, 1.499999999999999556 ) ) ;
#15747=CARTESIAN_POINT ( 'NONE',  ( 3.286352104298968069, -0.1045966074583460498, 1.312070483712308500 ) ) ;
#15758=CARTESIAN_POINT ( 'NONE',  ( -2.863349216192390578, 0.2791979387067957119, -0.7890172491793835396 ) ) ;
#15762=ORIENTED_EDGE ( 'NONE', *, *, #27506, .T. ) ;
#15764=CARTESIAN_POINT ( 'NONE',  ( 107.6300413742128228, -19.95926608421483195, 0.000000000000000000 ) ) ;
#15765=CARTESIAN_POINT ( 'NONE',  ( 12.65465643788354200, -15.70291107026620914, -1.500000000000000444 ) ) ;
#15767=CARTESIAN_POINT ( 'NONE',  ( 107.9748542853220954, -17.70727008077477649, 5.017937325796186343 ) ) ;
#15774=DIRECTION ( 'NONE',  ( -1.000000000000000000, 2.473959037481237219E-13, 0.000000000000000000 ) ) ;
#15775=CARTESIAN_POINT ( 'NONE',  ( 107.3476768466458253, -15.88628154573095586, -1.500000000000000000 ) ) ;
#15783=CARTESIAN_POINT ( 'NONE',  ( 15.81158201665590290, -16.37188494488893298, -1.753542180525299532 ) ) ;
#15791=CARTESIAN_POINT ( 'NONE',  ( 107.4500593345376558, -17.36019228850485163, -4.522129901861164925 ) ) ;
#15799=CARTESIAN_POINT ( 'NONE',  ( 18.06874303396881132, -21.14907373874090979, -1.751201621421682120 ) ) ;
#15806=CARTESIAN_POINT ( 'NONE',  ( -3.827997810773342557, -10.69410007036992560, -0.9788672205760856615 ) ) ;
#15816=EDGE_CURVE ( 'NONE', #22652, #12927, #7457, .T. ) ;
#15823=CARTESIAN_POINT ( 'NONE',  ( -1.033057378353319677, -8.048844657541355474, -4.522129901861164925 ) ) ;
#15826=CARTESIAN_POINT ( 'NONE',  ( 24.59223457117506229, -17.46620485449347271, 1.489769045320403551 ) ) ;
#15827=CARTESIAN_POINT ( 'NONE',  ( 23.07496344424409784, -21.92049039159586954, 1.202267146568063660 ) ) ;
#15828=CARTESIAN_POINT ( 'NONE',  ( 9.350000000000001421, 0.000000000000000000, 1.500000000000000000 ) ) ;
#15829=CARTESIAN_POINT ( 'NONE',  ( 21.31323116099372328, -21.82417724537273074, 1.319197765239640718 ) ) ;
#15835=CARTESIAN_POINT ( 'NONE',  ( 20.69346795579748388, -16.15118080677402190, 1.499999999999722444 ) ) ;
#15857=ORIENTED_EDGE ( 'NONE', *, *, #20442, .F. ) ;
#15858=CARTESIAN_POINT ( 'NONE',  ( 22.17354848663237732, -17.00157258782005343, -1.495009212619101246 ) ) ;
#15859=DIRECTION ( 'NONE',  ( 0.000000000000000000, 0.000000000000000000, -1.000000000000000000 ) ) ;
#15868=ORIENTED_EDGE ( 'NONE', *, *, #17121, .T. ) ;
#15881=CARTESIAN_POINT ( 'NONE',  ( -0.3880080537174158128, -2.647099810593990465, -4.522129901861164925 ) ) ;
#15887=CARTESIAN_POINT ( 'NONE',  ( 107.6033161557439115, -19.58148931974192664, 3.296621981446858918 ) ) ;
#15889=CARTESIAN_POINT ( 'NONE',  ( -0.4074492901130932210, -14.65424174162825999, 1.499999999999921174 ) ) ;
#15895=EDGE_CURVE ( 'NONE', #21513, #28748, #7963, .T. ) ;
#15902=CARTESIAN_POINT ( 'NONE',  ( -2.861038829132525496, 0.01832029024615380863, -1.013940918434634186 ) ) ;
#15903=CARTESIAN_POINT ( 'NONE',  ( 107.9870691068026076, -17.88316047137711351, 4.509750785975439769 ) ) ;
#15904=DIRECTION ( 'NONE',  ( 1.000000000000000000, 0.000000000000000000, 0.000000000000000000 ) ) ;
#15910=CARTESIAN_POINT ( 'NONE',  ( 108.0529998774959353, -18.83254716784343330, 4.756559617914289717 ) ) ;
#15911=EDGE_LOOP ( 'NONE', ( #28758, #8511, #15066, #23238 ) ) ;
#15917=ORIENTED_EDGE ( 'NONE', *, *, #10856, .T. ) ;
#15920=EDGE_CURVE ( 'NONE', #7812, #32996, #15474, .T. ) ;
#15922=DIRECTION ( 'NONE',  ( 1.000000000000000000, 0.000000000000000000, 0.000000000000000000 ) ) ;
#15926=CARTESIAN_POINT ( 'NONE',  ( 22.01492382912217849, -21.80158502930435915, -1.372788961214118197 ) ) ;
#15931=CARTESIAN_POINT ( 'NONE',  ( 8.519413124347837041, -14.04790626066225023, 1.499999999999999334 ) ) ;
#15942=CARTESIAN_POINT ( 'NONE',  ( -15.06907680150159656, -25.68921844201283022, 1.340913934978426258 ) ) ;
#15945=CARTESIAN_POINT ( 'NONE',  ( 1.867614357912406930, -10.11604448560295744, -1.500000000000000444 ) ) ;
#15957=VERTEX_POINT ( 'NONE', #16308 ) ;
#15960=LINE ( 'NONE', #21011, #21867 ) ;
#15962=ORIENTED_EDGE ( 'NONE', *, *, #13779, .F. ) ;
#15964=CARTESIAN_POINT ( 'NONE',  ( 42.13509523489886277, -21.36880892310108138, -5.485967528433937979 ) ) ;
#15979=CARTESIAN_POINT ( 'NONE',  ( 8.789577373539158245, -11.69574158658721252, 1.500000000000000000 ) ) ;
#16000=EDGE_LOOP ( 'NONE', ( #20962, #17336 ) ) ;
#16012=CARTESIAN_POINT ( 'NONE',  ( 21.32535692059145660, -21.82495604402121003, -1.318256435726663955 ) ) ;
#16014=ADVANCED_FACE ( 'NONE', ( #13145 ), #18646, .T. ) ;
#16016=EDGE_CURVE ( 'NONE', #29157, #18318, #26596, .T. ) ;
#16025=ORIENTED_EDGE ( 'NONE', *, *, #17942, .T. ) ;
#16027=CYLINDRICAL_SURFACE ( 'NONE', #17228, 0.5000000000000000000 ) ;
#16030=CARTESIAN_POINT ( 'NONE',  ( 0.8232120717395272624, -3.227314771018384487, -1.762270855091927491 ) ) ;
#16035=CARTESIAN_POINT ( 'NONE',  ( 6.069864835170823980, -18.63409169915096442, 1.499999999999999112 ) ) ;
#16039=CARTESIAN_POINT ( 'NONE',  ( 24.13073845333548206, -17.43243825926032642, 1.517345177934881439 ) ) ;
#16046=CYLINDRICAL_SURFACE ( 'NONE', #28916, 0.5000000000000004441 ) ;
#16059=ADVANCED_FACE ( 'NONE', ( #8453 ), #3175, .T. ) ;
#16062=CARTESIAN_POINT ( 'NONE',  ( 107.9488651208191357, -17.33303257717642154, 4.540600388780822172 ) ) ;
#16064=AXIS2_PLACEMENT_3D ( 'NONE', #20972, #31189, #9012 ) ;
#16081=CARTESIAN_POINT ( 'NONE',  ( -3.765825760583550785, -9.391035046880782389, -1.743616693177291843 ) ) ;
#16084=CARTESIAN_POINT ( 'NONE',  ( 20.69346795579692255, -16.15118080677321188, -1.499999999998890887 ) ) ;
#16085=CARTESIAN_POINT ( 'NONE',  ( 107.9802354097229369, -17.78475693344107711, -4.325021386167422044 ) ) ;
#16088=VECTOR ( 'NONE', #18467, 1000.000000000000000 ) ;
#16090=CARTESIAN_POINT ( 'NONE',  ( 0.8609591700481805665, -8.439992987522430212, 1.499999999999999334 ) ) ;
#16105=AXIS2_PLACEMENT_3D ( 'NONE', #6360, #20944, #31641 ) ;
#16110=CARTESIAN_POINT ( 'NONE',  ( 0.5630814792739097241, -7.170012529492013620, -1.499999999999999556 ) ) ;
#16115=CARTESIAN_POINT ( 'NONE',  ( 25.38393466668145493, -17.54878733605299601, -1.232996826557628545 ) ) ;
#16119=CARTESIAN_POINT ( 'NONE',  ( -1.331261126404138517, -14.27417440010677652, -0.9788672205760856615 ) ) ;
#16120=ORIENTED_EDGE ( 'NONE', *, *, #14839, .F. ) ;
#16121=ORIENTED_EDGE ( 'NONE', *, *, #8507, .T. ) ;
#16137=CARTESIAN_POINT ( 'NONE',  ( 108.0271851702406138, -18.46082180526434513, 4.398261384118815620 ) ) ;
#16139=CARTESIAN_POINT ( 'NONE',  ( -2.767073886773233848, -0.6621507858625382825, -1.748408842879326075 ) ) ;
#16140=DIRECTION ( 'NONE',  ( -0.000000000000000000, -0.000000000000000000, -1.000000000000000000 ) ) ;
#16143=DIRECTION ( 'NONE',  ( -0.000000000000000000, -0.000000000000000000, -1.000000000000000000 ) ) ;
#16144=CIRCLE ( 'NONE', #3871, 8.500000000000000000 ) ;
#16145=DIRECTION ( 'NONE',  ( -1.000000000000000000, 0.000000000000000000, 0.000000000000000000 ) ) ;
#16148=AXIS2_PLACEMENT_3D ( 'NONE', #26114, #3875, #15904 ) ;
#16159=CARTESIAN_POINT ( 'NONE',  ( 7.845473912040171527, -1.949903631124794146, 1.500000000000000000 ) ) ;
#16164=CARTESIAN_POINT ( 'NONE',  ( 0.2476201786951250650, -6.180873974445452390, 1.500000000000142997 ) ) ;
#16178=CIRCLE ( 'NONE', #25287, 0.4499999999999999001 ) ;
#16181=CARTESIAN_POINT ( 'NONE',  ( 1.565787006715318563, -2.348723853601413669, 0.9788672205888330202 ) ) ;
#16182=ORIENTED_EDGE ( 'NONE', *, *, #27552, .F. ) ;
#16190=EDGE_CURVE ( 'NONE', #30204, #2520, #14526, .T. ) ;
#16194=CARTESIAN_POINT ( 'NONE',  ( 0.004027955751649570440, -11.10248303872730169, 5.485967528433933538 ) ) ;
#16195=EDGE_CURVE ( 'NONE', #10544, #7488, #4354, .T. ) ;
#16201=CARTESIAN_POINT ( 'NONE',  ( 107.4763673390317962, -17.74216696756428391, -5.015857065170183482 ) ) ;
#16213=CARTESIAN_POINT ( 'NONE',  ( 24.39659513448100725, -17.41072360183587264, -1.416990234759457401 ) ) ;
#16216=CARTESIAN_POINT ( 'NONE',  ( -3.103992766986577667, 8.326672684866362132E-14, -1.052556072988602986 ) ) ;
#16217=ORIENTED_EDGE ( 'NONE', *, *, #2811, .F. ) ;
#16222=CARTESIAN_POINT ( 'NONE',  ( 1.635938383118674677, -1.437486021841400730, -1.758786398149086327 ) ) ;
#16230=CARTESIAN_POINT ( 'NONE',  ( 5.388021529391686215, -18.36754117723517510, 1.500000000000001332 ) ) ;
#16236=EDGE_CURVE ( 'NONE', #593, #21890, #4603, .T. ) ;
#16244=DIRECTION ( 'NONE',  ( 1.000000000000000000, 0.000000000000000000, 0.000000000000000000 ) ) ;
#16267=CARTESIAN_POINT ( 'NONE',  ( 9.126991455997314873, -11.32614230997805471, -1.500000000000000000 ) ) ;
#16268=CARTESIAN_POINT ( 'NONE',  ( 107.9476224718558939, -17.31513874123385932, -4.492091147515819394 ) ) ;
#16274=CARTESIAN_POINT ( 'NONE',  ( 2.913020537602753368, 0.09936728819756490694, 1.050862340634253211 ) ) ;
#16276=CARTESIAN_POINT ( 'NONE',  ( 107.8806307222008627, -16.35047421165092985, -1.384330804613826293 ) ) ;
#16283=DIRECTION ( 'NONE',  ( 1.000000000000000000, 0.000000000000000000, 0.000000000000000000 ) ) ;
#16285=CARTESIAN_POINT ( 'NONE',  ( 15.98710106916323781, -15.99254912437086240, -1.500000000000000222 ) ) ;
#16302=EDGE_CURVE ( 'NONE', #22652, #11, #6223, .T. ) ;
#16308=CARTESIAN_POINT ( 'NONE',  ( -31.35000000000000142, -10.96966150227469328, 4.500000000000000888 ) ) ;
#16313=CARTESIAN_POINT ( 'NONE',  ( 23.12748563068209151, -21.92617699668438291, 1.175810100957690008 ) ) ;
#16324=CARTESIAN_POINT ( 'NONE',  ( 6.669411210322924610, -6.378078458905314108, 1.500000000000000000 ) ) ;
#16328=CARTESIAN_POINT ( 'NONE',  ( 0.9576657675042646867, -9.536988708453836949, 1.767396803601621214 ) ) ;
#16335=ADVANCED_FACE ( 'NONE', ( #21739 ), #31947, .T. ) ;
#16338=DIRECTION ( 'NONE',  ( 1.000000000000000000, 0.000000000000000000, 0.000000000000000000 ) ) ;
#16346=B_SPLINE_CURVE_WITH_KNOTS ( 'NONE', 3,
 ( #8498, #10862, #31586, #5828, #8839, #23882 ),
 .UNSPECIFIED., .F., .F.,
 ( 4, 2, 4 ),
 ( -1.393633244722569653E-05, 0.0003803243175954409668, 0.0007745849676381076979 ),
 .UNSPECIFIED. ) ;
#16350=CARTESIAN_POINT ( 'NONE',  ( 73.45519860865672968, -21.36028973287419674, 4.522129901861159595 ) ) ;
#16358=CARTESIAN_POINT ( 'NONE',  ( 3.569153896158649086, -0.01695480042954932223, -1.144240241240434441 ) ) ;
#16361=CARTESIAN_POINT ( 'NONE',  ( -15.12340757463330476, -27.93932300454937590, -1.000000000000000000 ) ) ;
#16366=DIRECTION ( 'NONE',  ( 0.000000000000000000, 0.000000000000000000, 1.000000000000000000 ) ) ;
#16374=CARTESIAN_POINT ( 'NONE',  ( 0.2073616445840893718, -5.485889181658371250, -1.769987010377963355 ) ) ;
#16376=VERTEX_POINT ( 'NONE', #1518 ) ;
#16380=LINE ( 'NONE', #26100, #29561 ) ;
#16386=FACE_OUTER_BOUND ( 'NONE', #29129, .T. ) ;
#16387=CARTESIAN_POINT ( 'NONE',  ( -3.562847368662853231, -10.36282323065911370, -1.499999999999920286 ) ) ;
#16392=CARTESIAN_POINT ( 'NONE',  ( 20.58436699794813052, -21.58689779341593251, 1.578270943419565420 ) ) ;
#16412=CARTESIAN_POINT ( 'NONE',  ( 12.23764924856644143, -13.51220073293806223, 1.000000000000000000 ) ) ;
#16414=CYLINDRICAL_SURFACE ( 'NONE', #24087, 0.5000000000000007772 ) ;
#16415=CARTESIAN_POINT ( 'NONE',  ( 8.486535498731882399, -10.66169397748177161, -1.000000000000000000 ) ) ;
#16420=CARTESIAN_POINT ( 'NONE',  ( 17.97422212134408781, -19.86246923125032282, 4.522129901861158707 ) ) ;
#16425=FACE_OUTER_BOUND ( 'NONE', #31010, .T. ) ;
#16436=ORIENTED_EDGE ( 'NONE', *, *, #17503, .T. ) ;
#16437=CARTESIAN_POINT ( 'NONE',  ( 24.55820472632857232, -17.37661330403883397, -1.293157874817485231 ) ) ;
#16451=CARTESIAN_POINT ( 'NONE',  ( 107.5622803136338490, -18.99091296950214769, 4.502146529677950149 ) ) ;
#16454=CARTESIAN_POINT ( 'NONE',  ( -15.12340757463330654, -27.93932300454937590, -1.000000000000000000 ) ) ;
#16465=CARTESIAN_POINT ( 'NONE',  ( 107.5818156268159669, -17.35116702072363637, 4.522076865625765940 ) ) ;
#16468=CARTESIAN_POINT ( 'NONE',  ( 7.192400643299417418, -7.644771086296574758, 1.000000000000000000 ) ) ;
#16469=ORIENTED_EDGE ( 'NONE', *, *, #7132, .F. ) ;
#16473=CARTESIAN_POINT ( 'NONE',  ( 0.3472807118842683449, -7.723390615030998774, 1.499999999999999778 ) ) ;
#16482=ORIENTED_EDGE ( 'NONE', *, *, #14434, .F. ) ;
#16485=CARTESIAN_POINT ( 'NONE',  ( 23.24965665534714176, -21.93932291342295215, -1.034606501595533024 ) ) ;
#16497=CARTESIAN_POINT ( 'NONE',  ( 42.13509523493340936, -21.36880892310108493, 5.485967528433933538 ) ) ;
#16508=ORIENTED_EDGE ( 'NONE', *, *, #2458, .T. ) ;
#16516=CARTESIAN_POINT ( 'NONE',  ( 7.211599578357735574, -7.804913758300354054, -1.000000000000000222 ) ) ;
#16517=AXIS2_PLACEMENT_3D ( 'NONE', #7604, #27660, #4940 ) ;
#16526=CARTESIAN_POINT ( 'NONE',  ( 2.053744806908957887, -0.9196371613258790267, -1.500000000000420552 ) ) ;
#16532=DIRECTION ( 'NONE',  ( -0.000000000000000000, -1.000000000000000000, -0.000000000000000000 ) ) ;
#16541=AXIS2_PLACEMENT_3D ( 'NONE', #19028, #21541, #11648 ) ;
#16543=DIRECTION ( 'NONE',  ( 1.000000000000000000, 0.000000000000000000, 0.000000000000000000 ) ) ;
#16545=AXIS2_PLACEMENT_3D ( 'NONE', #22306, #26997, #9081 ) ;
#16552=CARTESIAN_POINT ( 'NONE',  ( 21.07900179210102820, -21.69205259094532678, 1.492586111083458400 ) ) ;
#16559=FACE_BOUND ( 'NONE', #13831, .T. ) ;
#16574=CARTESIAN_POINT ( 'NONE',  ( 108.1106105794459609, -19.66212694419082396, -1.922248489706470664 ) ) ;
#16575=CARTESIAN_POINT ( 'NONE',  ( 9.851448551969891554, -11.91728849095333231, -1.500000000000000000 ) ) ;
#16576=CARTESIAN_POINT ( 'NONE',  ( 107.4493004345435878, -17.34926456629034419, -4.492266965380428800 ) ) ;
#16579=VECTOR ( 'NONE', #25075, 1000.000000000000000 ) ;
#16587=CARTESIAN_POINT ( 'NONE',  ( -17.35000000000000142, -10.96966150227469505, -11.50000000000000000 ) ) ;
#16591=CARTESIAN_POINT ( 'NONE',  ( 107.4362021328091288, -17.16097444018121365, -4.113685213696737897 ) ) ;
#16595=VECTOR ( 'NONE', #17656, 1000.000000000000000 ) ;
#16598=CARTESIAN_POINT ( 'NONE',  ( 17.39502519978889694, -21.04076415203780925, 1.751145182513948351 ) ) ;
#16599=ORIENTED_EDGE ( 'NONE', *, *, #4653, .T. ) ;
#16600=DIRECTION ( 'NONE',  ( 0.9151824489413823427, -0.4030398059120888776, 0.000000000000000000 ) ) ;
#16601=ORIENTED_EDGE ( 'NONE', *, *, #16628, .T. ) ;
#16604=CARTESIAN_POINT ( 'NONE',  ( 24.76851591958248378, -17.41692718791852812, -1.262548836151033305 ) ) ;
#16619=CARTESIAN_POINT ( 'NONE',  ( 108.0598809612459519, -18.93163306209645214, 4.567750811147567092 ) ) ;
#16624=CARTESIAN_POINT ( 'NONE',  ( 110.4915906369627123, -18.78144465615449832, -4.522129901861166701 ) ) ;
#16628=EDGE_CURVE ( 'NONE', #15401, #22172, #24931, .T. ) ;
#16641=CARTESIAN_POINT ( 'NONE',  ( 8.060276135842133982, -2.738905749622256636, 1.499999999999713785 ) ) ;
#16643=CARTESIAN_POINT ( 'NONE',  ( 13.10266514559061868, -14.23637329403187479, -1.500000000000000000 ) ) ;
#16648=CARTESIAN_POINT ( 'NONE',  ( 3.334879154417976554, -11.42275455914650095, 1.500000000000000000 ) ) ;
#16650=DIRECTION ( 'NONE',  ( 0.000000000000000000, 0.000000000000000000, 1.000000000000000000 ) ) ;
#16657=CARTESIAN_POINT ( 'NONE',  ( 24.07542780979855834, -17.38801686517327738, -1.438486003925340428 ) ) ;
#16666=AXIS2_PLACEMENT_3D ( 'NONE', #6417, #6118, #31859 ) ;
#16668=AXIS2_PLACEMENT_3D ( 'NONE', #19617, #29815, #24797 ) ;
#16685=CARTESIAN_POINT ( 'NONE',  ( 24.94969606499759962, -17.50686502442625425, -1.454450177773842112 ) ) ;
#16701=CIRCLE ( 'NONE', #31666, 0.5000000000000008882 ) ;
#16708=ORIENTED_EDGE ( 'NONE', *, *, #16190, .F. ) ;
#16712=CARTESIAN_POINT ( 'NONE',  ( 1.947447778977702049, -0.8602978363041573484, -1.758031988188919037 ) ) ;
#16714=ORIENTED_EDGE ( 'NONE', *, *, #12328, .T. ) ;
#16734=CARTESIAN_POINT ( 'NONE',  ( -4.099836581868715690, -5.441267727784081742, -1.745641626744263153 ) ) ;
#16745=CARTESIAN_POINT ( 'NONE',  ( 24.22349034905825960, -17.32906192875332962, 1.351230503573712216 ) ) ;
#16759=CARTESIAN_POINT ( 'NONE',  ( -2.596426400646765220, -12.68075645936657381, -1.499999999999999778 ) ) ;
#16766=CARTESIAN_POINT ( 'NONE',  ( 7.166310626576994025, -7.340520188510355482, -1.000000000000000000 ) ) ;
#16767=CARTESIAN_POINT ( 'NONE',  ( 107.5607856375281557, -18.96928505737806248, -4.559234559040556967 ) ) ;
#16778=CARTESIAN_POINT ( 'NONE',  ( 107.4500373638804120, -17.36019379023677089, -4.522129901861164036 ) ) ;
#16789=ORIENTED_EDGE ( 'NONE', *, *, #1620, .F. ) ;
#16796=EDGE_CURVE ( 'NONE', #9413, #15401, #3064, .T. ) ;
#16806=CARTESIAN_POINT ( 'NONE',  ( 6.448894291894883501, -17.04229596238074151, -4.522129901861166701 ) ) ;
#16808=DIRECTION ( 'NONE',  ( -0.000000000000000000, -0.000000000000000000, 1.000000000000000000 ) ) ;
#16817=LINE ( 'NONE', #24989, #23681 ) ;
#16818=CARTESIAN_POINT ( 'NONE',  ( 0.9232102171129904500, 0.000000000000000000, 4.522129901861156931 ) ) ;
#16820=ORIENTED_EDGE ( 'NONE', *, *, #22766, .T. ) ;
#16821=CARTESIAN_POINT ( 'NONE',  ( 14.08105513877552895, -14.60666186089152419, -1.499999999999999556 ) ) ;
#16823=CARTESIAN_POINT ( 'NONE',  ( 0.1512386650912407315, -7.218081413057891638, 1.774506574461718111 ) ) ;
#16826=CARTESIAN_POINT ( 'NONE',  ( -2.807368950796196305, -12.37532080748741237, 1.500000000000000000 ) ) ;
#16830=CARTESIAN_POINT ( 'NONE',  ( -2.617344628312510135, 0.000000000000000000, 1.468739241856748867 ) ) ;
#16831=CARTESIAN_POINT ( 'NONE',  ( 21.03177542174510606, -17.18603084754150601, -1.753176640694676047 ) ) ;
#16835=ORIENTED_EDGE ( 'NONE', *, *, #22667, .T. ) ;
#16843=CARTESIAN_POINT ( 'NONE',  ( 3.554613218822866738, -15.76807188677689275, -4.522129901861166701 ) ) ;
#16848=SPHERICAL_SURFACE ( 'NONE', #13990, 0.5000000000000000000 ) ;
#16851=B_SPLINE_CURVE_WITH_KNOTS ( 'NONE', 3,
 ( #9930, #10584, #25134, #20145 ),
 .UNSPECIFIED., .F., .F.,
 ( 4, 4 ),
 ( 0.000000000000000000, 0.0001149031832728065387 ),
 .UNSPECIFIED. ) ;
#16852=CYLINDRICAL_SURFACE ( 'NONE', #11918, 0.5000000000000000000 ) ;
#16862=ORIENTED_EDGE ( 'NONE', *, *, #10582, .T. ) ;
#16864=B_SPLINE_CURVE_WITH_KNOTS ( 'NONE', 3,
 ( #25117, #12423, #4087, #4233, #19475, #32351, #11750, #19624, #9253, #29822, #6898, #17092, #4423, #24806, #8061, #23291, #5586, #12590, #541, #7904, #12738, #15261, #25464, #2573, #27985, #28287, #2420, #5085, #22944, #56, #25971, #27796, #10244, #3079 ),
 .UNSPECIFIED., .F., .F.,
 ( 4, 2, 2, 2, 2, 2, 2, 2, 2, 2, 2, 2, 2, 2, 2, 2, 4 ),
 ( -5.999999999868128345E-08, 0.001865929031388419103, 0.003731918062776836981, 0.005597907094165255511, 0.006530901609859464559, 0.007463896125553672739, 0.008396890641247883522, 0.009329885156942092569, 0.01119587418833051587, 0.01306186321971893743, 0.01399485773541314995, 0.01492785225110736247, 0.01679384128249578750, 0.01865983031388421601, 0.02239180837666106955, 0.02612378643943793349, 0.02985576450221478703 ),
 .UNSPECIFIED. ) ;
#16873=CARTESIAN_POINT ( 'NONE',  ( 1.138845227633290769, -9.034331793438131086, -1.500000000000000444 ) ) ;
#16877=DIRECTION ( 'NONE',  ( -1.000000000000000000, 0.000000000000000000, 0.000000000000000000 ) ) ;
#16879=DIRECTION ( 'NONE',  ( 0.9873162094020069279, -0.1587661886298609715, 2.857460637125401170E-14 ) ) ;
#16881=CARTESIAN_POINT ( 'NONE',  ( -15.01523975624633067, -21.93625144122058757, 1.063946347602459985 ) ) ;
#16888=CYLINDRICAL_SURFACE ( 'NONE', #19368, 6.000000000000001776 ) ;
#16913=CARTESIAN_POINT ( 'NONE',  ( -4.436748700219182773, -8.316102859869440422, -1.500000000000000444 ) ) ;
#16917=CARTESIAN_POINT ( 'NONE',  ( -2.767073886773234292, -0.6621507858625358400, 1.748408842879327407 ) ) ;
#16918=CARTESIAN_POINT ( 'NONE',  ( 7.931701155947533444, -9.929036424221253654, -1.000000000000000000 ) ) ;
#16919=CARTESIAN_POINT ( 'NONE',  ( 108.0159102312815378, -18.29846548910601101, -4.592014164311896351 ) ) ;
#16921=CARTESIAN_POINT ( 'NONE',  ( 0.000000000000000000, 0.000000000000000000, 4.137834579201376428 ) ) ;
#16923=B_SPLINE_CURVE_WITH_KNOTS ( 'NONE', 3,
 ( #3205, #31302, #26101, #5566, #15747, #3059, #8375, #13215, #31, #12721 ),
 .UNSPECIFIED., .F., .F.,
 ( 4, 2, 2, 2, 4 ),
 ( 0.000000000000000000, 0.0003402153055305003082, 0.0006804306110610006163, 0.001020645916591500979, 0.001360861222122001233 ),
 .UNSPECIFIED. ) ;
#16926=CARTESIAN_POINT ( 'NONE',  ( 24.73076886165253185, -17.48512500876796238, -1.500000000000000666 ) ) ;
#16934=EDGE_CURVE ( 'NONE', #31320, #1139, #30237, .T. ) ;
#16935=CARTESIAN_POINT ( 'NONE',  ( 2.995361005316267811, -0.2432974174152454927, -1.434016190628302212 ) ) ;
#16937=CARTESIAN_POINT ( 'NONE',  ( -17.45597128428593336, -27.93932300454937590, 10.99999999999999822 ) ) ;
#16944=VERTEX_POINT ( 'NONE', #20537 ) ;
#16947=ORIENTED_EDGE ( 'NONE', *, *, #187, .T. ) ;
#16957=CARTESIAN_POINT ( 'NONE',  ( 13.54302414779168373, -18.70685303420762935, -5.485967528433938867 ) ) ;
#16959=CARTESIAN_POINT ( 'NONE',  ( -50.60000000000000142, -10.96966150227468972, 7.500000000000000000 ) ) ;
#16972=DIRECTION ( 'NONE',  ( 1.000000000000000000, 0.000000000000000000, 0.000000000000000000 ) ) ;
#16975=CARTESIAN_POINT ( 'NONE',  ( 15.99612907445991183, -15.99421271805945288, 1.500000000000000000 ) ) ;
#16986=CARTESIAN_POINT ( 'NONE',  ( 23.18045508973794711, -21.93188832360385732, -1.140730425198753117 ) ) ;
#16988=EDGE_CURVE ( 'NONE', #11582, #4684, #21453, .T. ) ;
#17014=CARTESIAN_POINT ( 'NONE',  ( 7.331643324767637360, -8.426631371196835474, -0.9999999999999997780 ) ) ;
#17015=DIRECTION ( 'NONE',  ( 0.000000000000000000, 0.000000000000000000, 1.000000000000000000 ) ) ;
#17021=CARTESIAN_POINT ( 'NONE',  ( 10.87894471766993654, -15.23741606896315837, -1.754278687356615851 ) ) ;
#17027=CARTESIAN_POINT ( 'NONE',  ( 108.0633640349745548, -18.98178845726371122, -3.316617650382913229 ) ) ;
#17035=EDGE_CURVE ( 'NONE', #2302, #30719, #29448, .T. ) ;
#17041=VERTEX_POINT ( 'NONE', #12798 ) ;
#17050=ORIENTED_EDGE ( 'NONE', *, *, #8631, .F. ) ;
#17061=CARTESIAN_POINT ( 'NONE',  ( 107.4500373638809947, -17.36019379023286646, 4.522129901861156931 ) ) ;
#17062=ORIENTED_EDGE ( 'NONE', *, *, #7854, .T. ) ;
#17065=CARTESIAN_POINT ( 'NONE',  ( -3.729005870813945744, -1.848196750359484497, 1.499999999999999112 ) ) ;
#17066=CARTESIAN_POINT ( 'NONE',  ( 8.305304940806125913, -2.146676032413550761, -1.000000000000000000 ) ) ;
#17067=CARTESIAN_POINT ( 'NONE',  ( 108.0129365102922918, -18.25564464663832354, -5.138066728956478535 ) ) ;
#17079=CIRCLE ( 'NONE', #19219, 0.5000000000000004441 ) ;
#17083=EDGE_CURVE ( 'NONE', #21390, #4392, #18120, .T. ) ;
#17084=FACE_OUTER_BOUND ( 'NONE', #16000, .T. ) ;
#17085=DIRECTION ( 'NONE',  ( 0.000000000000000000, 0.000000000000000000, -1.000000000000000000 ) ) ;
#17090=CARTESIAN_POINT ( 'NONE',  ( 3.406359441062986715, 0.6647459039674445958, -0.7949826693599028049 ) ) ;
#17092=CARTESIAN_POINT ( 'NONE',  ( 7.168240634028618885, -7.372423425476283931, 1.000000000000000222 ) ) ;
#17094=AXIS2_PLACEMENT_3D ( 'NONE', #18243, #5567, #25951 ) ;
#17107=CARTESIAN_POINT ( 'NONE',  ( -4.365512850963738423, -6.230587388684557304, 1.500000000000000000 ) ) ;
#17111=EDGE_CURVE ( 'NONE', #1705, #24091, #26522, .T. ) ;
#17121=EDGE_CURVE ( 'NONE', #23722, #26388, #18542, .T. ) ;
#17123=VECTOR ( 'NONE', #16140, 1000.000000000000000 ) ;
#17127=VECTOR ( 'NONE', #22731, 1000.000000000000000 ) ;
#17134=CARTESIAN_POINT ( 'NONE',  ( 22.61755859552698311, -21.90439257241343185, -1.185952627206551035 ) ) ;
#17140=ORIENTED_EDGE ( 'NONE', *, *, #26153, .F. ) ;
#17145=B_SPLINE_CURVE_WITH_KNOTS ( 'NONE', 3,
 ( #28001, #5100, #22807, #15427, #73, #10261, #5601, #28150, #2948, #17608, #25478, #33012, #7772, #25638, #30998, #27812, #10587, #25326, #4928, #2435, #20792, #22958, #5252, #8080, #2753, #10084, #12928, #12753, #15609, #23151, #15783, #20646, #23450, #23307 ),
 .UNSPECIFIED., .F., .F.,
 ( 4, 2, 2, 2, 2, 2, 2, 2, 2, 2, 2, 2, 2, 2, 2, 2, 4 ),
 ( 0.000000000000000000, 0.001968049515999117927, 0.003936099031998235853, 0.004920123789997794816, 0.005904148547997353780, 0.006888173305996912743, 0.007872198063996471706, 0.009840247579995589633, 0.01180829709599470756, 0.01279232185399426652, 0.01377634661199382549, 0.01574439612799293994, 0.01771244564399205440, 0.01968049515999117233, 0.02361659419198941165, 0.02755269322398765097, 0.03148879225598588683 ),
 .UNSPECIFIED. ) ;
#17147=CARTESIAN_POINT ( 'NONE',  ( -3.727408454243656077, -1.844569501927837862, 1.499999999999999778 ) ) ;
#17148=VECTOR ( 'NONE', #30345, 1000.000000000000000 ) ;
#17159=DIRECTION ( 'NONE',  ( -0.000000000000000000, 0.000000000000000000, 1.000000000000000000 ) ) ;
#17190=CONICAL_SURFACE ( 'NONE', #2803, 9.500000000000003553, 0.1919862177193767117 ) ;
#17194=EDGE_LOOP ( 'NONE', ( #5841, #2137 ) ) ;
#17204=AXIS2_PLACEMENT_3D ( 'NONE', #15248, #42, #25793 ) ;
#17211=CARTESIAN_POINT ( 'NONE',  ( 2.040402999919812110, -10.88381885264265492, -1.762032186063900108 ) ) ;
#17212=CARTESIAN_POINT ( 'NONE',  ( 0.2678094507063553675, -7.640026513854723866, 1.500000000000000444 ) ) ;
#17222=CARTESIAN_POINT ( 'NONE',  ( 21.04767255914985213, -17.06392231637775225, 1.500000000000857314 ) ) ;
#17228=AXIS2_PLACEMENT_3D ( 'NONE', #690, #8851, #11188 ) ;
#17230=CARTESIAN_POINT ( 'NONE',  ( 14.56325452644739649, -20.55228321368884892, -1.750894134686189041 ) ) ;
#17258=CARTESIAN_POINT ( 'NONE',  ( 2.040255037894282530, -16.78712277524563490, -1.499999999999999334 ) ) ;
#17260=AXIS2_PLACEMENT_3D ( 'NONE', #4486, #10475, #8302 ) ;
#17262=CARTESIAN_POINT ( 'NONE',  ( 2.655375060943963472, -12.56041828387959747, -1.000000000000000000 ) ) ;
#17267=CARTESIAN_POINT ( 'NONE',  ( 7.637044425070966369, -3.948987408479414096, -1.500000000000000888 ) ) ;
#17268=CARTESIAN_POINT ( 'NONE',  ( 107.5605230035171189, -18.96547504619710267, -4.568439005055447311 ) ) ;
#17285=FACE_OUTER_BOUND ( 'NONE', #24140, .T. ) ;
#17289=ORIENTED_EDGE ( 'NONE', *, *, #6392, .T. ) ;
#17309=AXIS2_PLACEMENT_3D ( 'NONE', #21204, #1133, #23712 ) ;
#17310=CARTESIAN_POINT ( 'NONE',  ( 73.45519860865672968, -21.36028973287419319, -4.522129901861166701 ) ) ;
#17320=ORIENTED_EDGE ( 'NONE', *, *, #21117, .F. ) ;
#17329=CARTESIAN_POINT ( 'NONE',  ( 19.80507712518364372, -16.61824031234324295, 1.500000000000000666 ) ) ;
#17334=CARTESIAN_POINT ( 'NONE',  ( 9.096376384877638444, -0.1528062924499160868, -1.364612494264896281 ) ) ;
#17336=ORIENTED_EDGE ( 'NONE', *, *, #3013, .T. ) ;
#17337=DIRECTION ( 'NONE',  ( 0.000000000000000000, 0.000000000000000000, -1.000000000000000000 ) ) ;
#17345=CARTESIAN_POINT ( 'NONE',  ( 0.9232102171129938917, 0.000000000000000000, -4.522129901861164925 ) ) ;
#17349=CARTESIAN_POINT ( 'NONE',  ( 107.5617723795401872, -18.98359893170738744, -4.522129901861166701 ) ) ;
#17357=CARTESIAN_POINT ( 'NONE',  ( -23.35000000000000142, -10.96966150227469505, 4.000000000000000000 ) ) ;
#17373=ADVANCED_FACE ( 'NONE', ( #14132 ), #27010, .F. ) ;
#17381=CARTESIAN_POINT ( 'NONE',  ( 4.139048519582217089, -11.97498679546279199, -1.500000000000001332 ) ) ;
#17382=CARTESIAN_POINT ( 'NONE',  ( -0.7739934281325318022, -8.972773999336984829, 4.522129901861157819 ) ) ;
#17389=CARTESIAN_POINT ( 'NONE',  ( 23.72853298629391006, -17.37454644214624722, 1.486007232661737065 ) ) ;
#17394=LINE ( 'NONE', #27587, #23742 ) ;
#17397=CARTESIAN_POINT ( 'NONE',  ( 15.97646417262808072, -20.81271057983140338, -1.751026346894440255 ) ) ;
#17407=CARTESIAN_POINT ( 'NONE',  ( -31.85000000000000497, -10.96966150227469505, 4.500000000000000888 ) ) ;
#17411=CARTESIAN_POINT ( 'NONE',  ( 0.000000000000000000, 0.000000000000000000, -1.500000000000000000 ) ) ;
#17415=CARTESIAN_POINT ( 'NONE',  ( -53.12500000000000000, -10.96966150227468972, 7.500000000000000000 ) ) ;
#17417=CARTESIAN_POINT ( 'NONE',  ( 107.3476768466457401, -15.88628154573096651, 1.500000000000000000 ) ) ;
#17419=CARTESIAN_POINT ( 'NONE',  ( 107.5617944031221640, -18.98359742639815551, 4.522129901861158707 ) ) ;
#17423=CARTESIAN_POINT ( 'NONE',  ( 107.9850792167139275, -17.85450654912270707, -4.471870475959497604 ) ) ;
#17425=CARTESIAN_POINT ( 'NONE',  ( 22.00639167669143603, -21.80013755708273848, 1.500000000000000000 ) ) ;
#17428=CARTESIAN_POINT ( 'NONE',  ( 24.55229918076951989, -17.45956433520428774, -1.484437869256384213 ) ) ;
#17429=LINE ( 'NONE', #22440, #661 ) ;
#17439=CARTESIAN_POINT ( 'NONE',  ( 3.238981242682563710, 0.6371288015966571905, -1.059614580210906043 ) ) ;
#17444=FACE_OUTER_BOUND ( 'NONE', #5134, .T. ) ;
#17451=CARTESIAN_POINT ( 'NONE',  ( 0.5309851148689820333, -4.399114163800174282, 1.500000000000000000 ) ) ;
#17457=CARTESIAN_POINT ( 'NONE',  ( 107.9497830788478581, -17.34625094442601068, -4.563380564795206595 ) ) ;
#17458=CARTESIAN_POINT ( 'NONE',  ( 25.48003136492429377, -17.55790038815346676, 1.043845799725922951 ) ) ;
#17466=ORIENTED_EDGE ( 'NONE', *, *, #4119, .T. ) ;
#17474=CARTESIAN_POINT ( 'NONE',  ( 107.9988559483833370, -18.05288805794269535, 4.627775613152216749 ) ) ;
#17476=CARTESIAN_POINT ( 'NONE',  ( 12.16199335750468258, -15.44738821017505259, 1.500000000000415668 ) ) ;
#17478=FACE_OUTER_BOUND ( 'NONE', #19545, .T. ) ;
#17482=( BOUNDED_CURVE ( )  B_SPLINE_CURVE ( 3, ( #13753, #15942, #26339, #923 ),
 .UNSPECIFIED., .F., .F. ) 
 B_SPLINE_CURVE_WITH_KNOTS ( ( 4, 4 ),
 ( 4.712388980384687009, 6.091199089460269889 ),
 .UNSPECIFIED. ) 
 CURVE ( )  GEOMETRIC_REPRESENTATION_ITEM ( )  RATIONAL_B_SPLINE_CURVE ( ( 1.000000000000000000, 0.8477497222584666758, 0.8477497222584666758, 1.000000000000000000 ) ) 
 REPRESENTATION_ITEM ( '' )  );
#17483=CARTESIAN_POINT ( 'NONE',  ( 108.0270953819671291, -18.45952887646314977, -4.403827697248457795 ) ) ;
#17488=CARTESIAN_POINT ( 'NONE',  ( 21.63953834185432257, -21.76333864698586140, -1.486663794871770916 ) ) ;
#17503=EDGE_CURVE ( 'NONE', #6111, #6331, #4764, .T. ) ;
#17505=ORIENTED_EDGE ( 'NONE', *, *, #16796, .T. ) ;
#17510=CARTESIAN_POINT ( 'NONE',  ( 2.281627749324421917, -0.2935656086769610207, 1.757435426329174044 ) ) ;
#17527=CARTESIAN_POINT ( 'NONE',  ( 3.335187914516625440, -11.42298369410695535, -1.500000000000000444 ) ) ;
#17534=CARTESIAN_POINT ( 'NONE',  ( -32.18314092741314880, -27.93932300454937590, -1.500000000000000000 ) ) ;
#17535=ORIENTED_EDGE ( 'NONE', *, *, #657, .T. ) ;
#17536=CARTESIAN_POINT ( 'NONE',  ( 23.86874014608549288, -17.38228585591217623, 1.471223822905279199 ) ) ;
#17544=CARTESIAN_POINT ( 'NONE',  ( -0.5878747269098347772, -14.86239685203039862, -1.500000000000000444 ) ) ;
#17559=ORIENTED_EDGE ( 'NONE', *, *, #17594, .F. ) ;
#17566=CARTESIAN_POINT ( 'NONE',  ( 107.5617723795404999, -18.98359893170737323, 4.522129901861158707 ) ) ;
#17567=CARTESIAN_POINT ( 'NONE',  ( 41.56220206661831895, -20.97620094563766457, 4.522129901861156931 ) ) ;
#17569=CARTESIAN_POINT ( 'NONE',  ( 8.842484022065033145, 0.1108283380285731701, -1.500000000000000000 ) ) ;
#17570=CARTESIAN_POINT ( 'NONE',  ( 108.0291956795919219, -18.48977263977070606, -4.324979624428802794 ) ) ;
#17571=ORIENTED_EDGE ( 'NONE', *, *, #6240, .T. ) ;
#17572=EDGE_CURVE ( 'NONE', #9922, #9843, #9169, .T. ) ;
#17584=VERTEX_POINT ( 'NONE', #4204 ) ;
#17588=CARTESIAN_POINT ( 'NONE',  ( -31.59999999999999787, 0.000000000000000000, 1.500000000000000000 ) ) ;
#17594=EDGE_CURVE ( 'NONE', #19511, #9922, #22114, .T. ) ;
#17595=CARTESIAN_POINT ( 'NONE',  ( 107.3477315916820913, -15.88627780335592021, 1.500000000000000000 ) ) ;
#17598=CARTESIAN_POINT ( 'NONE',  ( 23.22564588060096469, -22.38932300456763969, -1.000000000000000000 ) ) ;
#17605=CARTESIAN_POINT ( 'NONE',  ( 6.013832568680315127, -13.53405802968792848, -1.500000000000000000 ) ) ;
#17608=CARTESIAN_POINT ( 'NONE',  ( 0.1334381338377635395, -6.141084277567379957, -1.772361585196223999 ) ) ;
#17612=CIRCLE ( 'NONE', #8006, 4.499999999999997335 ) ;
#17616=CARTESIAN_POINT ( 'NONE',  ( 25.49907528997210093, -17.55969604403590978, 1.109946655922742664 ) ) ;
#17617=FACE_OUTER_BOUND ( 'NONE', #8990, .T. ) ;
#17628=CARTESIAN_POINT ( 'NONE',  ( -50.60000000000000142, -10.96966150227468972, 1.500000000000000000 ) ) ;
#17629=ORIENTED_EDGE ( 'NONE', *, *, #13071, .T. ) ;
#17631=CARTESIAN_POINT ( 'NONE',  ( 108.0225568495473567, -18.39417513866207088, 4.506423374900446532 ) ) ;
#17634=CARTESIAN_POINT ( 'NONE',  ( 8.397160224431742037, -14.43505762332009823, 1.755102938775167098 ) ) ;
#17636=CARTESIAN_POINT ( 'NONE',  ( -3.616018626656801960, -10.49347358198851943, -1.499999999999999556 ) ) ;
#17639=CARTESIAN_POINT ( 'NONE',  ( 11.84005032159772419, -19.96225593911332297, 1.750548462235233416 ) ) ;
#17644=DIRECTION ( 'NONE',  ( 1.000000000000000000, 0.000000000000000000, 0.000000000000000000 ) ) ;
#17647=AXIS2_PLACEMENT_3D ( 'NONE', #32972, #15053, #4871 ) ;
#17648=ADVANCED_FACE ( 'NONE', ( #31343 ), #26658, .F. ) ;
#17649=CARTESIAN_POINT ( 'NONE',  ( 21.60651947346046953, -21.76079427965450819, -1.483814047169784711 ) ) ;
#17654=FACE_OUTER_BOUND ( 'NONE', #4915, .T. ) ;
#17656=DIRECTION ( 'NONE',  ( 0.000000000000000000, 1.000000000000000000, -0.000000000000000000 ) ) ;
#17660=DIRECTION ( 'NONE',  ( -1.000000000000000000, 0.000000000000000000, 0.000000000000000000 ) ) ;
#17662=CARTESIAN_POINT ( 'NONE',  ( 22.70718278262391010, -21.88016059487456033, 1.342589741762119315 ) ) ;
#17672=CARTESIAN_POINT ( 'NONE',  ( 2.629595859988236750, -11.38843847601185288, 1.760289366381509346 ) ) ;
#17675=LINE ( 'NONE', #2495, #20427 ) ;
#17680=ORIENTED_EDGE ( 'NONE', *, *, #20442, .T. ) ;
#17693=DIRECTION ( 'NONE',  ( -0.000000000000000000, -0.000000000000000000, 1.000000000000000000 ) ) ;
#17694=FACE_OUTER_BOUND ( 'NONE', #8440, .T. ) ;
#17702=CARTESIAN_POINT ( 'NONE',  ( 23.30969226767722091, -17.20274083179980451, 1.451821733976742301 ) ) ;
#17715=CARTESIAN_POINT ( 'NONE',  ( 8.236088440266469135, -19.08859993110833742, -1.499999999999919620 ) ) ;
#17738=CIRCLE ( 'NONE', #15082, 0.5000000000000000000 ) ;
#17740=CARTESIAN_POINT ( 'NONE',  ( 14.13431920379513862, -20.70626837987542856, -1.500000000000000000 ) ) ;
#17742=DIRECTION ( 'NONE',  ( 1.000000000000000000, 0.000000000000000000, 0.000000000000000000 ) ) ;
#17748=CARTESIAN_POINT ( 'NONE',  ( 0.5689136306499625872, -15.77252859670922724, 1.500000000000000444 ) ) ;
#17749=CARTESIAN_POINT ( 'NONE',  ( 7.158832484464809021, -3.801775501247948164, -1.500000000000000000 ) ) ;
#17762=CARTESIAN_POINT ( 'NONE',  ( -23.35000000000000142, -10.96966150227469505, -1.500000000000000000 ) ) ;
#17771=CARTESIAN_POINT ( 'NONE',  ( -52.69999999999999574, -10.96966150227468972, 7.074999999999997513 ) ) ;
#17780=CARTESIAN_POINT ( 'NONE',  ( 107.5300661083891640, -18.52314831157204011, 5.060106418404170192 ) ) ;
#17793=CARTESIAN_POINT ( 'NONE',  ( 0.8174570305809125692, -9.170357625429589987, 1.500000000000000000 ) ) ;
#17805=CARTESIAN_POINT ( 'NONE',  ( -0.7739934281325634435, -8.972773999336988382, 4.522129901861156931 ) ) ;
#17815=VECTOR ( 'NONE', #6359, 999.9999999999998863 ) ;
#17825=VERTEX_POINT ( 'NONE', #6737 ) ;
#17828=CARTESIAN_POINT ( 'NONE',  ( -1.694237876702966217, -1.500727999663088896, -4.522129901861166701 ) ) ;
#17829=ORIENTED_EDGE ( 'NONE', *, *, #9356, .F. ) ;
#17831=CARTESIAN_POINT ( 'NONE',  ( -4.121075341857856067, -7.626600714980313889, 1.744488919440858377 ) ) ;
#17854=CARTESIAN_POINT ( 'NONE',  ( 22.92640216610012516, -21.90430348730595966, 1.195188340063319199 ) ) ;
#17861=B_SPLINE_CURVE_WITH_KNOTS ( 'NONE', 3,
 ( #21507, #29810, #30312, #13782 ),
 .UNSPECIFIED., .F., .F.,
 ( 4, 4 ),
 ( 0.005731821976040855568, 0.005732069968806756399 ),
 .UNSPECIFIED. ) ;
#17863=CARTESIAN_POINT ( 'NONE',  ( 18.41703969107078365, -16.82189904609263564, 1.753330412709693586 ) ) ;
#17869=VERTEX_POINT ( 'NONE', #6577 ) ;
#17885=ORIENTED_EDGE ( 'NONE', *, *, #21318, .F. ) ;
#17899=B_SPLINE_CURVE_WITH_KNOTS ( 'NONE', 3,
 ( #31102, #31760, #21370, #18693, #3518, #23877, #8834, #31271, #23546, #18541, #11166, #5824 ),
 .UNSPECIFIED., .F., .F.,
 ( 4, 2, 2, 2, 2, 4 ),
 ( 0.004476667581006692556, 0.005062001261575544211, 0.005354668101859973509, 0.005501001522002187290, 0.005574168232073290277, 0.005647334942144392397 ),
 .UNSPECIFIED. ) ;
#17900=EDGE_CURVE ( 'NONE', #7488, #24872, #17429, .T. ) ;
#17911=ORIENTED_EDGE ( 'NONE', *, *, #3437, .F. ) ;
#17915=ORIENTED_EDGE ( 'NONE', *, *, #21318, .T. ) ;
#17916=CARTESIAN_POINT ( 'NONE',  ( -3.616018626656801960, -10.49347358198851943, -1.500000000000000000 ) ) ;
#17925=CARTESIAN_POINT ( 'NONE',  ( -1.597432620025311945, -13.32264212359284805, 1.744099735884073965 ) ) ;
#17928=CARTESIAN_POINT ( 'NONE',  ( 108.0606309209090199, -18.94243229463347333, -4.540944552663033207 ) ) ;
#17942=EDGE_CURVE ( 'NONE', #30719, #2302, #1236, .T. ) ;
#17948=CARTESIAN_POINT ( 'NONE',  ( 6.220890055307039646, -15.20372210278347680, -4.522129901861164925 ) ) ;
#17953=CARTESIAN_POINT ( 'NONE',  ( -2.799189356623903890, 0.2797963115142978463, 0.9035254090724027520 ) ) ;
#17954=CARTESIAN_POINT ( 'NONE',  ( -3.222375984151269357, 0.000000000000000000, 1.000000000000000000 ) ) ;
#17965=CARTESIAN_POINT ( 'NONE',  ( 16.87487612390083669, -15.54663979847903477, -1.500000000000000000 ) ) ;
#17972=CARTESIAN_POINT ( 'NONE',  ( 0.1517578099452172036, -1.375880305419571625, 4.522129901861156931 ) ) ;
#17976=EDGE_CURVE ( 'NONE', #25934, #18680, #6405, .T. ) ;
#17983=FACE_OUTER_BOUND ( 'NONE', #15911, .T. ) ;
#17987=ADVANCED_FACE ( 'NONE', ( #4894 ), #25295, .T. ) ;
#17995=ADVANCED_FACE ( 'NONE', ( #12729 ), #5965, .F. ) ;
#18003=CARTESIAN_POINT ( 'NONE',  ( 22.00639167669224960, -21.80013755708282730, -1.499999999999999556 ) ) ;
#18007=CARTESIAN_POINT ( 'NONE',  ( -17.04380309137718186, -25.93932300454937945, 11.50000000000000000 ) ) ;
#18010=CARTESIAN_POINT ( 'NONE',  ( 24.42490082288193065, -17.42819879232223101, 1.446796129083761873 ) ) ;
#18015=EDGE_CURVE ( 'NONE', #28748, #6111, #16701, .T. ) ;
#18022=CARTESIAN_POINT ( 'NONE',  ( 7.362531900907073990, -8.542914936921636837, 1.000000000000000000 ) ) ;
#18023=ORIENTED_EDGE ( 'NONE', *, *, #15895, .F. ) ;
#18024=CARTESIAN_POINT ( 'NONE',  ( 21.62027785038666394, -21.76162169609135688, 1.485493366284274863 ) ) ;
#18066=CARTESIAN_POINT ( 'NONE',  ( -23.35000000000000142, -10.96966150227469505, 4.500000000000000888 ) ) ;
#18068=CARTESIAN_POINT ( 'NONE',  ( -23.35000000000000142, -10.96966150227469505, 1.500000000000000000 ) ) ;
#18074=CARTESIAN_POINT ( 'NONE',  ( -2.351930117019871425, -12.55067978397925721, 1.499999999999719780 ) ) ;
#18078=CARTESIAN_POINT ( 'NONE',  ( 108.0612055743968369, -18.95070716190199889, -4.518753833174125489 ) ) ;
#18086=CARTESIAN_POINT ( 'NONE',  ( -2.983877251335087077, -0.2474135948681053798, -1.436677650513773941 ) ) ;
#18088=CARTESIAN_POINT ( 'NONE',  ( 107.9932884231783277, -17.97271708001612822, 4.596977851539515214 ) ) ;
#18092=CARTESIAN_POINT ( 'NONE',  ( -16.96515769256209794, -25.93932300454937945, 11.09540449768827131 ) ) ;
#18093=CARTESIAN_POINT ( 'NONE',  ( 0.9232102171129938917, 0.000000000000000000, -4.522129901861164925 ) ) ;
#18101=CARTESIAN_POINT ( 'NONE',  ( -3.115650298287759856, -0.007755536299741299863, 1.107207510975252385 ) ) ;
#18111=DIRECTION ( 'NONE',  ( 0.000000000000000000, 1.000000000000000000, 0.000000000000000000 ) ) ;
#18112=CARTESIAN_POINT ( 'NONE',  ( 21.67755997557487291, -21.76174915995097336, -1.411535641070696068 ) ) ;
#18113=CARTESIAN_POINT ( 'NONE',  ( 108.1300413742128512, -20.08325238768279064, -1.420916680477450011 ) ) ;
#18120=B_SPLINE_CURVE_WITH_KNOTS ( 'NONE', 3,
 ( #30896, #7969, #31054, #8139, #18349, #7459, #15170, #12651, #33056, #29038 ),
 .UNSPECIFIED., .F., .F.,
 ( 4, 2, 2, 2, 4 ),
 ( 0.000000000000000000, 0.001704392904692032329, 0.002556589357038042964, 0.002982687583211043620, 0.003408785809384044276 ),
 .UNSPECIFIED. ) ;
#18135=ORIENTED_EDGE ( 'NONE', *, *, #1091, .T. ) ;
#18141=LINE ( 'NONE', #10112, #10223 ) ;
#18150=CARTESIAN_POINT ( 'NONE',  ( -52.69999999999999574, -10.96966150227468972, 0.9999999999999991118 ) ) ;
#18151=EDGE_CURVE ( 'NONE', #19632, #31676, #19928, .T. ) ;
#18166=ADVANCED_FACE ( 'NONE', ( #1687 ), #16888, .F. ) ;
#18169=CARTESIAN_POINT ( 'NONE',  ( 107.9128139062042209, -20.39012166861472508, 1.488290602270393892 ) ) ;
#18170=DIRECTION ( 'NONE',  ( 0.000000000000000000, 0.000000000000000000, 1.000000000000000000 ) ) ;
#18171=CARTESIAN_POINT ( 'NONE',  ( 14.03158388662595435, -14.04624128054226340, 1.000000000000000000 ) ) ;
#18173=EDGE_CURVE ( 'NONE', #23895, #8122, #18316, .T. ) ;
#18179=ADVANCED_FACE ( 'NONE', ( #1371 ), #8495, .F. ) ;
#18203=AXIS2_PLACEMENT_3D ( 'NONE', #14652, #14804, #17337 ) ;
#18206=CIRCLE ( 'NONE', #9655, 0.5000000000000004441 ) ;
#18215=DIRECTION ( 'NONE',  ( -0.000000000000000000, 0.000000000000000000, 1.000000000000000000 ) ) ;
#18219=ORIENTED_EDGE ( 'NONE', *, *, #27506, .F. ) ;
#18220=ADVANCED_FACE ( 'NONE', ( #13185 ), #10291, .T. ) ;
#18237=CARTESIAN_POINT ( 'NONE',  ( 17.36028307725516839, -18.11957666780532250, 4.522129901861156931 ) ) ;
#18238=CARTESIAN_POINT ( 'NONE',  ( 0.4355866597345551816, -15.33293614044432118, 1.500000000000319300 ) ) ;
#18243=CARTESIAN_POINT ( 'NONE',  ( -29.24402871571405882, -25.93932300454937945, 11.00000000000000000 ) ) ;
#18262=FACE_OUTER_BOUND ( 'NONE', #29603, .T. ) ;
#18263=CARTESIAN_POINT ( 'NONE',  ( 0.4082220075202826481, -6.684754012654101629, -0.9788672205888330202 ) ) ;
#18266=CARTESIAN_POINT ( 'NONE',  ( 107.9935202411828215, -17.97605520161211956, 4.592059696647398326 ) ) ;
#18284=CARTESIAN_POINT ( 'NONE',  ( -31.67864539881508179, -21.93932300455407258, 1.095404497688272194 ) ) ;
#18290=CARTESIAN_POINT ( 'NONE',  ( 107.9802527803230419, -17.78500706576073753, 4.325704939602341703 ) ) ;
#18298=AXIS2_PLACEMENT_3D ( 'NONE', #4334, #6830, #17015 ) ;
#18312=CARTESIAN_POINT ( 'NONE',  ( 17.37538333147393388, -21.16291065652740144, -1.500000000000095923 ) ) ;
#18314=ORIENTED_EDGE ( 'NONE', *, *, #20557, .F. ) ;
#18316=CIRCLE ( 'NONE', #9761, 9.500000000000003553 ) ;
#18318=VERTEX_POINT ( 'NONE', #10857 ) ;
#18321=CIRCLE ( 'NONE', #30080, 0.4500000000000017319 ) ;
#18335=ORIENTED_EDGE ( 'NONE', *, *, #19353, .T. ) ;
#18349=CARTESIAN_POINT ( 'NONE',  ( 23.29109779593791529, -17.41442569313431221, -1.664431119656285540 ) ) ;
#18361=CARTESIAN_POINT ( 'NONE',  ( 13.44509804349992166, -13.81913516303365341, 1.000000000000000000 ) ) ;
#18372=CARTESIAN_POINT ( 'NONE',  ( -0.9232102171129843438, 0.000000000000000000, 4.522129901861158707 ) ) ;
#18378=CARTESIAN_POINT ( 'NONE',  ( -23.35000000000000142, -10.96966150227469505, 4.500000000000000888 ) ) ;
#18379=CARTESIAN_POINT ( 'NONE',  ( 9.337065666035901046, -0.007760238742138971836, 1.098363920870218946 ) ) ;
#18381=CARTESIAN_POINT ( 'NONE',  ( 24.38302348701447997, -17.39153354040979949, -1.380603655064296387 ) ) ;
#18385=CARTESIAN_POINT ( 'NONE',  ( -3.135269660805079628, -0.4999999999999985012, 1.949999999999999956 ) ) ;
#18389=AXIS2_PLACEMENT_3D ( 'NONE', #7157, #27693, #2632 ) ;
#18391=CARTESIAN_POINT ( 'NONE',  ( 108.1300413742128086, -19.94772548867798179, 1.389623142577374626 ) ) ;
#18398=CARTESIAN_POINT ( 'NONE',  ( 2.717504505341735932, -0.4236608596156875017, -1.500000000000000000 ) ) ;
#18408=VERTEX_POINT ( 'NONE', #13676 ) ;
#18410=CARTESIAN_POINT ( 'NONE',  ( 7.418618974160530399, -8.736763461978926060, -0.9999999999999997780 ) ) ;
#18418=CARTESIAN_POINT ( 'NONE',  ( 16.05919002109159521, -15.28992581341320545, 1.499999999999999778 ) ) ;
#18420=CARTESIAN_POINT ( 'NONE',  ( 107.6125222110667039, -19.71405102733161741, -3.024918492460353381 ) ) ;
#18423=CARTESIAN_POINT ( 'NONE',  ( 107.6236081988486859, -19.87368190684284386, 2.697742887155947233 ) ) ;
#18425=CARTESIAN_POINT ( 'NONE',  ( -1.691799335042641683, -13.40595961238992828, 1.500000000000560219 ) ) ;
#18428=CARTESIAN_POINT ( 'NONE',  ( 22.16007320322839647, -17.32365168620649953, 1.743368838329871995 ) ) ;
#18433=EDGE_CURVE ( 'NONE', #10617, #993, #25924, .T. ) ;
#18436=CARTESIAN_POINT ( 'NONE',  ( -2.619378609982131234, -0.1905507107690968260, -1.628225384166318346 ) ) ;
#18437=CARTESIAN_POINT ( 'NONE',  ( 108.0105421681096942, -18.22116671483598438, 4.637827421830889918 ) ) ;
#18441=DIRECTION ( 'NONE',  ( 0.000000000000000000, 0.000000000000000000, 1.000000000000000000 ) ) ;
#18442=CARTESIAN_POINT ( 'NONE',  ( 2.600000000000000089, 0.000000000000000000, -1.500000000000000444 ) ) ;
#18444=CARTESIAN_POINT ( 'NONE',  ( 107.9482554908978500, -17.32425405796034568, 4.517001157681336920 ) ) ;
#18448=CARTESIAN_POINT ( 'NONE',  ( -2.609487367013886505, -0.08210191867241613262, 1.553472644056475449 ) ) ;
#18456=PLANE ( 'NONE',  #20456 ) ;
#18457=CARTESIAN_POINT ( 'NONE',  ( -4.027720362024412637, -8.337845212197136036, -1.744153996925280392 ) ) ;
#18460=CARTESIAN_POINT ( 'NONE',  ( 24.38441422956718085, -17.22282062799148150, -1.499999999997775779 ) ) ;
#18462=CARTESIAN_POINT ( 'NONE',  ( 107.8864559843597988, -16.43435653759661363, 1.556338746034127363 ) ) ;
#18464=CARTESIAN_POINT ( 'NONE',  ( 21.08401840680159367, -16.78474387324287775, 1.500000000000000000 ) ) ;
#18467=DIRECTION ( 'NONE',  ( 0.8571673007021120005, 0.000000000000000000, 0.5150380749100547106 ) ) ;
#18470=FACE_OUTER_BOUND ( 'NONE', #8914, .T. ) ;
#18485=ORIENTED_EDGE ( 'NONE', *, *, #2496, .T. ) ;
#18493=CARTESIAN_POINT ( 'NONE',  ( 108.0320971364573239, -18.53155289684145046, 4.239511015329910926 ) ) ;
#18498=CARTESIAN_POINT ( 'NONE',  ( 72.72614267428248525, -20.12349919388105945, -5.485967528433937979 ) ) ;
#18514=CYLINDRICAL_SURFACE ( 'NONE', #2878, 0.4499999999999990119 ) ;
#18515=CARTESIAN_POINT ( 'NONE',  ( 9.037136197880096589, -11.91234824294609140, 1.500000000000000000 ) ) ;
#18516=ORIENTED_EDGE ( 'NONE', *, *, #28693, .F. ) ;
#18519=CARTESIAN_POINT ( 'NONE',  ( 0.6278659085242910276, -4.203768939204204358, 1.500000000000068390 ) ) ;
#18529=B_SPLINE_CURVE_WITH_KNOTS ( 'NONE', 3,
 ( #20610, #375, #31142, #25600 ),
 .UNSPECIFIED., .F., .F.,
 ( 4, 4 ),
 ( 0.005732069968871694905, 0.4737525964756066910 ),
 .UNSPECIFIED. ) ;
#18537=EDGE_CURVE ( 'NONE', #25587, #21122, #16178, .T. ) ;
#18541=CARTESIAN_POINT ( 'NONE',  ( 25.41902038486284354, -17.54124217233828631, 1.046354159564242714 ) ) ;
#18542=B_SPLINE_CURVE_WITH_KNOTS ( 'NONE', 3,
 ( #26190, #21183, #13466, #8457, #5792, #15827, #16313, #3299, #26035, #29186, #5647, #28850 ),
 .UNSPECIFIED., .F., .F.,
 ( 4, 2, 2, 2, 2, 4 ),
 ( -5.999999999585006259E-08, 0.0007057886787611236407, 0.001058713018141682572, 0.001235175187831967242, 0.001323406272677110120, 0.001411637357522252997 ),
 .UNSPECIFIED. ) ;
#18544=DIRECTION ( 'NONE',  ( 0.000000000000000000, 0.000000000000000000, -1.000000000000000000 ) ) ;
#18545=EDGE_CURVE ( 'NONE', #3159, #12213, #20346, .T. ) ;
#18546=CARTESIAN_POINT ( 'NONE',  ( 107.5501783195510370, -18.81539188448605415, -4.846927202741923679 ) ) ;
#18562=CARTESIAN_POINT ( 'NONE',  ( 6.680689650589743067, -6.092366900306463329, 1.500000000000000222 ) ) ;
#18564=( BOUNDED_SURFACE ( )  B_SPLINE_SURFACE ( 3, 3, ( 
 ( #6472, #16350, #19813, #29225, #11164, #30024, #26559, #13996, #21703, #22316, #3659, #984, #13815, #4451, #24211, #3517 ),
 ( #14629, #24829, #29382, #12120, #21369, #1146, #31575, #21550, #26418, #13514, #1333, #31757, #23726, #1947, #3346, #8832 ),
 ( #19037, #6311, #16497, #32528, #11506, #7112, #26705, #840, #16194, #3819, #31911, #8977, #11017, #19188, #9591, #31415 ),
 ( #8490, #18691, #28890, #5998, #25488, #4763, #28011, #10092, #22815, #17805, #7271, #14937, #25648, #7420, #17972, #33020 ) ),
 .UNSPECIFIED., .F., .F., .F. ) 
 B_SPLINE_SURFACE_WITH_KNOTS ( ( 4, 4 ),
 ( 4, 2, 2, 2, 2, 2, 2, 4 ),
 ( 0.000000000000000000, 1.000000000000000000 ),
 ( 0.000000000000000000, 0.5000000000000000000, 0.6250000000000000000, 0.7500000000000000000, 0.8125000000000000000, 0.8750000000000000000, 0.9375000000000000000, 1.000000000000000000 ),
 .UNSPECIFIED. ) 
 GEOMETRIC_REPRESENTATION_ITEM ( )  RATIONAL_B_SPLINE_SURFACE ( (
 ( 1.000000000000000000, 1.000000000000000000, 1.000000000000000000, 1.000000000000000000, 1.000000000000000000, 1.000000000000000000, 1.000000000000000000, 1.000000000000000000, 1.000000000000000000, 1.000000000000000000, 1.000000000000000000, 1.000000000000000000, 1.000000000000000000, 1.000000000000000000, 1.000000000000000000, 1.000000000000000000),
 ( 0.5895302151065218155, 0.5895302151065218155, 0.5895302151065218155, 0.5895302151065218155, 0.5895302151065218155, 0.5895302151065218155, 0.5895302151065218155, 0.5895302151065218155, 0.5895302151065218155, 0.5895302151065218155, 0.5895302151065218155, 0.5895302151065218155, 0.5895302151065218155, 0.5895302151065218155, 0.5895302151065218155, 0.5895302151065218155),
 ( 0.5895302151065218155, 0.5895302151065218155, 0.5895302151065218155, 0.5895302151065218155, 0.5895302151065218155, 0.5895302151065218155, 0.5895302151065218155, 0.5895302151065218155, 0.5895302151065218155, 0.5895302151065218155, 0.5895302151065218155, 0.5895302151065218155, 0.5895302151065218155, 0.5895302151065218155, 0.5895302151065218155, 0.5895302151065218155),
 ( 1.000000000000000000, 1.000000000000000000, 1.000000000000000000, 1.000000000000000000, 1.000000000000000000, 1.000000000000000000, 1.000000000000000000, 1.000000000000000000, 1.000000000000000000, 1.000000000000000000, 1.000000000000000000, 1.000000000000000000, 1.000000000000000000, 1.000000000000000000, 1.000000000000000000, 1.000000000000000000) ) ) 
 REPRESENTATION_ITEM ( '' )  SURFACE ( )  );
#18569=CARTESIAN_POINT ( 'NONE',  ( 17.37538333147201186, -21.16291065652713854, 1.500000000000001332 ) ) ;
#18576=B_SPLINE_CURVE_WITH_KNOTS ( 'NONE', 3,
 ( #30397, #14988, #20547, #7976, #12810, #23024, #25207, #2330 ),
 .UNSPECIFIED., .F., .F.,
 ( 4, 2, 2, 4 ),
 ( -5.677916165041726082E-06, 0.0007318671105578830301, 0.001100639623919344836, 0.001469412137280806750 ),
 .UNSPECIFIED. ) ;
#18577=DIRECTION ( 'NONE',  ( -0.1587661886299353009, -0.9873162094019949375, 0.000000000000000000 ) ) ;
#18582=CARTESIAN_POINT ( 'NONE',  ( -17.45597128428593336, -25.93932300454937945, 10.99999999999999822 ) ) ;
#18583=LINE ( 'NONE', #28279, #3880 ) ;
#18588=CARTESIAN_POINT ( 'NONE',  ( -2.976964752645617107, -0.1884360924510954383, -1.392852931015429174 ) ) ;
#18591=CARTESIAN_POINT ( 'NONE',  ( 108.0159574833865292, -18.29914590766157900, 4.591531417968990780 ) ) ;
#18595=FACE_OUTER_BOUND ( 'NONE', #12397, .T. ) ;
#18611=CARTESIAN_POINT ( 'NONE',  ( 12.21775235206943755, -15.17036961632329373, 1.500000000000000000 ) ) ;
#18612=CARTESIAN_POINT ( 'NONE',  ( 23.24967726704456084, -21.43932300456764750, 1.500000000000000000 ) ) ;
#18614=CARTESIAN_POINT ( 'NONE',  ( 2.974466146320851934, 0.1107971263338725920, 0.9540093664865986200 ) ) ;
#18624=CARTESIAN_POINT ( 'NONE',  ( 21.07900179210031411, -21.69205259094561100, -1.492586111082710110 ) ) ;
#18626=CARTESIAN_POINT ( 'NONE',  ( 0.6377051968875022681, -7.657409712011349789, -1.500000000000000000 ) ) ;
#18627=ORIENTED_EDGE ( 'NONE', *, *, #4183, .F. ) ;
#18629=CARTESIAN_POINT ( 'NONE',  ( 25.45368006873471955, -17.55541207042469765, -1.083666005368261409 ) ) ;
#18634=ADVANCED_FACE ( 'NONE', ( #32805 ), #3637, .T. ) ;
#18644=CARTESIAN_POINT ( 'NONE',  ( 107.5592006082064529, -18.94629055990540678, 4.613091233250001366 ) ) ;
#18646=CYLINDRICAL_SURFACE ( 'NONE', #1734, 8.500000000000000000 ) ;
#18662=CARTESIAN_POINT ( 'NONE',  ( 7.502484982177588080, -10.19046547981977291, 1.500000000000000000 ) ) ;
#18671=ADVANCED_FACE ( 'NONE', ( #848 ), #9787, .T. ) ;
#18680=VERTEX_POINT ( 'NONE', #16012 ) ;
#18691=CARTESIAN_POINT ( 'NONE',  ( 72.52374898132083558, -19.78015497543642809, 4.522129901861156931 ) ) ;
#18693=CARTESIAN_POINT ( 'NONE',  ( 25.02099912015120609, -17.46522996914712422, 1.208347673492914165 ) ) ;
#18710=CARTESIAN_POINT ( 'NONE',  ( 17.19530788743130145, -15.12182558545884525, -1.000000000000000000 ) ) ;
#18715=CARTESIAN_POINT ( 'NONE',  ( 107.4500373638804120, -17.36019379023677089, -4.522129901861164036 ) ) ;
#18718=CARTESIAN_POINT ( 'NONE',  ( 0.6728940978343175283, -5.225733934469498188, -1.500000000000000000 ) ) ;
#18723=ADVANCED_BREP_SHAPE_REPRESENTATION ( '', ( #10233, #2865 ), #179 ) ;
#18729=ORIENTED_EDGE ( 'NONE', *, *, #24945, .F. ) ;
#18749=LINE ( 'NONE', #24080, #13943 ) ;
#18750=CARTESIAN_POINT ( 'NONE',  ( 107.4495527293423578, -17.35289746557307211, 4.502194843723872353 ) ) ;
#18755=( BOUNDED_CURVE ( )  B_SPLINE_CURVE ( 3, ( #22078, #14198, #6691, #1364 ),
 .UNSPECIFIED., .F., .F. ) 
 B_SPLINE_CURVE_WITH_KNOTS ( ( 4, 4 ),
 ( 4.712388980384689674, 6.283185307179586232 ),
 .UNSPECIFIED. ) 
 CURVE ( )  GEOMETRIC_REPRESENTATION_ITEM ( )  RATIONAL_B_SPLINE_CURVE ( ( 1.000000000000000000, 0.8047378541243649375, 0.8047378541243649375, 1.000000000000000000 ) ) 
 REPRESENTATION_ITEM ( '' )  );
#18756=LINE ( 'NONE', #892, #2723 ) ;
#18759=CARTESIAN_POINT ( 'NONE',  ( 21.33742408005867830, -21.80181733054034154, -1.346293739632234088 ) ) ;
#18760=DIRECTION ( 'NONE',  ( 1.000000000000000000, 0.000000000000000000, 0.000000000000000000 ) ) ;
#18772=CARTESIAN_POINT ( 'NONE',  ( 0.9575256569274729346, -15.55590288271891630, -1.746220241394478290 ) ) ;
#18773=FACE_OUTER_BOUND ( 'NONE', #32005, .T. ) ;
#18774=CARTESIAN_POINT ( 'NONE',  ( 8.103242287716716064, -10.98376420866757464, -1.500000000000000000 ) ) ;
#18775=CARTESIAN_POINT ( 'NONE',  ( 107.9731642803859444, -17.68293443006343324, -4.116431948592269130 ) ) ;
#18790=CARTESIAN_POINT ( 'NONE',  ( -31.69232733568932403, -28.43932300454937590, -1.595404497688272638 ) ) ;
#18798=CARTESIAN_POINT ( 'NONE',  ( 0.5291759363107053638, -6.520544204277276101, -1.500000000000001110 ) ) ;
#18804=CARTESIAN_POINT ( 'NONE',  ( 25.48003136492769372, -17.55790038815476350, -1.043845799725529710 ) ) ;
#18805=B_SPLINE_SURFACE_WITH_KNOTS ( 'NONE', 1, 3, ( 
 ( #15646, #22988, #23331, #22688, #107, #23182, #25857, #291, #20022, #5451, #30214, #10464, #28029, #2975, #17828, #435 ),
 ( #2613, #20514, #5126, #25506, #20329, #30727, #7799, #27677, #20675, #12476, #17636, #30877, #13129, #7948, #28337, #7287 ),
 ( #32891, #9957, #27842, #20998, #31360, #21305, #5628, #8773, #16119, #18978, #15806, #23818, #5925, #26168, #21162, #930 ) ),
 .UNSPECIFIED., .F., .F., .F.,
 ( 2, 1, 2 ),
 ( 4, 2, 2, 2, 2, 2, 2, 4 ),
 ( 0.000000000000000000, 1.000000000000000000, 1.172438907772619610 ),
 ( 0.000000000000000000, 0.5000000000000000000, 0.6250000000000000000, 0.7500000000000000000, 0.8125000000000000000, 0.8750000000000000000, 0.9375000000000000000, 1.000000000000000000 ),
 .UNSPECIFIED. ) ;
#18830=CARTESIAN_POINT ( 'NONE',  ( 17.36028307726380504, -18.11957666779667875, -4.522129901861164925 ) ) ;
#18843=AXIS2_PLACEMENT_3D ( 'NONE', #7069, #29975, #2407 ) ;
#18849=CARTESIAN_POINT ( 'NONE',  ( 7.278212736155783347, -5.482579125108129503, 1.499999999999858113 ) ) ;
#18854=CARTESIAN_POINT ( 'NONE',  ( 4.832184221226294873, -12.72809002048187388, 1.499999999999788391 ) ) ;
#18876=EDGE_LOOP ( 'NONE', ( #22326, #22296, #14767, #13646 ) ) ;
#18889=EDGE_CURVE ( 'NONE', #6370, #6440, #4012, .T. ) ;
#18891=CARTESIAN_POINT ( 'NONE',  ( 3.093679806470315263, -0.1913619822784921320, -1.398088436977038773 ) ) ;
#18895=CIRCLE ( 'NONE', #22645, 5.000000000000000888 ) ;
#18903=CARTESIAN_POINT ( 'NONE',  ( -2.775296318097017156, 4.123808329995814975E-33, -1.260187769642231226 ) ) ;
#18918=FACE_OUTER_BOUND ( 'NONE', #12353, .T. ) ;
#18928=CARTESIAN_POINT ( 'NONE',  ( -4.037226184167227672, -8.274238725605433942, -1.744146341608699746 ) ) ;
#18937=CARTESIAN_POINT ( 'NONE',  ( 107.9477478514680371, -17.31694417646615136, 4.497024978861354327 ) ) ;
#18940=ORIENTED_EDGE ( 'NONE', *, *, #9536, .F. ) ;
#18941=CARTESIAN_POINT ( 'NONE',  ( 0.000000000000000000, 0.000000000000000000, -1.500000000000000000 ) ) ;
#18946=CARTESIAN_POINT ( 'NONE',  ( 72.25703127509153489, -22.87839253411022611, -1.499999999999999556 ) ) ;
#18952=CARTESIAN_POINT ( 'NONE',  ( 108.1288400433390393, -19.92462668933126579, -1.384270303710054328 ) ) ;
#18953=CARTESIAN_POINT ( 'NONE',  ( 10.63777811968158993, -12.44241537618683147, -1.500000000000426104 ) ) ;
#18966=DIRECTION ( 'NONE',  ( 1.000000000000000000, 0.000000000000000000, 0.000000000000000000 ) ) ;
#18972=CARTESIAN_POINT ( 'NONE',  ( 12.21818417105343713, -15.17047698692286239, -1.499999999999999112 ) ) ;
#18977=CARTESIAN_POINT ( 'NONE',  ( 25.24493059864625977, -17.53551310887482373, -1.328338028042538976 ) ) ;
#18978=CARTESIAN_POINT ( 'NONE',  ( -3.142639414282944799, -12.00291247001954531, -0.9788672205760856615 ) ) ;
#18984=CARTESIAN_POINT ( 'NONE',  ( -2.786590204610738475, -5.640011313470055576, 4.522129901861158707 ) ) ;
#18992=CARTESIAN_POINT ( 'NONE',  ( 108.0613718287933978, -18.95310118385105369, 4.512205001694104212 ) ) ;
#18993=( BOUNDED_CURVE ( )  B_SPLINE_CURVE ( 3, ( #14309, #32253, #27376, #21846 ),
 .UNSPECIFIED., .F., .F. ) 
 B_SPLINE_CURVE_WITH_KNOTS ( ( 4, 4 ),
 ( 4.712388980384689674, 6.091199089460276106 ),
 .UNSPECIFIED. ) 
 CURVE ( )  GEOMETRIC_REPRESENTATION_ITEM ( )  RATIONAL_B_SPLINE_CURVE ( ( 1.000000000000000000, 0.8477497222584658987, 0.8477497222584658987, 1.000000000000000000 ) ) 
 REPRESENTATION_ITEM ( '' )  );
#18998=ADVANCED_FACE ( 'NONE', ( #27397 ), #25412, .T. ) ;
#19008=CARTESIAN_POINT ( 'NONE',  ( 107.4500593345382811, -17.36019228850094720, 4.522129901861156931 ) ) ;
#19010=CARTESIAN_POINT ( 'NONE',  ( 8.254683653268195087, -1.057518490445428672, 1.500000000000000000 ) ) ;
#19012=CARTESIAN_POINT ( 'NONE',  ( 6.840024017557566616, -8.509480309817710975, -1.500000000000000222 ) ) ;
#19017=CARTESIAN_POINT ( 'NONE',  ( 0.5876463044851316653, -8.554742072817132836, 1.500000000000176303 ) ) ;
#19025=DIRECTION ( 'NONE',  ( -1.000000000000000000, 0.000000000000000000, -0.000000000000000000 ) ) ;
#19028=CARTESIAN_POINT ( 'NONE',  ( -23.35000000000000142, -10.96966150227469505, -11.00000000000000000 ) ) ;
#19036=DIRECTION ( 'NONE',  ( 1.000000000000000000, 0.000000000000000000, 0.000000000000000000 ) ) ;
#19037=CARTESIAN_POINT ( 'NONE',  ( 109.7220438555052056, -17.55815402607574782, 5.485967528433933538 ) ) ;
#19043=CARTESIAN_POINT ( 'NONE',  ( 3.286352104298968069, -0.1045966074583460359, -1.312070483712308056 ) ) ;
#19045=ORIENTED_EDGE ( 'NONE', *, *, #24802, .T. ) ;
#19068=CARTESIAN_POINT ( 'NONE',  ( 14.53973501903505294, -20.67384794426875061, 1.499999999998431477 ) ) ;
#19077=CARTESIAN_POINT ( 'NONE',  ( -3.467105996041551119, -1.941686652642359512, -1.500000000000638156 ) ) ;
#19083=CARTESIAN_POINT ( 'NONE',  ( 19.75018141866911847, -21.43174828998465031, 1.668660430087062219 ) ) ;
#19086=CARTESIAN_POINT ( 'NONE',  ( 23.67724090058579733, -17.25947716274867716, 1.422757073343390521 ) ) ;
#19102=CARTESIAN_POINT ( 'NONE',  ( 2.453231587674435055, -16.55902999108526430, -1.747541913858293050 ) ) ;
#19104=CARTESIAN_POINT ( 'NONE',  ( 9.827398781245305415, -12.51289689083529488, -1.500000000000000000 ) ) ;
#19110=CARTESIAN_POINT ( 'NONE',  ( -1.694237876703138967, -1.500727999663424184, 4.522129901861158707 ) ) ;
#19117=CARTESIAN_POINT ( 'NONE',  ( 21.34740231350966866, -21.82855858833832485, -1.313840182778319932 ) ) ;
#19130=CARTESIAN_POINT ( 'NONE',  ( 17.97422212134408781, -19.86246923125032282, 4.522129901861158707 ) ) ;
#19134=CARTESIAN_POINT ( 'NONE',  ( 22.61756301589401374, -21.90439283146508131, 1.185951968833306003 ) ) ;
#19139=CARTESIAN_POINT ( 'NONE',  ( 107.5613070931556194, -18.97684952450245888, 4.540105482573447482 ) ) ;
#19140=CARTESIAN_POINT ( 'NONE',  ( 73.25280475358511012, -21.01694209560737292, -5.485967528433938867 ) ) ;
#19148=EDGE_CURVE ( 'NONE', #28448, #3025, #13015, .T. ) ;
#19156=CARTESIAN_POINT ( 'NONE',  ( 7.168700580349852025, -6.410142746795773228, 1.000000000000000000 ) ) ;
#19158=CARTESIAN_POINT ( 'NONE',  ( 6.682200477904348901, -7.715721153620951789, -1.500000000000000000 ) ) ;
#19160=CARTESIAN_POINT ( 'NONE',  ( 2.895885197758577334, -11.44804382260450204, 1.500000000000177858 ) ) ;
#19178=DIRECTION ( 'NONE',  ( 0.9916316928896840022, -0.1290991311231002303, 6.658392840697635979E-13 ) ) ;
#19188=CARTESIAN_POINT ( 'NONE',  ( -0.7867377105083910305, -2.707992247746365599, 5.485967528433933538 ) ) ;
#19191=ORIENTED_EDGE ( 'NONE', *, *, #9690, .T. ) ;
#19195=CARTESIAN_POINT ( 'NONE',  ( 107.4543400279316216, -17.42228489399607128, -4.691808660060365455 ) ) ;
#19205=ADVANCED_FACE ( 'NONE', ( #30870 ), #23473, .T. ) ;
#19211=B_SPLINE_CURVE_WITH_KNOTS ( 'NONE', 3,
 ( #5069, #28622, #10899, #27965 ),
 .UNSPECIFIED., .F., .F.,
 ( 4, 4 ),
 ( 0.005731821976040855568, 0.005732069968807134569 ),
 .UNSPECIFIED. ) ;
#19219=AXIS2_PLACEMENT_3D ( 'NONE', #10086, #14619, #32688 ) ;
#19234=AXIS2_PLACEMENT_3D ( 'NONE', #11007, #23866, #21207 ) ;
#19236=DIRECTION ( 'NONE',  ( 0.000000000000000000, 0.000000000000000000, -1.000000000000000000 ) ) ;
#19242=EDGE_LOOP ( 'NONE', ( #26196, #7579, #22065, #18729 ) ) ;
#19243=EDGE_CURVE ( 'NONE', #31676, #8978, #5118, .T. ) ;
#19258=CARTESIAN_POINT ( 'NONE',  ( -3.828276826527910348, -10.43768764654175918, -1.500000000000000222 ) ) ;
#19261=CIRCLE ( 'NONE', #36, 0.5000000000000004441 ) ;
#19264=CARTESIAN_POINT ( 'NONE',  ( 10.90710808056851278, -12.60204455863677531, -1.499999999999860112 ) ) ;
#19265=CARTESIAN_POINT ( 'NONE',  ( 108.0601201328837817, -18.93507707413851904, -4.559426007957987359 ) ) ;
#19273=DESIGN_CONTEXT ( 'detailed design', #7986, 'design' ) ;
#19284=ADVANCED_FACE ( 'NONE', ( #17983 ), #8119, .F. ) ;
#19287=VECTOR ( 'NONE', #20382, 1000.000000000000000 ) ;
#19288=EDGE_CURVE ( 'NONE', #21586, #12444, #30664, .T. ) ;
#19292=CARTESIAN_POINT ( 'NONE',  ( 2.318812167152461967, -10.58295493561522882, -1.500000000000000444 ) ) ;
#19314=CARTESIAN_POINT ( 'NONE',  ( 0.5220033361344523781, 0.000000000000000000, -5.485967528433937979 ) ) ;
#19319=CIRCLE ( 'NONE', #16105, 5.500000000000001776 ) ;
#19324=CARTESIAN_POINT ( 'NONE',  ( -31.18783180709124636, -25.43932300454937234, 1.500000000000000000 ) ) ;
#19336=CARTESIAN_POINT ( 'NONE',  ( 6.680689650589764383, -6.092366900306257271, -1.500000000000000000 ) ) ;
#19341=CARTESIAN_POINT ( 'NONE',  ( 1.653004494525485146, -10.31337013662990998, 1.499999999999999556 ) ) ;
#19345=CARTESIAN_POINT ( 'NONE',  ( -4.176545177854389834, -3.225705193879217170, 1.500000000000000888 ) ) ;
#19347=AXIS2_PLACEMENT_3D ( 'NONE', #5591, #15774, #5736 ) ;
#19351=DIRECTION ( 'NONE',  ( 8.519590295723598769E-19, 5.916484360648977690E-20, 1.000000000000000000 ) ) ;
#19353=EDGE_CURVE ( 'NONE', #17584, #1029, #20765, .T. ) ;
#19355=CARTESIAN_POINT ( 'NONE',  ( 22.65740490676343555, -21.90673157959303197, -1.180310388834369784 ) ) ;
#19360=CARTESIAN_POINT ( 'NONE',  ( -28.35000000000000497, -10.96966150227469505, 1.500000000000000000 ) ) ;
#19368=AXIS2_PLACEMENT_3D ( 'NONE', #29434, #3554, #27085 ) ;
#19376=EDGE_CURVE ( 'NONE', #31676, #21250, #18895, .T. ) ;
#19381=CARTESIAN_POINT ( 'NONE',  ( 0.000000000000000000, -0.5000000000000000000, -1.500000000000000000 ) ) ;
#19388=CIRCLE ( 'NONE', #22586, 6.500000000000002665 ) ;
#19403=CARTESIAN_POINT ( 'NONE',  ( 3.708298821157957725, -12.03564075718119852, -1.499999999999999556 ) ) ;
#19424=DIRECTION ( 'NONE',  ( 0.000000000000000000, -1.000000000000000000, 0.000000000000000000 ) ) ;
#19430=ADVANCED_FACE ( 'NONE', ( #17285 ), #19622, .T. ) ;
#19436=CARTESIAN_POINT ( 'NONE',  ( 107.4497430981611075, -17.35563866676828582, 4.509685912366180105 ) ) ;
#19438=ADVANCED_FACE ( 'NONE', ( #32667 ), #7246, .F. ) ;
#19440=CARTESIAN_POINT ( 'NONE',  ( 19.66689578795203985, -21.64324770234357587, 1.457654425243584129 ) ) ;
#19449=CARTESIAN_POINT ( 'NONE',  ( 17.33093461831547444, -21.43932300456618378, -1.500000000000000000 ) ) ;
#19450=EDGE_LOOP ( 'NONE', ( #19191, #14149, #20460, #18627 ) ) ;
#19455=CARTESIAN_POINT ( 'NONE',  ( 7.154313482939221203, -6.723190066306958812, -1.500000000000143219 ) ) ;
#19456=CARTESIAN_POINT ( 'NONE',  ( 107.5591617223737018, -18.94572639363423860, -4.614305386542819853 ) ) ;
#19475=CARTESIAN_POINT ( 'NONE',  ( 8.030511337664275828, -2.816904086294465870, 0.9999999999999997780 ) ) ;
#19476=ORIENTED_EDGE ( 'NONE', *, *, #17111, .T. ) ;
#19477=ADVANCED_FACE ( 'NONE', ( #32846 ), #26282, .T. ) ;
#19481=VERTEX_POINT ( 'NONE', #20942 ) ;
#19506=DIRECTION ( 'NONE',  ( 0.000000000000000000, -1.000000000000000000, 0.000000000000000000 ) ) ;
#19510=CARTESIAN_POINT ( 'NONE',  ( 17.05941372759221153, -15.60161612857906910, -1.500000000000001110 ) ) ;
#19511=VERTEX_POINT ( 'NONE', #17771 ) ;
#19512=CARTESIAN_POINT ( 'NONE',  ( 0.5363866353863503411, -4.520465117293254842, 1.500000000000034861 ) ) ;
#19516=CARTESIAN_POINT ( 'NONE',  ( -4.075753277656722240, -9.746161035319881094, 1.499999999999999778 ) ) ;
#19519=CARTESIAN_POINT ( 'NONE',  ( 24.43445557112633892, -17.40480440763370495, -1.396984404749928022 ) ) ;
#19523=CARTESIAN_POINT ( 'NONE',  ( 0.000000000000000000, -0.5000000000000000000, 1.000000000000000000 ) ) ;
#19529=CARTESIAN_POINT ( 'NONE',  ( -23.35000000000000142, -10.96966150227469505, 4.000000000000000000 ) ) ;
#19530=CARTESIAN_POINT ( 'NONE',  ( -2.223027892448373510, -2.927336879246196677, -4.522129901861166701 ) ) ;
#19534=CARTESIAN_POINT ( 'NONE',  ( 25.11449300058561462, -17.48310186013782896, -1.186355288471905300 ) ) ;
#19545=EDGE_LOOP ( 'NONE', ( #17571, #28139, #26817, #2736, #5879, #11186, #13474, #7806, #12255, #23509 ) ) ;
#19547=ORIENTED_EDGE ( 'NONE', *, *, #19572, .F. ) ;
#19551=CARTESIAN_POINT ( 'NONE',  ( 8.770293993838562230, -1.124525571980899086, -0.9999999999999997780 ) ) ;
#19552=FACE_OUTER_BOUND ( 'NONE', #18876, .T. ) ;
#19559=CARTESIAN_POINT ( 'NONE',  ( 0.7770785076403996516, -9.232944038193473091, -1.768683507966675617 ) ) ;
#19563=CYLINDRICAL_SURFACE ( 'NONE', #30484, 0.4499999999999990119 ) ;
#19568=CARTESIAN_POINT ( 'NONE',  ( 3.285054055080412816, -2.054325274013051460E-30, 1.174876329418460541 ) ) ;
#19572=EDGE_CURVE ( 'NONE', #2424, #19481, #13566, .T. ) ;
#19575=CARTESIAN_POINT ( 'NONE',  ( -4.154892416117755616, -6.512770286199655700, -1.745058604112273981 ) ) ;
#19594=ORIENTED_EDGE ( 'NONE', *, *, #25129, .T. ) ;
#19599=CARTESIAN_POINT ( 'NONE',  ( 0.5282775464098437013, -15.74330118545617552, -1.499999999999998890 ) ) ;
#19606=CARTESIAN_POINT ( 'NONE',  ( 107.9934725388863939, -17.97536830041021005, -4.591573371172586349 ) ) ;
#19617=CARTESIAN_POINT ( 'NONE',  ( -15.35000000000000320, -10.96966150227469505, 4.000000000000000000 ) ) ;
#19622=CYLINDRICAL_SURFACE ( 'NONE', #9255, 0.5000000000000004441 ) ;
#19624=CARTESIAN_POINT ( 'NONE',  ( 7.274195578026668052, -5.507181329334641440, 1.000000000000000000 ) ) ;
#19628=CARTESIAN_POINT ( 'NONE',  ( -2.837798564937276335, -0.5311976243150138277, 1.513817338014894265 ) ) ;
#19632=VERTEX_POINT ( 'NONE', #3708 ) ;
#19639=CARTESIAN_POINT ( 'NONE',  ( 74.30107678963170770, -22.79527490385382649, 1.500000000000000000 ) ) ;
#19647=CARTESIAN_POINT ( 'NONE',  ( 108.0633640349754359, -18.98178845727616704, 3.316617650393312466 ) ) ;
#19664=CARTESIAN_POINT ( 'NONE',  ( 8.528645601772334217, -0.5000000000000000000, -1.500000000000000000 ) ) ;
#19667=CARTESIAN_POINT ( 'NONE',  ( 19.74808449209627526, -17.01894530462115540, 1.753250788838565777 ) ) ;
#19679=CARTESIAN_POINT ( 'NONE',  ( 23.03032540518322335, -21.91564990537378321, -1.226001752879117168 ) ) ;
#19692=ORIENTED_EDGE ( 'NONE', *, *, #2301, .F. ) ;
#19716=CARTESIAN_POINT ( 'NONE',  ( 4.773718314179047795, -12.83538324571378375, -1.756822410893565278 ) ) ;
#19717=CARTESIAN_POINT ( 'NONE',  ( 25.43628654896178176, -17.54453578616395149, 1.000000000000000000 ) ) ;
#19725=ORIENTED_EDGE ( 'NONE', *, *, #1663, .F. ) ;
#19731=CARTESIAN_POINT ( 'NONE',  ( 11.72335232094827440, -20.06224895199573410, -1.500000000000938583 ) ) ;
#19735=CARTESIAN_POINT ( 'NONE',  ( 107.3476768466315008, -15.88628154573193463, 1.499999999999999778 ) ) ;
#19738=ORIENTED_EDGE ( 'NONE', *, *, #20448, .F. ) ;
#19745=CARTESIAN_POINT ( 'NONE',  ( 17.33093461831347781, -21.43932300456618378, 1.500000000000000000 ) ) ;
#19746=ORIENTED_EDGE ( 'NONE', *, *, #327, .T. ) ;
#19753=CARTESIAN_POINT ( 'NONE',  ( -1.427453063608020711, -14.09184579787261349, -1.500000000000000000 ) ) ;
#19760=CARTESIAN_POINT ( 'NONE',  ( 108.0584826075918699, -18.91149711731186756, -4.614517767564248807 ) ) ;
#19762=DIRECTION ( 'NONE',  ( 0.000000000000000000, 0.000000000000000000, -1.000000000000000000 ) ) ;
#19769=CARTESIAN_POINT ( 'NONE',  ( 21.16281565822855981, -21.79884031534714595, -1.349901004997131615 ) ) ;
#19777=ORIENTED_EDGE ( 'NONE', *, *, #27813, .T. ) ;
#19780=CARTESIAN_POINT ( 'NONE',  ( 5.978127801841131017, -13.24614298058319228, -0.9788672205888330202 ) ) ;
#19784=ADVANCED_FACE ( 'NONE', ( #24022 ), #18564, .T. ) ;
#19788=ORIENTED_EDGE ( 'NONE', *, *, #3278, .T. ) ;
#19789=CARTESIAN_POINT ( 'NONE',  ( -2.800010172794385355, -0.4410551771863211457, 1.509141217649250688 ) ) ;
#19798=AXIS2_PLACEMENT_3D ( 'NONE', #19529, #29726, #27191 ) ;
#19800=ORIENTED_EDGE ( 'NONE', *, *, #2609, .T. ) ;
#19804=CARTESIAN_POINT ( 'NONE',  ( 108.1641292914955699, -20.43278308392471132, 1.481931422883725480 ) ) ;
#19806=CARTESIAN_POINT ( 'NONE',  ( 0.3285611067768016147, -13.34342412962908320, -4.522129901861166701 ) ) ;
#19807=CARTESIAN_POINT ( 'NONE',  ( 107.8771114573266630, -16.29979767294532067, -1.280413873165473060 ) ) ;
#19813=CARTESIAN_POINT ( 'NONE',  ( 42.88108885377457824, -22.62752020922544105, 4.522129901861159595 ) ) ;
#19820=EDGE_CURVE ( 'NONE', #25887, #1302, #2134, .T. ) ;
#19822=ORIENTED_EDGE ( 'NONE', *, *, #328, .T. ) ;
#19830=CARTESIAN_POINT ( 'NONE',  ( 14.65326944990388469, -16.14433300766637203, 1.753659756057876162 ) ) ;
#19835=CARTESIAN_POINT ( 'NONE',  ( 7.381887142741853758, -19.12185317620300040, 1.499999999999999556 ) ) ;
#19836=AXIS2_PLACEMENT_3D ( 'NONE', #25330, #30514, #7599 ) ;
#19840=( BOUNDED_SURFACE ( )  B_SPLINE_SURFACE ( 3, 2, ( 
 ( #7008, #17222, #21736 ),
 ( #31945, #15019, #25242 ),
 ( #30120, #4683, #30273 ),
 ( #25564, #32788, #22575 ),
 ( #17702, #10016, #7345 ),
 ( #27731, #17389, #33096 ),
 ( #10362, #17536, #22742 ),
 ( #20395, #15208, #32946 ),
 ( #20227, #14853, #27583 ),
 ( #20077, #5029, #4839 ),
 ( #7694, #25409, #9866 ),
 ( #28084, #30612, #2671 ) ),
 .UNSPECIFIED., .F., .F., .F. ) 
 B_SPLINE_SURFACE_WITH_KNOTS ( ( 4, 2, 2, 2, 2, 4 ),
 ( 3, 3 ),
 ( 0.02103335055035494144, 0.02276256425207544981, 0.02362717110293570399, 0.02405947452836583456, 0.02427562624108089984, 0.02449177795379596165 ),
 ( 0.000000000000000000, 1.000000000000000000 ),
 .UNSPECIFIED. ) 
 GEOMETRIC_REPRESENTATION_ITEM ( )  RATIONAL_B_SPLINE_SURFACE ( (
 ( 1.000000000000000000, 0.8477574071937623579, 1.000000000000000000),
 ( 1.000000000000000000, 0.8716452794067105492, 1.000000000000000000),
 ( 1.000000000000000000, 0.8956763213340630525, 1.000000000000000000),
 ( 1.000000000000000000, 0.9319482906210421191, 1.000000000000000000),
 ( 1.000000000000000000, 0.9440737053929729727, 1.000000000000000000),
 ( 1.000000000000000000, 0.9620964665820456174, 1.000000000000000000),
 ( 1.000000000000000000, 0.9681025352175841592, 1.000000000000000000),
 ( 1.000000000000000000, 0.9768916256375786977, 1.000000000000000000),
 ( 1.000000000000000000, 0.9797842808058671027, 1.000000000000000000),
 ( 1.000000000000000000, 0.9854258872291890015, 1.000000000000000000),
 ( 1.000000000000000000, 0.9882007853475265335, 1.000000000000000000),
 ( 1.000000000000000000, 0.9906937806494865439, 1.000000000000000000) ) ) 
 REPRESENTATION_ITEM ( '' )  SURFACE ( )  );
#19849=DIRECTION ( 'NONE',  ( 1.000000000000000000, 0.000000000000000000, 0.000000000000000000 ) ) ;
#19853=ORIENTED_EDGE ( 'NONE', *, *, #19572, .T. ) ;
#19858=FACE_OUTER_BOUND ( 'NONE', #8547, .T. ) ;
#19867=CARTESIAN_POINT ( 'NONE',  ( -50.60000000000000142, -10.96966150227468972, 1.500000000000000000 ) ) ;
#19877=AXIS2_PLACEMENT_3D ( 'NONE', #27105, #32328, #2203 ) ;
#19879=CARTESIAN_POINT ( 'NONE',  ( 21.45589226044351605, -21.75378945804406072, 1.461253459911962871 ) ) ;
#19898=CARTESIAN_POINT ( 'NONE',  ( 5.359470034614179035, -13.14317863668938990, -1.756412691015132754 ) ) ;
#19899=CARTESIAN_POINT ( 'NONE',  ( 16.80274661516410006, -16.53680364986711737, 1.500000000000000444 ) ) ;
#19918=CARTESIAN_POINT ( 'NONE',  ( 15.90621625741256828, -21.21022000644183692, -1.499999999999999112 ) ) ;
#19922=AXIS2_PLACEMENT_3D ( 'NONE', #19867, #29890, #31914 ) ;
#19924=CARTESIAN_POINT ( 'NONE',  ( 107.3822631069532179, -16.38429022892126241, 2.521216264009422670 ) ) ;
#19928=CIRCLE ( 'NONE', #682, 0.5000000000000000000 ) ;
#19937=PLANE ( 'NONE',  #23635 ) ;
#19941=CARTESIAN_POINT ( 'NONE',  ( -50.60000000000000142, -10.96966150227468972, 7.500000000000000000 ) ) ;
#19950=CARTESIAN_POINT ( 'NONE',  ( 9.134478070116774262, -0.4075412269878618265, -1.500000000000000000 ) ) ;
#19951=ADVANCED_FACE ( 'NONE', ( #17478 ), #18805, .T. ) ;
#19953=CARTESIAN_POINT ( 'NONE',  ( 107.5354980707616761, -18.60211189756912020, -5.018107870159036921 ) ) ;
#19963=CARTESIAN_POINT ( 'NONE',  ( 23.27353278736380204, -21.94187821002792660, -1.000000000000000000 ) ) ;
#19964=CARTESIAN_POINT ( 'NONE',  ( 19.66689578795281790, -21.64324770234364337, -1.457654425243551266 ) ) ;
#19965=ORIENTED_EDGE ( 'NONE', *, *, #19376, .F. ) ;
#19969=ORIENTED_EDGE ( 'NONE', *, *, #29034, .F. ) ;
#19972=CARTESIAN_POINT ( 'NONE',  ( 2.458207506242386930, -0.2539630985812231234, -1.478790212540520344 ) ) ;
#19978=EDGE_LOOP ( 'NONE', ( #2347, #2656, #8874, #18023, #10516 ) ) ;
#19983=EDGE_LOOP ( 'NONE', ( #20054, #7635, #6777, #2989 ) ) ;
#19994=CARTESIAN_POINT ( 'NONE',  ( 107.4500593345382811, -17.36019228850094720, 4.522129901861156931 ) ) ;
#19996=CARTESIAN_POINT ( 'NONE',  ( -50.60000000000000142, -10.96966150227468972, 0.9999999999999991118 ) ) ;
#20022=CARTESIAN_POINT ( 'NONE',  ( -0.5616989984784650503, -12.44624546261628417, -4.522129901861166701 ) ) ;
#20024=CARTESIAN_POINT ( 'NONE',  ( 0.5281637029061487798, -15.74321946213827061, 1.500000000000000222 ) ) ;
#20032=CARTESIAN_POINT ( 'NONE',  ( 21.36441059928002417, -21.76424620013107969, -1.417681050192670877 ) ) ;
#20040=CARTESIAN_POINT ( 'NONE',  ( -15.09999999999999609, 0.000000000000000000, 1.500000000000000000 ) ) ;
#20045=CARTESIAN_POINT ( 'NONE',  ( 23.15652614122341291, -21.92931078907622933, 1.107159753868761198 ) ) ;
#20053=CARTESIAN_POINT ( 'NONE',  ( 1.429697474035917404, -10.23340377719132377, 1.764565172273165228 ) ) ;
#20054=ORIENTED_EDGE ( 'NONE', *, *, #19288, .T. ) ;
#20060=EDGE_CURVE ( 'NONE', #13510, #31647, #4766, .T. ) ;
#20061=FACE_OUTER_BOUND ( 'NONE', #2469, .T. ) ;
#20069=CARTESIAN_POINT ( 'NONE',  ( 0.9579555755618084367, -9.537443266964631405, -1.767394926759007223 ) ) ;
#20077=CARTESIAN_POINT ( 'NONE',  ( 24.25321317639194163, -17.33169478063257429, 1.345077977218910537 ) ) ;
#20082=( BOUNDED_CURVE ( )  B_SPLINE_CURVE ( 3, ( #28607, #23748, #13537, #23405 ),
 .UNSPECIFIED., .F., .F. ) 
 B_SPLINE_CURVE_WITH_KNOTS ( ( 4, 4 ),
 ( 3.333578871309104574, 4.712388980384684345 ),
 .UNSPECIFIED. ) 
 CURVE ( )  GEOMETRIC_REPRESENTATION_ITEM ( )  RATIONAL_B_SPLINE_CURVE ( ( 1.000000000000000000, 0.8477497222584673420, 0.8477497222584673420, 1.000000000000000000 ) ) 
 REPRESENTATION_ITEM ( '' )  );
#20087=CARTESIAN_POINT ( 'NONE',  ( -3.446114928647880493, -10.31582149787081981, -1.743523040558758508 ) ) ;
#20103=ORIENTED_EDGE ( 'NONE', *, *, #14562, .F. ) ;
#20134=VERTEX_POINT ( 'NONE', #21961 ) ;
#20138=CARTESIAN_POINT ( 'NONE',  ( -3.082813266614905068, -0.4373090928652427212, 1.500000000000000000 ) ) ;
#20145=CARTESIAN_POINT ( 'NONE',  ( 21.32535692059155963, -21.82495604402122069, 1.318256435726650633 ) ) ;
#20160=EDGE_CURVE ( 'NONE', #7529, #6546, #31487, .T. ) ;
#20166=CARTESIAN_POINT ( 'NONE',  ( 107.5223429394918071, -18.41085303761574821, 5.107465446621668903 ) ) ;
#20174=CARTESIAN_POINT ( 'NONE',  ( 107.9823348541772390, -17.81498841130776256, -4.403862939664326959 ) ) ;
#20176=ORIENTED_EDGE ( 'NONE', *, *, #4495, .F. ) ;
#20178=CARTESIAN_POINT ( 'NONE',  ( 107.3477315916820913, -15.88627780335592732, -1.500000000000000000 ) ) ;
#20179=EDGE_CURVE ( 'NONE', #593, #5840, #22721, .T. ) ;
#20180=CARTESIAN_POINT ( 'NONE',  ( 21.86019183973456137, -21.78358645912093294, -1.498801117633766999 ) ) ;
#20182=B_SPLINE_CURVE_WITH_KNOTS ( 'NONE', 3,
 ( #27704, #25384, #17863, #20201, #12323, #5310, #15489, #25537, #2492, #25704, #2831, #22543, #27559, #7320, #27883, #13004, #17672, #23215, #20053, #10332, #146, #15332, #2142, #33067, #9837, #10142, #319, #20363, #30247, #4811, #30580, #10491, #7663, #20705, #2643, #17510 ),
 .UNSPECIFIED., .F., .F.,
 ( 4, 2, 2, 2, 2, 2, 2, 2, 2, 2, 2, 2, 2, 2, 2, 2, 2, 4 ),
 ( 0.08639979630981461933, 0.09035893056720895045, 0.09431806482460326768, 0.09827719908199758492, 0.1002567662106947505, 0.1022363333393919160, 0.1042159004680890816, 0.1052056840324376574, 0.1061954675967862471, 0.1081750347254834127, 0.1101546018541805783, 0.1106494936363548731, 0.1111443854185291680, 0.1121341689828777438, 0.1131239525472263197, 0.1141137361115749094, 0.1160933032402720610, 0.1180728703689692266 ),
 .UNSPECIFIED. ) ;
#20188=CARTESIAN_POINT ( 'NONE',  ( -16.96515769256209794, -27.93932300454937590, 11.09540449768827131 ) ) ;
#20192=CARTESIAN_POINT ( 'NONE',  ( 23.11934981620040119, -21.92529594990400099, 1.124851831741630503 ) ) ;
#20194=ADVANCED_FACE ( 'NONE', ( #30497 ), #32854, .T. ) ;
#20201=CARTESIAN_POINT ( 'NONE',  ( 15.82117458021303058, -16.37366068799997265, 1.753541294540382545 ) ) ;
#20216=LINE ( 'NONE', #2853, #17127 ) ;
#20219=FACE_OUTER_BOUND ( 'NONE', #4046, .T. ) ;
#20220=CARTESIAN_POINT ( 'NONE',  ( 0.5309851148689820333, -4.399114163800174282, 1.500000000000000444 ) ) ;
#20227=CARTESIAN_POINT ( 'NONE',  ( 24.12394826718730556, -17.31889127434072506, 1.369171926258124117 ) ) ;
#20234=CARTESIAN_POINT ( 'NONE',  ( 6.168868874606070918, -18.37414512067872607, -1.500000000000239142 ) ) ;
#20244=B_SPLINE_CURVE_WITH_KNOTS ( 'NONE', 3,
 ( #32394, #24493, #6635, #17334, #27028, #1613, #12137, #29710, #6792, #9453 ),
 .UNSPECIFIED., .F., .F.,
 ( 4, 2, 2, 2, 4 ),
 ( -4.729241382666969782E-06, 0.0005792517583992173695, 0.0008712422582901617647, 0.001017237508235635697, 0.001163232758181109629 ),
 .UNSPECIFIED. ) ;
#20260=CARTESIAN_POINT ( 'NONE',  ( 2.482257818914018532, 0.000000000000000000, 1.712210361609934672 ) ) ;
#20262=CARTESIAN_POINT ( 'NONE',  ( -3.789234217576226804, -9.307600915532304953, 1.743674089339463329 ) ) ;
#20263=CARTESIAN_POINT ( 'NONE',  ( 8.254683653268546806, -1.057518490444498971, -1.500000000000000000 ) ) ;
#20270=FACE_OUTER_BOUND ( 'NONE', #6226, .T. ) ;
#20286=EDGE_LOOP ( 'NONE', ( #6242, #20960, #17915 ) ) ;
#20287=CARTESIAN_POINT ( 'NONE',  ( -2.785986023666444211, -0.02407431902794407788, 1.185596063489961383 ) ) ;
#20292=EDGE_CURVE ( 'NONE', #15269, #15578, #5242, .T. ) ;
#20295=DIRECTION ( 'NONE',  ( 1.000000000000000000, 0.000000000000000000, 0.000000000000000000 ) ) ;
#20296=CARTESIAN_POINT ( 'NONE',  ( 0.3277201397524639459, -5.271209332775584677, 1.500000000000000000 ) ) ;
#20298=VECTOR ( 'NONE', #4746, 1000.000000000000000 ) ;
#20305=CYLINDRICAL_SURFACE ( 'NONE', #27326, 6.000000000000001776 ) ;
#20306=CARTESIAN_POINT ( 'NONE',  ( 24.36752972617692592, -17.44836528598961678, 1.442218785864448405 ) ) ;
#20309=CARTESIAN_POINT ( 'NONE',  ( -4.176822952881705575, -3.225712836238914250, 0.9788672205877712029 ) ) ;
#20317=ORIENTED_EDGE ( 'NONE', *, *, #3830, .F. ) ;
#20319=TOROIDAL_SURFACE ( 'NONE', #19234, 6.500000000000002665, 0.5000000000000000000 ) ;
#20322=CARTESIAN_POINT ( 'NONE',  ( 19.75018141867016297, -21.43174828998459702, -1.668660430087435254 ) ) ;
#20329=CARTESIAN_POINT ( 'NONE',  ( 14.13431920379513862, -20.70626837987542856, -1.499999999999999556 ) ) ;
#20339=DIRECTION ( 'NONE',  ( 1.000000000000000000, -0.000000000000000000, -0.000000000000000000 ) ) ;
#20340=CARTESIAN_POINT ( 'NONE',  ( 22.91474828513863216, -21.90304137343319724, -1.273718548422748231 ) ) ;
#20346=B_SPLINE_CURVE_WITH_KNOTS ( 'NONE', 3,
 ( #14211, #4043, #32460, #6206, #26601, #3704 ),
 .UNSPECIFIED., .F., .F.,
 ( 4, 2, 4 ),
 ( 2.626357090645241657E-13, 0.0003954463998646022939, 0.0007908927994665688630 ),
 .UNSPECIFIED. ) ;
#20347=DIRECTION ( 'NONE',  ( -0.000000000000000000, 0.000000000000000000, 1.000000000000000000 ) ) ;
#20352=CARTESIAN_POINT ( 'NONE',  ( 24.70609432061683464, -17.48198453993439117, 1.498641547862707979 ) ) ;
#20355=CARTESIAN_POINT ( 'NONE',  ( 23.18045508973627378, -21.93188832360367257, 1.140730425197365561 ) ) ;
#20358=ORIENTED_EDGE ( 'NONE', *, *, #18173, .T. ) ;
#20361=CIRCLE ( 'NONE', #10202, 5.000000000000000888 ) ;
#20363=CARTESIAN_POINT ( 'NONE',  ( 0.2024771939337984550, -5.520608663253200099, 1.770108805539934327 ) ) ;
#20366=DIRECTION ( 'NONE',  ( -0.1908089953765452762, 0.000000000000000000, -0.9816271834476639757 ) ) ;
#20382=DIRECTION ( 'NONE',  ( -0.000000000000000000, -0.000000000000000000, 1.000000000000000000 ) ) ;
#20384=CARTESIAN_POINT ( 'NONE',  ( 18.48753670594055976, -16.70790065660999346, -1.499999999999860334 ) ) ;
#20395=CARTESIAN_POINT ( 'NONE',  ( 24.05790257984262226, -17.31116499701224853, 1.379149890412948221 ) ) ;
#20399=CARTESIAN_POINT ( 'NONE',  ( 23.67724090058426611, -17.25947716274855281, -1.422757073343587919 ) ) ;
#20406=CARTESIAN_POINT ( 'NONE',  ( 7.453146289620847575, -19.12801665242071181, -1.500000000000000444 ) ) ;
#20410=CARTESIAN_POINT ( 'NONE',  ( 107.8806061109513763, -16.35011981546645998, 2.521000801048293383 ) ) ;
#20422=VERTEX_POINT ( 'NONE', #15775 ) ;
#20427=VECTOR ( 'NONE', #20366, 999.9999999999998863 ) ;
#20428=CARTESIAN_POINT ( 'NONE',  ( 6.655951778521610684, -18.71196003547629516, -1.500000000000000000 ) ) ;
#20437=CARTESIAN_POINT ( 'NONE',  ( -3.353579435673377240, -11.46043295930974004, 1.499999999999999112 ) ) ;
#20440=CARTESIAN_POINT ( 'NONE',  ( 108.0614315348869781, -18.95396093674897386, -4.509855988468532750 ) ) ;
#20442=EDGE_CURVE ( 'NONE', #17869, #5840, #25977, .T. ) ;
#20448=EDGE_CURVE ( 'NONE', #697, #25155, #21462, .T. ) ;
#20456=AXIS2_PLACEMENT_3D ( 'NONE', #28793, #20791, #22513 ) ;
#20458=CARTESIAN_POINT ( 'NONE',  ( -50.60000000000000142, -0.5000000000000000000, -1.500000000000000000 ) ) ;
#20460=ORIENTED_EDGE ( 'NONE', *, *, #8432, .T. ) ;
#20466=CARTESIAN_POINT ( 'NONE',  ( 2.889143798718251333, 0.000000000000000000, -0.9788672205888330202 ) ) ;
#20484=CARTESIAN_POINT ( 'NONE',  ( 0.3277201397524639459, -5.271209332775584677, -1.500000000000000000 ) ) ;
#20492=CARTESIAN_POINT ( 'NONE',  ( 0.9078783126652600899, -4.283561563640669867, 1.499999999999999778 ) ) ;
#20514=CARTESIAN_POINT ( 'NONE',  ( 74.30107678963170770, -22.79527490385382649, -1.499999999999999556 ) ) ;
#20517=CARTESIAN_POINT ( 'NONE',  ( -2.160548182721718113, -12.59940861538154167, 1.743857535748950971 ) ) ;
#20519=ORIENTED_EDGE ( 'NONE', *, *, #21047, .F. ) ;
#20528=CARTESIAN_POINT ( 'NONE',  ( 21.78705206151444074, -21.77640818797000932, -1.495779539311291817 ) ) ;
#20531=DIRECTION ( 'NONE',  ( -0.000000000000000000, 0.000000000000000000, 1.000000000000000000 ) ) ;
#20537=CARTESIAN_POINT ( 'NONE',  ( 108.1300413742128228, -19.95926608421481063, -1.392287898180229133 ) ) ;
#20539=DIRECTION ( 'NONE',  ( 0.000000000000000000, -0.000000000000000000, -1.000000000000000000 ) ) ;
#20540=ORIENTED_EDGE ( 'NONE', *, *, #8723, .T. ) ;
#20544=( BOUNDED_CURVE ( )  B_SPLINE_CURVE ( 3, ( #31924, #11842, #29396, #27211 ),
 .UNSPECIFIED., .F., .F. ) 
 B_SPLINE_CURVE_WITH_KNOTS ( ( 4, 4 ),
 ( 0.1919862177193129571, 1.570796326794901887 ),
 .UNSPECIFIED. ) 
 CURVE ( )  GEOMETRIC_REPRESENTATION_ITEM ( )  RATIONAL_B_SPLINE_CURVE ( ( 1.000000000000000000, 0.8477497222584654546, 0.8477497222584654546, 1.000000000000000000 ) ) 
 REPRESENTATION_ITEM ( '' )  );
#20545=AXIS2_PLACEMENT_3D ( 'NONE', #16959, #1285, #8791 ) ;
#20547=CARTESIAN_POINT ( 'NONE',  ( 3.285049811803533171, 7.727496690442961710E-33, -1.174877964933951802 ) ) ;
#20548=CARTESIAN_POINT ( 'NONE',  ( 9.851448552576139051, -11.91728849018574721, 1.000000000000000000 ) ) ;
#20551=B_SPLINE_CURVE_WITH_KNOTS ( 'NONE', 3,
 ( #30962, #8044, #27620, #2212 ),
 .UNSPECIFIED., .F., .F.,
 ( 4, 4 ),
 ( 0.01682050255738576708, 0.01682075285862154324 ),
 .UNSPECIFIED. ) ;
#20557=EDGE_CURVE ( 'NONE', #28620, #32499, #7900, .T. ) ;
#20563=LINE ( 'NONE', #10161, #19287 ) ;
#20566=CARTESIAN_POINT ( 'NONE',  ( 12.65465643788354200, -15.70291107026620914, 1.500000000000000444 ) ) ;
#20571=CARTESIAN_POINT ( 'NONE',  ( 24.35832023931450507, -17.33818253687174860, -1.317734466820339900 ) ) ;
#20582=CARTESIAN_POINT ( 'NONE',  ( -23.35000000000000142, -10.96966150227469505, 4.500000000000000888 ) ) ;
#20598=DIRECTION ( 'NONE',  ( -0.000000000000000000, 0.000000000000000000, 1.000000000000000000 ) ) ;
#20607=CARTESIAN_POINT ( 'NONE',  ( 0.7297941506389588051, -15.54810501259861688, 1.500000000000000666 ) ) ;
#20610=CARTESIAN_POINT ( 'NONE',  ( 107.3476768466457401, -15.88628154573096651, 1.500000000000000000 ) ) ;
#20611=CARTESIAN_POINT ( 'NONE',  ( 108.0609297225750396, -18.94673496429123105, -4.529582879229646863 ) ) ;
#20624=CARTESIAN_POINT ( 'NONE',  ( 107.5183782604217129, -18.35318718675820904, -5.137737709513164219 ) ) ;
#20629=CARTESIAN_POINT ( 'NONE',  ( 0.1962428234089072521, -6.885380501030516243, -1.500000000000000444 ) ) ;
#20646=CARTESIAN_POINT ( 'NONE',  ( 18.41217767841934716, -16.82117819851176677, -1.753330701571969907 ) ) ;
#20653=CARTESIAN_POINT ( 'NONE',  ( 0.5630063594414467243, -7.169269592067868402, 1.500000000000000222 ) ) ;
#20655=CARTESIAN_POINT ( 'NONE',  ( 107.4500446874326940, -17.36019328965951303, -4.522129901861167589 ) ) ;
#20662=EDGE_LOOP ( 'NONE', ( #11992, #30983, #28483, #3327 ) ) ;
#20675=CARTESIAN_POINT ( 'NONE',  ( -1.218076164763124636, -14.00532792343563848, -1.499999999999999556 ) ) ;
#20678=CARTESIAN_POINT ( 'NONE',  ( -3.406057470504892493, -10.41438730896155462, 1.743528078589993147 ) ) ;
#20688=EDGE_LOOP ( 'NONE', ( #28342, #16708, #31578, #14797 ) ) ;
#20694=CARTESIAN_POINT ( 'NONE',  ( 24.53773319407783760, -17.45675205880590752, 1.481708193828056963 ) ) ;
#20695=DIRECTION ( 'NONE',  ( 0.000000000000000000, 0.000000000000000000, -1.000000000000000000 ) ) ;
#20705=CARTESIAN_POINT ( 'NONE',  ( 1.624846380744160435, -1.458043416193428143, 1.758813134411630230 ) ) ;
#20706=CARTESIAN_POINT ( 'NONE',  ( 25.61042644977005622, -17.59778802277103082, 1.500000000000000000 ) ) ;
#20727=EDGE_LOOP ( 'NONE', ( #21868, #24898, #30867, #16820, #7025, #31734, #12088, #22191 ) ) ;
#20737=ADVANCED_FACE ( 'NONE', ( #2083 ), #7098, .F. ) ;
#20739=CARTESIAN_POINT ( 'NONE',  ( -23.35000000000000142, -10.96966150227469505, 4.000000000000000000 ) ) ;
#20741=DIRECTION ( 'NONE',  ( -0.1908089953765494118, -0.000000000000000000, -0.9816271834476630875 ) ) ;
#20745=ORIENTED_EDGE ( 'NONE', *, *, #13212, .T. ) ;
#20750=CARTESIAN_POINT ( 'NONE',  ( -3.370691070153704949, -1.614088942876946264, 1.500000000000000000 ) ) ;
#20754=DIRECTION ( 'NONE',  ( 0.9816271834476637537, 0.000000000000000000, -0.1908089953765453872 ) ) ;
#20756=CARTESIAN_POINT ( 'NONE',  ( 107.6439010983367410, -20.16588486397409596, 2.098868881559764255 ) ) ;
#20758=CARTESIAN_POINT ( 'NONE',  ( -3.446172085536864049, -10.31568092537763270, 1.743523032603425671 ) ) ;
#20761=DIRECTION ( 'NONE',  ( 1.000000000000000000, 0.000000000000000000, 0.000000000000000000 ) ) ;
#20762=ORIENTED_EDGE ( 'NONE', *, *, #14811, .T. ) ;
#20765=B_SPLINE_CURVE_WITH_KNOTS ( 'NONE', 3,
 ( #16598, #31500, #26638, #1067, #3593, #6586, #23956, #23809, #31685, #8585 ),
 .UNSPECIFIED., .F., .F.,
 ( 4, 2, 2, 2, 4 ),
 ( 0.000000000000000000, 0.002028609684475585380, 0.003042914526713378070, 0.003550066947832274632, 0.004057219368951170760 ),
 .UNSPECIFIED. ) ;
#20773=DIRECTION ( 'NONE',  ( 1.000000000000000000, -2.473959037481237219E-13, 0.000000000000000000 ) ) ;
#20775=DIRECTION ( 'NONE',  ( 0.9816271834476639757, 0.000000000000000000, -0.1908089953765449709 ) ) ;
#20779=CARTESIAN_POINT ( 'NONE',  ( 107.4505400438408742, -17.36716520511782136, 4.540783781969483179 ) ) ;
#20785=ORIENTED_EDGE ( 'NONE', *, *, #2575, .F. ) ;
#20791=DIRECTION ( 'NONE',  ( 2.473959037481237219E-13, 1.000000000000000000, -0.000000000000000000 ) ) ;
#20792=CARTESIAN_POINT ( 'NONE',  ( 3.679561191470742454, -12.16212054601122539, -1.758156634178598798 ) ) ;
#20793=EDGE_CURVE ( 'NONE', #25934, #12596, #27497, .T. ) ;
#20803=CARTESIAN_POINT ( 'NONE',  ( 107.4500520109482409, -17.36019278854280401, -4.522129900387231949 ) ) ;
#20836=CARTESIAN_POINT ( 'NONE',  ( -0.3880080537174158128, -2.647099810594272462, -4.522129901861164925 ) ) ;
#20839=EDGE_CURVE ( 'NONE', #31833, #17869, #25637, .T. ) ;
#20842=CARTESIAN_POINT ( 'NONE',  ( 24.41770876813069791, -17.42528320598814062, 1.442338022868773439 ) ) ;
#20853=CARTESIAN_POINT ( 'NONE',  ( 16.87487612390540903, -15.54663979847974176, 1.500000000000000000 ) ) ;
#20858=CARTESIAN_POINT ( 'NONE',  ( 2.632061376486628301, -0.4999999999999986122, 1.500000000000000000 ) ) ;
#20865=AXIS2_PLACEMENT_3D ( 'NONE', #28924, #15740, #31608 ) ;
#20887=CARTESIAN_POINT ( 'NONE',  ( 17.37538333147394098, -21.16291065652744763, -1.500000000000001554 ) ) ;
#20894=AXIS2_PLACEMENT_3D ( 'NONE', #8439, #6256, #781 ) ;
#20904=AXIS2_PLACEMENT_3D ( 'NONE', #6277, #14134, #31384 ) ;
#20909=ADVANCED_FACE ( 'NONE', ( #4752 ), #3602, .T. ) ;
#20910=VECTOR ( 'NONE', #9136, 1000.000000000000000 ) ;
#20911=CARTESIAN_POINT ( 'NONE',  ( 11.67286638378806352, -13.57952815233281640, 1.499999999999999778 ) ) ;
#20916=ORIENTED_EDGE ( 'NONE', *, *, #32794, .F. ) ;
#20919=EDGE_CURVE ( 'NONE', #1029, #6686, #16851, .T. ) ;
#20920=CARTESIAN_POINT ( 'NONE',  ( -3.686313051336277180, -9.650521517436112973, 1.743567022824936696 ) ) ;
#20923=CARTESIAN_POINT ( 'NONE',  ( 23.29109779593935414, -17.41442569313434063, 1.664431119656365254 ) ) ;
#20933=CARTESIAN_POINT ( 'NONE',  ( 107.9852701348502819, -17.85725572279256212, 4.475774678959534292 ) ) ;
#20941=CARTESIAN_POINT ( 'NONE',  ( -3.043440560540900286, -0.3795130046622989806, -1.490258760090589218 ) ) ;
#20942=CARTESIAN_POINT ( 'NONE',  ( -29.24402871571405882, -25.43932300454937945, 11.00000000000000000 ) ) ;
#20944=DIRECTION ( 'NONE',  ( 0.000000000000000000, -0.000000000000000000, -1.000000000000000000 ) ) ;
#20945=CARTESIAN_POINT ( 'NONE',  ( 107.4510466397278350, -17.37451394313761099, 4.559260914617079052 ) ) ;
#20960=ORIENTED_EDGE ( 'NONE', *, *, #24287, .T. ) ;
#20962=ORIENTED_EDGE ( 'NONE', *, *, #21383, .T. ) ;
#20963=CARTESIAN_POINT ( 'NONE',  ( 0.09007350345950326798, -14.90606730690115000, -1.745535732425882225 ) ) ;
#20966=TOROIDAL_SURFACE ( 'NONE', #22035, 5.500000000000001776, 0.5000000000000000000 ) ;
#20971=VECTOR ( 'NONE', #26798, 1000.000000000000000 ) ;
#20972=CARTESIAN_POINT ( 'NONE',  ( -15.12340757463330654, -27.93932300454937590, -1.000000000000000000 ) ) ;
#20973=CARTESIAN_POINT ( 'NONE',  ( 2.318314390550209048, -10.58246510144062924, 1.499999999999999778 ) ) ;
#20976=LINE ( 'NONE', #28805, #16088 ) ;
#20994=ADVANCED_FACE ( 'NONE', ( #28648 ), #5743, .T. ) ;
#20995=ORIENTED_EDGE ( 'NONE', *, *, #17035, .F. ) ;
#20996=CARTESIAN_POINT ( 'NONE',  ( 107.6300413742128228, -19.95926608421483195, 0.000000000000000000 ) ) ;
#20998=CARTESIAN_POINT ( 'NONE',  ( 18.62789956201168096, -21.71817389964364153, -0.9788672205760856615 ) ) ;
#21011=CARTESIAN_POINT ( 'NONE',  ( -61.56966150227469114, -10.96966150227468972, 1.500000000000000000 ) ) ;
#21014=CIRCLE ( 'NONE', #1803, 2.099999999999997868 ) ;
#21015=AXIS2_PLACEMENT_3D ( 'NONE', #26386, #21035, #11136 ) ;
#21021=AXIS2_PLACEMENT_3D ( 'NONE', #6893, #17085, #8761 ) ;
#21022=AXIS2_PLACEMENT_3D ( 'NONE', #20739, #10863, #26075 ) ;
#21035=DIRECTION ( 'NONE',  ( 0.000000000000000000, -0.000000000000000000, -1.000000000000000000 ) ) ;
#21036=CARTESIAN_POINT ( 'NONE',  ( 9.360049168480738757, -11.53021799169789752, 1.500000000000214939 ) ) ;
#21042=CARTESIAN_POINT ( 'NONE',  ( 0.9355032790606521154, -3.271333551678202056, 1.499999999999860778 ) ) ;
#21047=EDGE_CURVE ( 'NONE', #9004, #21250, #19261, .T. ) ;
#21048=CARTESIAN_POINT ( 'NONE',  ( 2.482257818914018088, 0.000000000000000000, -1.712210361609936005 ) ) ;
#21050=AXIS2_PLACEMENT_3D ( 'NONE', #3676, #3041, #3187 ) ;
#21054=DIRECTION ( 'NONE',  ( -1.000000000000000000, 0.000000000000000000, 0.000000000000000000 ) ) ;
#21056=CARTESIAN_POINT ( 'NONE',  ( 9.350000000000004974, -2.117582368135751233E-18, 1.049909311857671668 ) ) ;
#21073=DIRECTION ( 'NONE',  ( 1.000000000000000000, 0.000000000000000000, 0.000000000000000000 ) ) ;
#21084=CARTESIAN_POINT ( 'NONE',  ( 24.35832023931602208, -17.33818253687209676, 1.317734466820223549 ) ) ;
#21090=CARTESIAN_POINT ( 'NONE',  ( 3.541509388326463004, -13.88765124358303993, -4.522129901861164925 ) ) ;
#21092=CARTESIAN_POINT ( 'NONE',  ( 9.613697478362638549, -12.36077863760316475, 1.500000000000000222 ) ) ;
#21093=CARTESIAN_POINT ( 'NONE',  ( 2.303429269646776412, -1.057870905165122055, -1.499999999999999112 ) ) ;
#21102=ORIENTED_EDGE ( 'NONE', *, *, #30826, .T. ) ;
#21112=CARTESIAN_POINT ( 'NONE',  ( -16.20597128428593336, -10.96966150227469328, -11.50000000000000000 ) ) ;
#21117=EDGE_CURVE ( 'NONE', #5623, #25934, #27632, .T. ) ;
#21118=CARTESIAN_POINT ( 'NONE',  ( -3.167307446159718598, 1.905824131322175763E-18, -1.051955142024793677 ) ) ;
#21121=CARTESIAN_POINT ( 'NONE',  ( 107.9815407526517390, -17.80355354688649072, 4.374676372033779792 ) ) ;
#21122=VERTEX_POINT ( 'NONE', #29642 ) ;
#21125=PLANE ( 'NONE',  #8130 ) ;
#21135=CARTESIAN_POINT ( 'NONE',  ( 22.49117028854483635, -21.89694127986737371, -1.202706146049568048 ) ) ;
#21136=CARTESIAN_POINT ( 'NONE',  ( 20.55552624091252056, -16.63177717300871095, -1.500000000000000666 ) ) ;
#21137=CARTESIAN_POINT ( 'NONE',  ( 107.9807375830284002, -17.79198810411418918, -4.344786411726714981 ) ) ;
#21142=CARTESIAN_POINT ( 'NONE',  ( -0.9232102171129841217, 0.000000000000000000, 4.522129901861158707 ) ) ;
#21154=CARTESIAN_POINT ( 'NONE',  ( 20.72551590764745910, -21.66366526924183233, -1.459983613673072167 ) ) ;
#21160=CARTESIAN_POINT ( 'NONE',  ( 25.41068576271571544, -17.53965252855327961, -1.057866664603150708 ) ) ;
#21162=CARTESIAN_POINT ( 'NONE',  ( -3.659776827764270379, -1.633636780108817854, -0.9788672205760856615 ) ) ;
#21172=CARTESIAN_POINT ( 'NONE',  ( -14.85000000000000142, -10.96966150227469328, 4.000000000000000000 ) ) ;
#21176=B_SPLINE_CURVE_WITH_KNOTS ( 'NONE', 3,
 ( #9653, #12514, #32763, #12168, #27707, #19879, #7831, #4658, #18024, #23027, #27887, #28064 ),
 .UNSPECIFIED., .F., .F.,
 ( 4, 2, 2, 2, 2, 4 ),
 ( 0.000000000000000000, 4.210616338135260222E-05, 8.421232676270520444E-05, 0.0001684246535254206817, 0.0003368493070508517717, 0.0006736986141017032182 ),
 .UNSPECIFIED. ) ;
#21181=EDGE_CURVE ( 'NONE', #1933, #22549, #7690, .T. ) ;
#21183=CARTESIAN_POINT ( 'NONE',  ( 22.23605616177110278, -21.82696876987042600, 1.456498850422674574 ) ) ;
#21184=CARTESIAN_POINT ( 'NONE',  ( -50.60000000000000142, 0.000000000000000000, -1.000000000000000000 ) ) ;
#21192=CARTESIAN_POINT ( 'NONE',  ( 8.486535498532832733, -10.66169397763358795, 1.500000000000000000 ) ) ;
#21196=CARTESIAN_POINT ( 'NONE',  ( 2.303449397150664435, -1.057836737633686353, 1.500000000000000000 ) ) ;
#21204=CARTESIAN_POINT ( 'NONE',  ( -31.59999999999999787, -25.43932300454937945, 11.50000000000000000 ) ) ;
#21206=CARTESIAN_POINT ( 'NONE',  ( 8.862909208978496878, -0.2945138977690186510, 1.470869863057392424 ) ) ;
#21207=DIRECTION ( 'NONE',  ( -1.000000000000000000, 0.000000000000000000, 0.000000000000000000 ) ) ;
#21236=EDGE_LOOP ( 'NONE', ( #25801, #20745, #20995, #6941 ) ) ;
#21240=CARTESIAN_POINT ( 'NONE',  ( 6.963573770753491488, -4.510305581628904825, 1.500000000000000444 ) ) ;
#21241=CARTESIAN_POINT ( 'NONE',  ( 0.2683958477397258569, -5.146640226071303559, -1.768824076817805402 ) ) ;
#21246=FACE_OUTER_BOUND ( 'NONE', #28263, .T. ) ;
#21249=CARTESIAN_POINT ( 'NONE',  ( 21.03177542174608661, -17.18603084754167298, 1.753176640694532162 ) ) ;
#21250=VERTEX_POINT ( 'NONE', #22423 ) ;
#21257=CARTESIAN_POINT ( 'NONE',  ( -2.962625823238647982, -0.001292792641206102827, -0.8472062597617540103 ) ) ;
#21266=CARTESIAN_POINT ( 'NONE',  ( 107.9910885158944041, -17.94103896239631979, 4.566504411386732798 ) ) ;
#21276=DIRECTION ( 'NONE',  ( -1.000000000000000000, 0.000000000000000000, 0.000000000000000000 ) ) ;
#21280=CARTESIAN_POINT ( 'NONE',  ( 3.722807861074314939, -17.21380748779928993, -1.747812250015838176 ) ) ;
#21283=CARTESIAN_POINT ( 'NONE',  ( 107.4494260027903465, -17.35107267642216655, -4.497208115429102371 ) ) ;
#21290=CARTESIAN_POINT ( 'NONE',  ( 2.648464616715299424, 0.1990047044050357872, 1.630908343631527258 ) ) ;
#21297=CARTESIAN_POINT ( 'NONE',  ( 20.69942760064582998, -21.74528614261393500, -1.396244390127318491 ) ) ;
#21299=CARTESIAN_POINT ( 'NONE',  ( 10.97445643284022587, -14.84313750102852225, -1.499999999999999112 ) ) ;
#21305=CARTESIAN_POINT ( 'NONE',  ( 6.691656545361666986, -18.99987508458807639, -0.9788672205760856615 ) ) ;
#21306=ORIENTED_EDGE ( 'NONE', *, *, #1872, .F. ) ;
#21307=ORIENTED_EDGE ( 'NONE', *, *, #13487, .F. ) ;
#21308=DIRECTION ( 'NONE',  ( -1.000000000000000000, 0.000000000000000000, 0.000000000000000000 ) ) ;
#21318=EDGE_CURVE ( 'NONE', #11856, #7812, #9069, .T. ) ;
#21319=CARTESIAN_POINT ( 'NONE',  ( 108.0290699101298202, -18.48796159080449542, 4.329927758675821359 ) ) ;
#21320=( BOUNDED_CURVE ( )  B_SPLINE_CURVE ( 3, ( #21851, #11339, #27043, #4146 ),
 .UNSPECIFIED., .F., .F. ) 
 B_SPLINE_CURVE_WITH_KNOTS ( ( 4, 4 ),
 ( 4.520402762664171625, 4.712388980383413362 ),
 .UNSPECIFIED. ) 
 CURVE ( )  GEOMETRIC_REPRESENTATION_ITEM ( )  RATIONAL_B_SPLINE_CURVE ( ( 1.000000000000000000, 0.9969307989114568613, 0.9969307989114568613, 1.000000000000000000 ) ) 
 REPRESENTATION_ITEM ( '' )  );
#21326=DIRECTION ( 'NONE',  ( 0.000000000000000000, -0.000000000000000000, -1.000000000000000000 ) ) ;
#21329=CARTESIAN_POINT ( 'NONE',  ( 21.34414429286333714, -21.72097900651761648, 1.443623072031003485 ) ) ;
#21334=CIRCLE ( 'NONE', #32565, 2.099999999999997868 ) ;
#21343=CARTESIAN_POINT ( 'NONE',  ( 0.2685008736531913076, -5.146116540876891854, 1.768822251658703326 ) ) ;
#21348=CARTESIAN_POINT ( 'NONE',  ( 23.85741365831132654, -17.28578219493638812, -1.405688364266028056 ) ) ;
#21352=DIRECTION ( 'NONE',  ( 0.000000000000000000, 0.000000000000000000, -1.000000000000000000 ) ) ;
#21356=VECTOR ( 'NONE', #23310, 1000.000000000000114 ) ;
#21366=CARTESIAN_POINT ( 'NONE',  ( 108.0374854960985687, -18.60914393521796839, 4.376826314212413749 ) ) ;
#21368=CARTESIAN_POINT ( 'NONE',  ( 108.1300413742128228, -19.95926608421463300, 1.392287898181946426 ) ) ;
#21369=CARTESIAN_POINT ( 'NONE',  ( 13.54302414779168373, -18.70685303420125223, 5.485967528433935314 ) ) ;
#21370=CARTESIAN_POINT ( 'NONE',  ( 24.73877499206001218, -17.41122639143721784, 1.266735320468793224 ) ) ;
#21376=CARTESIAN_POINT ( 'NONE',  ( 0.000000000000000000, -0.5000000000000000000, -1.500000000000000000 ) ) ;
#21383=EDGE_CURVE ( 'NONE', #20134, #29829, #2181, .T. ) ;
#21389=CARTESIAN_POINT ( 'NONE',  ( 9.369450431866805928, -11.55901544634946987, -0.9999999999999997780 ) ) ;
#21390=VERTEX_POINT ( 'NONE', #5847 ) ;
#21394=EDGE_CURVE ( 'NONE', #10544, #29208, #27775, .T. ) ;
#21395=CARTESIAN_POINT ( 'NONE',  ( 0.1610798642962581184, -10.72944008624797974, -4.522129901861164925 ) ) ;
#21397=CARTESIAN_POINT ( 'NONE',  ( 10.51239158225386383, -12.94889321834415341, 1.500000000000000000 ) ) ;
#21398=CARTESIAN_POINT ( 'NONE',  ( 0.2475851010963652510, -6.181414723257675270, -1.499999999999999556 ) ) ;
#21426=ORIENTED_EDGE ( 'NONE', *, *, #16016, .F. ) ;
#21428=CARTESIAN_POINT ( 'NONE',  ( 25.43628654896178887, -17.54453578616395504, 1.000000000000000000 ) ) ;
#21432=CARTESIAN_POINT ( 'NONE',  ( 24.37017644008354722, -17.36705458137034697, 1.347230727348949442 ) ) ;
#21433=VERTEX_POINT ( 'NONE', #24734 ) ;
#21437=VECTOR ( 'NONE', #4751, 1000.000000000000000 ) ;
#21446=CARTESIAN_POINT ( 'NONE',  ( 108.0920678934618593, -19.39511687885960356, -2.469487401138616534 ) ) ;
#21447=CARTESIAN_POINT ( 'NONE',  ( 7.362531901230324749, -8.542914936813222226, -1.499999999999856559 ) ) ;
#21449=CARTESIAN_POINT ( 'NONE',  ( 107.9488496542534648, -17.33280986247086375, -4.539927485673689311 ) ) ;
#21453=CIRCLE ( 'NONE', #15584, 6.500000000000002665 ) ;
#21462=B_SPLINE_CURVE_WITH_KNOTS ( 'NONE', 3,
 ( #13729, #21432, #30987, #31649 ),
 .UNSPECIFIED., .F., .F.,
 ( 4, 4 ),
 ( -7.558714329344716932E-06, 0.0001212692847099137061 ),
 .UNSPECIFIED. ) ;
#21463=AXIS2_PLACEMENT_3D ( 'NONE', #13581, #23787, #21276 ) ;
#21477=CARTESIAN_POINT ( 'NONE',  ( 25.49907528997228923, -17.55969604403593110, -1.109946655923441883 ) ) ;
#21485=CIRCLE ( 'NONE', #17204, 0.9999999999999991118 ) ;
#21487=CIRCLE ( 'NONE', #32692, 8.500000000000000000 ) ;
#21489=CARTESIAN_POINT ( 'NONE',  ( -0.5616989984783457013, -12.44624546261724163, 4.522129901861158707 ) ) ;
#21496=LINE ( 'NONE', #21973, #27752 ) ;
#21499=CARTESIAN_POINT ( 'NONE',  ( 108.0293210873539067, -18.49157848034651153, 4.320045722282116252 ) ) ;
#21500=CARTESIAN_POINT ( 'NONE',  ( 0.1610798642962581184, -10.72944008624893542, -4.522129901861164925 ) ) ;
#21503=DIRECTION ( 'NONE',  ( -1.000000000000000000, -0.000000000000000000, -0.000000000000000000 ) ) ;
#21507=CARTESIAN_POINT ( 'NONE',  ( 107.3477315916820913, -15.88627780335592732, -1.500000000000000000 ) ) ;
#21513=VERTEX_POINT ( 'NONE', #32441 ) ;
#21518=CARTESIAN_POINT ( 'NONE',  ( 8.060276137098854932, -2.738905750061799704, 1.000000000000000000 ) ) ;
#21521=CARTESIAN_POINT ( 'NONE',  ( 10.28480887676876243, -12.81065604946471304, -1.500000000000000666 ) ) ;
#21523=B_SPLINE_CURVE_WITH_KNOTS ( 'NONE', 3,
 ( #19664, #31732, #32388, #21676, #3635, #22000, #19336, #32038, #19158, #19012, #29198, #1454, #9447, #23996, #29349, #22178, #11631, #9107, #31883, #29542, #6628, #21521, #27171, #9293, #14142, #16643, #16821, #29858, #19510, #1117, #27020, #6439 ),
 .UNSPECIFIED., .F., .F.,
 ( 4, 2, 2, 2, 2, 2, 2, 2, 2, 2, 2, 2, 2, 2, 2, 4 ),
 ( 8.673617379884035472E-19, 0.003232788846018234963, 0.004849183269027351577, 0.006465577692036469058, 0.008081972115045587407, 0.008890169326550144413, 0.009698366538054701419, 0.01050656374955926189, 0.01131476096106382237, 0.01293115538407293985, 0.01373935259557750033, 0.01454754980708205733, 0.01616394423009118522, 0.01939673307610943406, 0.02262952192212768984, 0.02586231076814594909 ),
 .UNSPECIFIED. ) ;
#21525=CARTESIAN_POINT ( 'NONE',  ( 0.2331433898338126642, -7.747061788033508201, 1.773832612458838609 ) ) ;
#21531=CARTESIAN_POINT ( 'NONE',  ( 22.17497728449690086, -17.32537947343252682, -1.743178009048997001 ) ) ;
#21541=DIRECTION ( 'NONE',  ( 0.000000000000000000, 0.000000000000000000, -1.000000000000000000 ) ) ;
#21545=DIRECTION ( 'NONE',  ( 0.000000000000000000, 0.000000000000000000, -1.000000000000000000 ) ) ;
#21550=CARTESIAN_POINT ( 'NONE',  ( 0.4398628304357217744, -12.95602692781729992, 5.485967528433935314 ) ) ;
#21553=CARTESIAN_POINT ( 'NONE',  ( 25.36291098745260797, -17.54678857751243370, -1.252584024796136175 ) ) ;
#21563=ORIENTED_EDGE ( 'NONE', *, *, #20179, .T. ) ;
#21577=DIRECTION ( 'NONE',  ( 0.000000000000000000, 0.000000000000000000, -1.000000000000000000 ) ) ;
#21580=AXIS2_PLACEMENT_3D ( 'NONE', #32337, #14584, #4886 ) ;
#21585=CARTESIAN_POINT ( 'NONE',  ( 23.00820037127764550, -17.39482224626776130, 1.688990564600256761 ) ) ;
#21586=VERTEX_POINT ( 'NONE', #19717 ) ;
#21591=CARTESIAN_POINT ( 'NONE',  ( -4.161545776608246427, -8.294432461897566000, -1.500000000000000000 ) ) ;
#21613=CARTESIAN_POINT ( 'NONE',  ( -3.192834903017093051, -11.75164088162766873, -1.500000000000000222 ) ) ;
#21614=VERTEX_POINT ( 'NONE', #27909 ) ;
#21616=CARTESIAN_POINT ( 'NONE',  ( -2.373172266667121555, -12.30297787492008688, -1.743844711840834449 ) ) ;
#21619=CARTESIAN_POINT ( 'NONE',  ( 7.931701156346584014, -9.929036423919631815, -1.500000000000359934 ) ) ;
#21620=CARTESIAN_POINT ( 'NONE',  ( 107.9107100874947349, -16.78360958907837031, -2.272491201332555555 ) ) ;
#21622=VECTOR ( 'NONE', #14746, 1000.000000000000000 ) ;
#21623=ADVANCED_FACE ( 'NONE', ( #17694 ), #13984, .T. ) ;
#21639=B_SPLINE_CURVE_WITH_KNOTS ( 'NONE', 3,
 ( #5696, #13691, #18903, #11035, #16216, #1169 ),
 .UNSPECIFIED., .F., .F.,
 ( 4, 2, 4 ),
 ( 6.133173666733496745E-19, 0.0003885750149250817857, 0.0007771500298501630294 ),
 .UNSPECIFIED. ) ;
#21641=CARTESIAN_POINT ( 'NONE',  ( 24.61821134308479841, -17.47399247671392430, -1.556972331815056121 ) ) ;
#21646=DIRECTION ( 'NONE',  ( -0.000000000000000000, -0.000000000000000000, -1.000000000000000000 ) ) ;
#21648=ORIENTED_EDGE ( 'NONE', *, *, #27368, .F. ) ;
#21657=CARTESIAN_POINT ( 'NONE',  ( 108.0610369550560250, -18.94827908534190897, 4.525375360948980408 ) ) ;
#21658=CARTESIAN_POINT ( 'NONE',  ( -1.671916146696470262, -10.12145986844939394, -5.485967528433938867 ) ) ;
#21666=ADVANCED_FACE ( 'NONE', ( #25727 ), #20319, .T. ) ;
#21673=DIRECTION ( 'NONE',  ( 0.1908089953765452484, 0.000000000000000000, 0.9816271834476638647 ) ) ;
#21674=CARTESIAN_POINT ( 'NONE',  ( 7.168700581566836760, -6.410142746917610879, 1.500000000000000222 ) ) ;
#21676=CARTESIAN_POINT ( 'NONE',  ( 7.106060642427864948, -3.992384276486344863, -1.499999999999999778 ) ) ;
#21678=CARTESIAN_POINT ( 'NONE',  ( 0.3845462673029811929, -5.169103183424899939, 1.499999999999964695 ) ) ;
#21682=EDGE_CURVE ( 'NONE', #15401, #4392, #32501, .T. ) ;
#21686=CARTESIAN_POINT ( 'NONE',  ( 21.59695500783953293, -17.14749606024714979, -1.524646196215473593 ) ) ;
#21689=CARTESIAN_POINT ( 'NONE',  ( 23.19969962673269492, -21.93395824423269147, -1.123858796072322974 ) ) ;
#21702=FACE_OUTER_BOUND ( 'NONE', #24139, .T. ) ;
#21703=CARTESIAN_POINT ( 'NONE',  ( -0.5616989984783476997, -12.44624546261724518, 4.522129901861159595 ) ) ;
#21719=CARTESIAN_POINT ( 'NONE',  ( 8.250826798929582040, -2.275785942832204256, -1.000000000000000000 ) ) ;
#21727=CARTESIAN_POINT ( 'NONE',  ( 0.6277548181752619083, -4.204133288872636598, -1.499999999999860778 ) ) ;
#21736=CARTESIAN_POINT ( 'NONE',  ( 21.03177542174608661, -17.18603084754167298, 1.753176640694531274 ) ) ;
#21739=FACE_OUTER_BOUND ( 'NONE', #20286, .T. ) ;
#21740=ADVANCED_FACE ( 'NONE', ( #14159 ), #5353, .T. ) ;
#21754=CARTESIAN_POINT ( 'NONE',  ( 22.17354848663391920, -17.00157258782028080, 1.495009212619065497 ) ) ;
#21758=CARTESIAN_POINT ( 'NONE',  ( 21.32535692059145660, -21.82495604402121003, -1.318256435726663955 ) ) ;
#21760=ORIENTED_EDGE ( 'NONE', *, *, #3062, .F. ) ;
#21764=CARTESIAN_POINT ( 'NONE',  ( -0.6222083319099647181, -14.83248753350331306, -1.499999999999999334 ) ) ;
#21768=CARTESIAN_POINT ( 'NONE',  ( 108.0331448824852032, -18.54664017899650830, -4.208585127045829211 ) ) ;
#21769=CARTESIAN_POINT ( 'NONE',  ( 10.11068945975151756, -12.10067465534980080, -1.000000000000000000 ) ) ;
#21770=CARTESIAN_POINT ( 'NONE',  ( 107.9600896886990853, -17.49466356266586686, -4.826758019528888610 ) ) ;
#21787=CARTESIAN_POINT ( 'NONE',  ( 3.858046770353062982, -11.79229388856150784, -1.499999999999999556 ) ) ;
#21792=CARTESIAN_POINT ( 'NONE',  ( 25.48003164478615190, -17.55790041459374962, -1.000000000000000444 ) ) ;
#21793=EDGE_CURVE ( 'NONE', #31825, #7812, #27188, .T. ) ;
#21794=CARTESIAN_POINT ( 'NONE',  ( 21.04494988260864474, -21.68420912488519647, -1.499840339240438469 ) ) ;
#21806=DIRECTION ( 'NONE',  ( 0.1908089953765452762, 0.000000000000000000, 0.9816271834476639757 ) ) ;
#21809=CARTESIAN_POINT ( 'NONE',  ( 107.5624059028085497, -18.99272140073565751, 4.497205547310911378 ) ) ;
#21814=DIRECTION ( 'NONE',  ( -1.387778780781444413E-14, -1.000000000000000000, 0.000000000000000000 ) ) ;
#21827=B_SPLINE_CURVE_WITH_KNOTS ( 'NONE', 3,
 ( #29864, #14957, #4129, #29548, #2292, #19835, #9802, #11803, #22011, #20024, #12293, #14458, #14295, #25171, #9615, #12478, #16826, #27359, #32234, #22505, #22184, #19516, #1801, #9300, #7138, #22690, #11988, #6946, #9116, #19345, #17147, #4475 ),
 .UNSPECIFIED., .F., .F.,
 ( 4, 2, 2, 2, 2, 2, 2, 2, 2, 2, 2, 2, 2, 2, 2, 4 ),
 ( 0.000000000000000000, 0.004377979416501958515, 0.008755958833003917030, 0.01313393824950587208, 0.01751191766600783059, 0.01860641252013331415, 0.01970090737425880464, 0.02188989708250978217, 0.02298439193663526572, 0.02407888679076075275, 0.02517338164488623631, 0.02626787649901171987, 0.02845686620726269739, 0.02955136106138818441, 0.03064585591551366797, 0.03502383533201561261 ),
 .UNSPECIFIED. ) ;
#21829=CARTESIAN_POINT ( 'NONE',  ( 0.1143091695231461258, -6.518402738280636655, 1.773884761005948274 ) ) ;
#21846=CARTESIAN_POINT ( 'NONE',  ( -31.67864539881508179, -21.93013659627822776, 1.095404497688272194 ) ) ;
#21851=CARTESIAN_POINT ( 'NONE',  ( -31.67864539881508179, -21.93013659627822776, 1.095404497688272194 ) ) ;
#21853=DIRECTION ( 'NONE',  ( 0.000000000000000000, 0.000000000000000000, -1.000000000000000000 ) ) ;
#21861=DIRECTION ( 'NONE',  ( -0.000000000000000000, -1.000000000000000000, -0.000000000000000000 ) ) ;
#21867=VECTOR ( 'NONE', #15657, 1000.000000000000000 ) ;
#21868=ORIENTED_EDGE ( 'NONE', *, *, #9385, .T. ) ;
#21873=CARTESIAN_POINT ( 'NONE',  ( 8.013022481854630286, -2.861148639377020686, -1.000000000000000000 ) ) ;
#21882=CARTESIAN_POINT ( 'NONE',  ( 7.168280658702385288, -13.96541762984794310, -1.755547115761689314 ) ) ;
#21890=VERTEX_POINT ( 'NONE', #13110 ) ;
#21900=CARTESIAN_POINT ( 'NONE',  ( -23.35000000000000142, -10.96966150227469505, -1.499999999999999556 ) ) ;
#21918=DIRECTION ( 'NONE',  ( 1.000000000000000000, 0.000000000000000000, 0.000000000000000000 ) ) ;
#21926=CYLINDRICAL_SURFACE ( 'NONE', #21463, 4.999999999999997335 ) ;
#21927=CARTESIAN_POINT ( 'NONE',  ( -3.135269660805078740, -0.5000000000000000000, -1.500000000000000000 ) ) ;
#21933=CARTESIAN_POINT ( 'NONE',  ( 12.08436850396365259, -13.77779907615468247, -1.500000000000000000 ) ) ;
#21934=CARTESIAN_POINT ( 'NONE',  ( 108.0402073727359351, -18.64833828181508224, -4.957871595061241088 ) ) ;
#21937=CIRCLE ( 'NONE', #28879, 0.5000000000000008882 ) ;
#21944=CIRCLE ( 'NONE', #12320, 0.5000000000000004441 ) ;
#21948=AXIS2_PLACEMENT_3D ( 'NONE', #11335, #3814, #21545 ) ;
#21951=CARTESIAN_POINT ( 'NONE',  ( -5.304000690461529555E-12, -21.43932300456189566, -1.000000000000000000 ) ) ;
#21961=CARTESIAN_POINT ( 'NONE',  ( -46.10000000000000142, -10.96966150227468972, 7.500000000000000000 ) ) ;
#21968=CARTESIAN_POINT ( 'NONE',  ( -5.304000690461529555E-12, -21.43932300456189566, -1.500000000000000000 ) ) ;
#21973=CARTESIAN_POINT ( 'NONE',  ( -29.65619690862280677, -27.93932300454937590, 11.50000000000000000 ) ) ;
#21978=CARTESIAN_POINT ( 'NONE',  ( -1.293118168543757385, -1.473601950426213447, -5.485967528433938867 ) ) ;
#21985=DIRECTION ( 'NONE',  ( 0.000000000000000000, 0.000000000000000000, -1.000000000000000000 ) ) ;
#21986=DIRECTION ( 'NONE',  ( 0.000000000000000000, -1.000000000000000000, 0.000000000000000000 ) ) ;
#21996=CARTESIAN_POINT ( 'NONE',  ( 6.694810660865657681, -7.699995848972423396, 1.500000000000000000 ) ) ;
#22000=CARTESIAN_POINT ( 'NONE',  ( 6.751043368244978637, -5.560327249377557735, -1.500000000000000000 ) ) ;
#22006=CARTESIAN_POINT ( 'NONE',  ( 0.7768566917565598029, -9.232541975952356594, 1.768685230608914694 ) ) ;
#22011=CARTESIAN_POINT ( 'NONE',  ( 2.040190332798762274, -16.78709061960636006, 1.500000000000000444 ) ) ;
#22014=B_SPLINE_CURVE_WITH_KNOTS ( 'NONE', 3,
 ( #25517, #9970, #4974, #2625 ),
 .UNSPECIFIED., .F., .F.,
 ( 4, 4 ),
 ( 0.01682050255744390113, 0.01682075285862147038 ),
 .UNSPECIFIED. ) ;
#22017=CARTESIAN_POINT ( 'NONE',  ( 23.88966202700583707, -17.43474874481648484, -1.573876621503120576 ) ) ;
#22020=EDGE_CURVE ( 'NONE', #926, #7472, #2756, .T. ) ;
#22021=CARTESIAN_POINT ( 'NONE',  ( 23.09498300328091247, -21.93193249238094822, -1.086362660086072296 ) ) ;
#22026=CIRCLE ( 'NONE', #16666, 10.46966150227469150 ) ;
#22035=AXIS2_PLACEMENT_3D ( 'NONE', #8050, #2405, #5575 ) ;
#22036=AXIS2_PLACEMENT_3D ( 'NONE', #31345, #13262, #11093 ) ;
#22039=DIRECTION ( 'NONE',  ( 0.000000000000000000, 0.000000000000000000, -1.000000000000000000 ) ) ;
#22044=ORIENTED_EDGE ( 'NONE', *, *, #11401, .T. ) ;
#22064=VECTOR ( 'NONE', #11650, 1000.000000000000000 ) ;
#22065=ORIENTED_EDGE ( 'NONE', *, *, #29364, .F. ) ;
#22072=CARTESIAN_POINT ( 'NONE',  ( 1.873231708749834912, -10.12253852703719126, -1.500000000000000000 ) ) ;
#22078=CARTESIAN_POINT ( 'NONE',  ( -15.12340757463330654, -21.43932300455815465, -1.500000000000000000 ) ) ;
#22080=CARTESIAN_POINT ( 'NONE',  ( 2.482257818914018532, 0.000000000000000000, 1.712210361609934672 ) ) ;
#22086=AXIS2_PLACEMENT_3D ( 'NONE', #4320, #22362, #24709 ) ;
#22092=CARTESIAN_POINT ( 'NONE',  ( -3.789055215328666737, -3.339008135070082872, -1.747105332058888738 ) ) ;
#22100=EDGE_LOOP ( 'NONE', ( #3316, #12299, #13957, #9216 ) ) ;
#22103=CARTESIAN_POINT ( 'NONE',  ( 21.62838417909457434, -16.89547707397456833, 1.499999999999873879 ) ) ;
#22114=LINE ( 'NONE', #17415, #5992 ) ;
#22115=EDGE_CURVE ( 'NONE', #9547, #24839, #25677, .T. ) ;
#22123=CARTESIAN_POINT ( 'NONE',  ( 107.9881338863072955, -17.89849303138035808, -5.107378633373170551 ) ) ;
#22128=ADVANCED_FACE ( 'NONE', ( #6231 ), #28808, .T. ) ;
#22136=PLANE ( 'NONE',  #1779 ) ;
#22139=CARTESIAN_POINT ( 'NONE',  ( 2.748213864407169638, 0.2993382933193693418, -1.561876010259312775 ) ) ;
#22145=CARTESIAN_POINT ( 'NONE',  ( -2.880987360464337677, -0.6119841066606553914, 1.500000000000000000 ) ) ;
#22146=CARTESIAN_POINT ( 'NONE',  ( 20.71913853892379009, -21.61372392228101802, -1.559032431776657068 ) ) ;
#22152=CARTESIAN_POINT ( 'NONE',  ( -1.218076164763124636, -14.00532792343563848, 1.500000000000000000 ) ) ;
#22172=VERTEX_POINT ( 'NONE', #30817 ) ;
#22178=CARTESIAN_POINT ( 'NONE',  ( 7.868768533615001282, -10.68327055928632063, -1.499999999999999778 ) ) ;
#22183=VERTEX_POINT ( 'NONE', #10550 ) ;
#22184=CARTESIAN_POINT ( 'NONE',  ( -3.828326524025771782, -10.43756472495370247, 1.499999999999999778 ) ) ;
#22191=ORIENTED_EDGE ( 'NONE', *, *, #28996, .T. ) ;
#22193=CARTESIAN_POINT ( 'NONE',  ( 23.27353193731599745, -21.94187811905321794, -1.045377498472113587 ) ) ;
#22222=CARTESIAN_POINT ( 'NONE',  ( 7.259701896292244605, -5.595974087570425581, -0.9999999999999997780 ) ) ;
#22225=ADVANCED_FACE ( 'NONE', ( #227 ), #5912, .T. ) ;
#22230=CARTESIAN_POINT ( 'NONE',  ( 0.1996956927336154264, -7.570410372035627944, -1.774174135624665638 ) ) ;
#22236=CARTESIAN_POINT ( 'NONE',  ( 17.33093461831546378, -21.43932300456649642, -1.950000000000000178 ) ) ;
#22237=EDGE_CURVE ( 'NONE', #30215, #24312, #20551, .T. ) ;
#22239=CARTESIAN_POINT ( 'NONE',  ( 3.744708216408842549, 0.000000000000000000, 1.000000000000000000 ) ) ;
#22241=EDGE_CURVE ( 'NONE', #25155, #16376, #31678, .T. ) ;
#22247=CARTESIAN_POINT ( 'NONE',  ( 6.070010019446702820, -18.63414725979056641, -1.500000000000000444 ) ) ;
#22251=ORIENTED_EDGE ( 'NONE', *, *, #32998, .T. ) ;
#22268=CARTESIAN_POINT ( 'NONE',  ( 107.4094642854696104, -16.77596786109937099, 3.324293658051870715 ) ) ;
#22269=ORIENTED_EDGE ( 'NONE', *, *, #743, .F. ) ;
#22270=DIRECTION ( 'NONE',  ( 1.000000000000000000, 0.000000000000000000, 0.000000000000000000 ) ) ;
#22274=CARTESIAN_POINT ( 'NONE',  ( 8.845957756505633540, -0.9823800962674188453, -1.000000000000000000 ) ) ;
#22275=CARTESIAN_POINT ( 'NONE',  ( 107.5220891496032891, -18.40716237041415937, -5.108771864772584159 ) ) ;
#22276=ORIENTED_EDGE ( 'NONE', *, *, #29625, .F. ) ;
#22292=CARTESIAN_POINT ( 'NONE',  ( 16.70660563659856734, -16.26387199941004624, -0.9788672205888330202 ) ) ;
#22296=ORIENTED_EDGE ( 'NONE', *, *, #17900, .F. ) ;
#22306=CARTESIAN_POINT ( 'NONE',  ( -50.60000000000000142, -10.96966150227468972, 7.500000000000000000 ) ) ;
#22312=CARTESIAN_POINT ( 'NONE',  ( -0.5220033361344396106, 0.000000000000000000, -5.485967528433938867 ) ) ;
#22313=CARTESIAN_POINT ( 'NONE',  ( 107.9151932993304968, -16.84816672442089569, -3.542199815890097359 ) ) ;
#22314=DIRECTION ( 'NONE',  ( 1.000000000000000000, 0.000000000000000000, 0.000000000000000000 ) ) ;
#22315=CARTESIAN_POINT ( 'NONE',  ( -29.65619690862280677, -28.43932300454937590, 11.00000000000000000 ) ) ;
#22316=CARTESIAN_POINT ( 'NONE',  ( -1.921189184902825975, -10.44034746380417822, 4.522129901861159595 ) ) ;
#22326=ORIENTED_EDGE ( 'NONE', *, *, #201, .T. ) ;
#22333=ORIENTED_EDGE ( 'NONE', *, *, #17594, .T. ) ;
#22344=CARTESIAN_POINT ( 'NONE',  ( 21.45958739454658115, -21.75417579598725126, -1.461374457712235175 ) ) ;
#22355=CARTESIAN_POINT ( 'NONE',  ( -31.57659242536668032, -21.93932300455408324, -1.000000000000000000 ) ) ;
#22356=CARTESIAN_POINT ( 'NONE',  ( 23.27353193731607206, -21.94187811905322505, 1.045377498471069089 ) ) ;
#22362=DIRECTION ( 'NONE',  ( 0.000000000000000000, 0.000000000000000000, -1.000000000000000000 ) ) ;
#22363=DIRECTION ( 'NONE',  ( 0.1908089953765420843, -0.000000000000000000, -0.9816271834476646418 ) ) ;
#22367=ADVANCED_FACE ( 'NONE', ( #18918 ), #31143, .T. ) ;
#22373=EDGE_CURVE ( 'NONE', #28214, #30338, #9560, .T. ) ;
#22374=DIRECTION ( 'NONE',  ( 1.000000000000000000, 0.000000000000000000, 0.000000000000000000 ) ) ;
#22381=CARTESIAN_POINT ( 'NONE',  ( 0.6389947482386004740, -7.663676466994388647, -1.499999999999999556 ) ) ;
#22388=ORIENTED_EDGE ( 'NONE', *, *, #4583, .T. ) ;
#22397=CARTESIAN_POINT ( 'NONE',  ( 7.581061048149257964, -18.74603139903822324, -1.749278969417850549 ) ) ;
#22411=DIRECTION ( 'NONE',  ( 0.9816271834476637537, 0.000000000000000000, 0.1908089953765453872 ) ) ;
#22413=ORIENTED_EDGE ( 'NONE', *, *, #18173, .F. ) ;
#22423=CARTESIAN_POINT ( 'NONE',  ( -28.35000000000000497, -10.96966150227469505, 4.000000000000000000 ) ) ;
#22429=CARTESIAN_POINT ( 'NONE',  ( 107.9813876837010156, -17.80134939207562184, -4.369343856298157469 ) ) ;
#22437=EDGE_CURVE ( 'NONE', #6440, #29313, #6473, .T. ) ;
#22439=CARTESIAN_POINT ( 'NONE',  ( 24.44878497425310826, -17.43662272166809046, -1.459033525497872796 ) ) ;
#22440=CARTESIAN_POINT ( 'NONE',  ( -17.04380309137718541, -27.93932300454937590, 11.50000000000000000 ) ) ;
#22441=AXIS2_PLACEMENT_3D ( 'NONE', #30741, #20347, #7645 ) ;
#22444=ADVANCED_FACE ( 'NONE', ( #24248 ), #19840, .F. ) ;
#22445=DIRECTION ( 'NONE',  ( 1.000000000000000000, 0.000000000000000000, 0.000000000000000000 ) ) ;
#22460=CARTESIAN_POINT ( 'NONE',  ( -3.135269660805080516, -0.5000000000000000000, 1.500000000000000000 ) ) ;
#22483=DIRECTION ( 'NONE',  ( -1.000000000000000000, -0.000000000000000000, 0.000000000000000000 ) ) ;
#22487=CONICAL_SURFACE ( 'NONE', #30494, 2.099999999999997868, 1.029744258676653867 ) ;
#22500=CARTESIAN_POINT ( 'NONE',  ( 15.94400161454247389, -16.27119544232739656, 1.500000000000836664 ) ) ;
#22505=CARTESIAN_POINT ( 'NONE',  ( -3.686605011514858088, -10.77444884474583908, 1.500000000000001110 ) ) ;
#22510=AXIS2_PLACEMENT_3D ( 'NONE', #18378, #28574, #16338 ) ;
#22513=DIRECTION ( 'NONE',  ( -1.000000000000000000, 2.473959037481237219E-13, 0.000000000000000000 ) ) ;
#22515=CARTESIAN_POINT ( 'NONE',  ( 21.37037762942230046, -21.76140461385139702, -1.424884447122514164 ) ) ;
#22523=FACE_BOUND ( 'NONE', #27254, .T. ) ;
#22539=LINE ( 'NONE', #19381, #7675 ) ;
#22543=CARTESIAN_POINT ( 'NONE',  ( 5.133822020161873390, -13.02681593462403242, 1.756567112590995183 ) ) ;
#22549=VERTEX_POINT ( 'NONE', #1798 ) ;
#22564=AXIS2_PLACEMENT_3D ( 'NONE', #25840, #15626, #28163 ) ;
#22565=CARTESIAN_POINT ( 'NONE',  ( 5.414747269551301478, -13.03415141497022489, -1.499999999999435785 ) ) ;
#22575=CARTESIAN_POINT ( 'NONE',  ( 23.03407491561165443, -17.39674082715752945, 1.686926596850292670 ) ) ;
#22585=CARTESIAN_POINT ( 'NONE',  ( -2.351824853402081583, -12.55082504084320227, -1.499999999999879430 ) ) ;
#22586=AXIS2_PLACEMENT_3D ( 'NONE', #10799, #28689, #2802 ) ;
#22591=CARTESIAN_POINT ( 'NONE',  ( 107.4168514414663491, -16.88233545631764798, 3.542414872601526543 ) ) ;
#22612=CARTESIAN_POINT ( 'NONE',  ( 0.1610798642962855409, -10.72944008624798506, 4.522129901861156931 ) ) ;
#22616=CARTESIAN_POINT ( 'NONE',  ( 8.706508905304815471, -1.271749511658105902, -1.000000000000000000 ) ) ;
#22617=CARTESIAN_POINT ( 'NONE',  ( 107.5625329803365702, -18.99455126352175682, -4.492206011592212889 ) ) ;
#22635=AXIS2_PLACEMENT_3D ( 'NONE', #24509, #32256, #13989 ) ;
#22636=AXIS2_PLACEMENT_3D ( 'NONE', #477, #10659, #21054 ) ;
#22639=EDGE_CURVE ( 'NONE', #23130, #12973, #5939, .T. ) ;
#22645=AXIS2_PLACEMENT_3D ( 'NONE', #13603, #11440, #31841 ) ;
#22648=CARTESIAN_POINT ( 'NONE',  ( -3.135269660805080516, -0.4999999999999993339, 1.500000000000000000 ) ) ;
#22650=ORIENTED_EDGE ( 'NONE', *, *, #24287, .F. ) ;
#22652=VERTEX_POINT ( 'NONE', #10171 ) ;
#22655=ORIENTED_EDGE ( 'NONE', *, *, #29337, .F. ) ;
#22657=CARTESIAN_POINT ( 'NONE',  ( 0.2678094507063553675, -7.640026513854723866, 1.500000000000000000 ) ) ;
#22662=DIRECTION ( 'NONE',  ( -0.000000000000000000, -0.000000000000000000, 1.000000000000000000 ) ) ;
#22666=CARTESIAN_POINT ( 'NONE',  ( 24.57728726453536439, -17.46986644505820152, 1.411007141444847512 ) ) ;
#22667=EDGE_CURVE ( 'NONE', #24091, #8502, #18206, .T. ) ;
#22681=DIRECTION ( 'NONE',  ( 0.000000000000000000, -0.000000000000000000, -1.000000000000000000 ) ) ;
#22683=CARTESIAN_POINT ( 'NONE',  ( 107.9829200570041507, -17.82341518643319489, 4.417814765846281411 ) ) ;
#22686=CARTESIAN_POINT ( 'NONE',  ( 21.08401840680260264, -16.78474387324011374, 1.500000000000000666 ) ) ;
#22688=CARTESIAN_POINT ( 'NONE',  ( 17.97422212134408781, -19.86246923125032282, -4.522129901861166701 ) ) ;
#22690=CARTESIAN_POINT ( 'NONE',  ( -4.555596785357748146, -6.492743774806009505, 1.500000000000000000 ) ) ;
#22692=CARTESIAN_POINT ( 'NONE',  ( 108.0241601323609615, -18.41726201233227300, -4.475732320008884102 ) ) ;
#22698=CARTESIAN_POINT ( 'NONE',  ( 21.38916691622168997, -21.75742400528990927, -1.437540121018670902 ) ) ;
#22701=DIRECTION ( 'NONE',  ( -0.8616149568369075862, 0.5075624751249188105, 0.000000000000000000 ) ) ;
#22706=EDGE_CURVE ( 'NONE', #25887, #31320, #2669, .T. ) ;
#22721=B_SPLINE_CURVE_WITH_KNOTS ( 'NONE', 3,
 ( #22460, #2580, #32677, #25125, #7581, #10424, #15101, #18101, #27643, #17954 ),
 .UNSPECIFIED., .F., .F.,
 ( 4, 2, 2, 2, 4 ),
 ( 0.000000000000000000, 0.0002246264387293540486, 0.0004492528774587080972, 0.0006738793161880621187, 0.0008985057549174161945 ),
 .UNSPECIFIED. ) ;
#22731=DIRECTION ( 'NONE',  ( -0.000000000000000000, -0.000000000000000000, -1.000000000000000000 ) ) ;
#22732=EDGE_CURVE ( 'NONE', #29863, #26510, #30609, .T. ) ;
#22735=CARTESIAN_POINT ( 'NONE',  ( 0.9306419922191575544, -8.901511148765193226, 0.9788672205888330202 ) ) ;
#22742=CARTESIAN_POINT ( 'NONE',  ( 23.88966202700896702, -17.43474874481661985, 1.573876621502935613 ) ) ;
#22743=ORIENTED_EDGE ( 'NONE', *, *, #20292, .F. ) ;
#22748=CARTESIAN_POINT ( 'NONE',  ( 0.4357215767673975892, -15.33303754249009287, -1.500000000000119238 ) ) ;
#22764=CARTESIAN_POINT ( 'NONE',  ( -2.600000000000000089, 0.000000000000000000, 1.500000000000000000 ) ) ;
#22766=EDGE_CURVE ( 'NONE', #12596, #25887, #31264, .T. ) ;
#22768=CARTESIAN_POINT ( 'NONE',  ( 107.5617944031221640, -18.98359742639815551, -4.522129901861166701 ) ) ;
#22772=CARTESIAN_POINT ( 'NONE',  ( -1.047937531484013585, -4.989690239015236450, 4.522129901861156931 ) ) ;
#22774=CARTESIAN_POINT ( 'NONE',  ( -3.000233502159942667, -11.27265617876589054, 1.743644579621235202 ) ) ;
#22775=CARTESIAN_POINT ( 'NONE',  ( 8.706508904963998319, -1.271749511501821583, -1.500000000000000000 ) ) ;
#22783=CARTESIAN_POINT ( 'NONE',  ( -2.767073886773233848, -0.6621507858625382825, -1.748408842879326075 ) ) ;
#22795=EDGE_CURVE ( 'NONE', #32499, #593, #14460, .T. ) ;
#22798=CARTESIAN_POINT ( 'NONE',  ( -2.962625823238651979, -0.001292792641227542925, 0.8472062597617511237 ) ) ;
#22805=CARTESIAN_POINT ( 'NONE',  ( 2.600000000000000089, 0.000000000000000000, -1.500000000000000000 ) ) ;
#22806=ORIENTED_EDGE ( 'NONE', *, *, #2575, .T. ) ;
#22807=CARTESIAN_POINT ( 'NONE',  ( 1.630591573041451303, -1.447622518949628123, -1.758800530465949752 ) ) ;
#22812=CARTESIAN_POINT ( 'NONE',  ( -23.35000000000000142, -10.96966150227469505, -11.50000000000000000 ) ) ;
#22813=CARTESIAN_POINT ( 'NONE',  ( 24.40424503925473232, -17.45211869376779390, 1.605444122987317757 ) ) ;
#22814=CARTESIAN_POINT ( 'NONE',  ( 6.691656545360866737, -18.99987508458162111, 0.9788672205877712029 ) ) ;
#22815=CARTESIAN_POINT ( 'NONE',  ( 0.1610798642962855409, -10.72944008624798506, 4.522129901861156931 ) ) ;
#22829=DIRECTION ( 'NONE',  ( -1.000000000000000000, 0.000000000000000000, 0.000000000000000000 ) ) ;
#22836=ORIENTED_EDGE ( 'NONE', *, *, #5410, .T. ) ;
#22845=CARTESIAN_POINT ( 'NONE',  ( 21.36697425079191959, -21.76267261028177913, -1.421487723214910570 ) ) ;
#22847=FACE_OUTER_BOUND ( 'NONE', #1907, .T. ) ;
#22848=B_SPLINE_CURVE_WITH_KNOTS ( 'NONE', 3,
 ( #18715, #6024, #3049, #29099, #10882, #13694, #21090, #6333, #21395, #13203, #23896, #13841, #5701, #15881, #3194, #1005 ),
 .UNSPECIFIED., .F., .F.,
 ( 4, 2, 2, 2, 2, 2, 2, 4 ),
 ( 0.009305842773645304003, 0.5000000000000000000, 0.6250000000000000000, 0.7500000000000000000, 0.8125000000000000000, 0.8750000000000000000, 0.9375000000000000000, 1.000000000000000000 ),
 .UNSPECIFIED. ) ;
#22855=CARTESIAN_POINT ( 'NONE',  ( 23.17076627986326542, -21.93622647232682965, 1.056592207990660670 ) ) ;
#22875=FACE_OUTER_BOUND ( 'NONE', #9991, .T. ) ;
#22883=DIRECTION ( 'NONE',  ( 1.000000000000000000, 0.000000000000000000, 0.000000000000000000 ) ) ;
#22884=CARTESIAN_POINT ( 'NONE',  ( -1.033057378353320788, -8.048844657541357250, 4.522129901861157819 ) ) ;
#22890=EDGE_LOOP ( 'NONE', ( #14881, #31266, #23651, #7164 ) ) ;
#22898=CARTESIAN_POINT ( 'NONE',  ( 0.5107832276858312870, -15.23285467310830477, -1.745873400673900289 ) ) ;
#22920=CARTESIAN_POINT ( 'NONE',  ( 107.6641948605100083, -20.45809826282308208, 1.500000000000000000 ) ) ;
#22921=CARTESIAN_POINT ( 'NONE',  ( 71.38866214471497074, -19.82505015900708401, 4.522129901861156931 ) ) ;
#22922=CARTESIAN_POINT ( 'NONE',  ( -3.308639368481777421, -10.63993487576245656, 1.743554625370035582 ) ) ;
#22924=CARTESIAN_POINT ( 'NONE',  ( 108.0288149916133733, -18.48429082758350717, -4.339956994117294187 ) ) ;
#22931=DIRECTION ( 'NONE',  ( 0.000000000000000000, 0.000000000000000000, -1.000000000000000000 ) ) ;
#22942=PLANE ( 'NONE',  #23167 ) ;
#22943=CARTESIAN_POINT ( 'NONE',  ( 109.5084093630373729, -17.21855534384546971, -4.522129901861164925 ) ) ;
#22944=CARTESIAN_POINT ( 'NONE',  ( 17.08731201381446851, -15.08866305798481733, 1.000000000000000222 ) ) ;
#22945=ORIENTED_EDGE ( 'NONE', *, *, #4036, .T. ) ;
#22948=CARTESIAN_POINT ( 'NONE',  ( -3.162653373152863878, 0.0004983460144369277704, 1.055926639512883680 ) ) ;
#22949=DIRECTION ( 'NONE',  ( 1.000000000000000000, 0.000000000000000000, 0.000000000000000000 ) ) ;
#22955=CARTESIAN_POINT ( 'NONE',  ( 1.305960519821096844, -9.941484022874826465, -1.500000000000000000 ) ) ;
#22956=ORIENTED_EDGE ( 'NONE', *, *, #4512, .F. ) ;
#22958=CARTESIAN_POINT ( 'NONE',  ( 4.523414449530823944, -12.69491784415721725, -1.757045753096131424 ) ) ;
#22966=CARTESIAN_POINT ( 'NONE',  ( 74.30107678963170770, -22.79527490385382649, 1.500000000000000000 ) ) ;
#22978=CARTESIAN_POINT ( 'NONE',  ( -2.600000000000000089, 0.000000000000000000, 1.500000000000000000 ) ) ;
#22979=CARTESIAN_POINT ( 'NONE',  ( 20.58436699794885882, -21.58689779341630199, -1.578270943419022077 ) ) ;
#22980=ORIENTED_EDGE ( 'NONE', *, *, #26153, .T. ) ;
#22988=CARTESIAN_POINT ( 'NONE',  ( 73.45519860863089434, -21.36028973287599086, -4.522129901861166701 ) ) ;
#22991=CARTESIAN_POINT ( 'NONE',  ( 10.46133304479515758, -19.61932188654371600, 1.750340032278390412 ) ) ;
#23006=FACE_OUTER_BOUND ( 'NONE', #20727, .T. ) ;
#23014=DIRECTION ( 'NONE',  ( -1.000000000000000000, -6.938893903907222067E-15, 0.000000000000000000 ) ) ;
#23019=EDGE_CURVE ( 'NONE', #31320, #25210, #32111, .T. ) ;
#23024=CARTESIAN_POINT ( 'NONE',  ( 2.637177389002316463, 8.024708101613472686E-33, -1.518999257951627158 ) ) ;
#23025=CARTESIAN_POINT ( 'NONE',  ( 15.81086013943126822, -14.68957281887663413, 1.000000000000000000 ) ) ;
#23027=CARTESIAN_POINT ( 'NONE',  ( 21.78578353139858947, -21.77542465828167551, 1.497561405439323368 ) ) ;
#23036=AXIS2_PLACEMENT_3D ( 'NONE', #10081, #12442, #20295 ) ;
#23039=DIRECTION ( 'NONE',  ( -0.000000000000000000, 0.000000000000000000, 1.000000000000000000 ) ) ;
#23048=CARTESIAN_POINT ( 'NONE',  ( 1.305960519821096844, -9.941484022874826465, 1.500000000000000444 ) ) ;
#23053=CIRCLE ( 'NONE', #24634, 0.5000000000000004441 ) ;
#23055=DIRECTION ( 'NONE',  ( -1.000000000000000000, 0.000000000000000000, -0.000000000000000000 ) ) ;
#23057=ORIENTED_EDGE ( 'NONE', *, *, #6907, .T. ) ;
#23062=AXIS2_PLACEMENT_3D ( 'NONE', #14740, #9226, #7380 ) ;
#23065=CONICAL_SURFACE ( 'NONE', #6517, 2.524999999999999467, 0.7853981633974472798 ) ;
#23066=EDGE_CURVE ( 'NONE', #11856, #32242, #27865, .T. ) ;
#23092=TOROIDAL_SURFACE ( 'NONE', #27360, 10.46966150227468795, 0.5000000000000000000 ) ;
#23100=CARTESIAN_POINT ( 'NONE',  ( 2.281627749324421917, -0.2935656086769610207, 1.757435426329174044 ) ) ;
#23101=CARTESIAN_POINT ( 'NONE',  ( -0.5879824335954042525, -14.86230332063114545, 1.500000000000000444 ) ) ;
#23121=CARTESIAN_POINT ( 'NONE',  ( 22.00639167669143603, -21.80013755708273848, 1.500000000000000000 ) ) ;
#23127=DIRECTION ( 'NONE',  ( -1.000000000000000000, 0.000000000000000000, 0.000000000000000000 ) ) ;
#23130=VERTEX_POINT ( 'NONE', #30562 ) ;
#23136=CARTESIAN_POINT ( 'NONE',  ( 107.4543402635612637, -17.42228831489675400, 4.691818008238314519 ) ) ;
#23151=CARTESIAN_POINT ( 'NONE',  ( 14.51811802657236505, -16.11687040489192313, -1.753674770401980387 ) ) ;
#23154=CARTESIAN_POINT ( 'NONE',  ( -45.60000000000000142, -10.96966150227468972, 1.500000000000000000 ) ) ;
#23161=DIRECTION ( 'NONE',  ( 1.000000000000000000, -2.473959037481237219E-13, 0.000000000000000000 ) ) ;
#23162=CARTESIAN_POINT ( 'NONE',  ( 14.13431920379513862, -20.70626837987542856, 1.500000000000000000 ) ) ;
#23167=AXIS2_PLACEMENT_3D ( 'NONE', #17588, #30325, #32994 ) ;
#23176=ORIENTED_EDGE ( 'NONE', *, *, #4183, .T. ) ;
#23180=CYLINDRICAL_SURFACE ( 'NONE', #28416, 0.5000000000000004441 ) ;
#23182=CARTESIAN_POINT ( 'NONE',  ( 6.448894291894883501, -17.04229596238074151, -4.522129901861166701 ) ) ;
#23185=CARTESIAN_POINT ( 'NONE',  ( -4.155175066657748495, -6.548221803322783252, 1.745040299909109027 ) ) ;
#23192=CARTESIAN_POINT ( 'NONE',  ( 108.0795389336126107, -19.21470297384341919, 2.839262079369133662 ) ) ;
#23195=CARTESIAN_POINT ( 'NONE',  ( -16.85000000000000142, -10.96966150227469683, -11.50000000000000000 ) ) ;
#23196=EDGE_CURVE ( 'NONE', #2628, #8281, #7964, .T. ) ;
#23204=CARTESIAN_POINT ( 'NONE',  ( 24.39659513448239991, -17.41072360183627055, 1.416990234759656575 ) ) ;
#23213=AXIS2_PLACEMENT_3D ( 'NONE', #24980, #2091, #3432 ) ;
#23215=CARTESIAN_POINT ( 'NONE',  ( 1.879786566314391560, -10.72333674525774860, 1.762694233963469026 ) ) ;
#23216=CARTESIAN_POINT ( 'NONE',  ( 10.11068946041697991, -12.10067465432540956, 1.499999999999575451 ) ) ;
#23220=CARTESIAN_POINT ( 'NONE',  ( 1.743702975966804347, -1.493758447930603195, 1.500000000000000000 ) ) ;
#23224=CARTESIAN_POINT ( 'NONE',  ( 2.410813113178261968, -0.09135288943933156380, -1.740945950644691154 ) ) ;
#23238=ORIENTED_EDGE ( 'NONE', *, *, #20060, .F. ) ;
#23240=CARTESIAN_POINT ( 'NONE',  ( 24.22349034905675325, -17.32906192875313423, -1.351230503573957131 ) ) ;
#23259=ORIENTED_EDGE ( 'NONE', *, *, #26662, .F. ) ;
#23262=CARTESIAN_POINT ( 'NONE',  ( 18.53175858344379634, -21.44524224917989130, 1.500000000000000000 ) ) ;
#23264=CARTESIAN_POINT ( 'NONE',  ( 8.528645601772334217, -0.5000000000000011102, 1.500000000000000000 ) ) ;
#23270=CARTESIAN_POINT ( 'NONE',  ( 2.288113303901286422, -16.46502519983721413, 1.747280108055323522 ) ) ;
#23273=CARTESIAN_POINT ( 'NONE',  ( 107.5618984974341146, -18.98541497655834220, -4.517168112729012641 ) ) ;
#23285=CARTESIAN_POINT ( 'NONE',  ( 107.6641398346957033, -20.45810202417174750, 1.500000000000000000 ) ) ;
#23288=CARTESIAN_POINT ( 'NONE',  ( -15.51216819290874227, -21.43932300455805873, 1.500000000000000000 ) ) ;
#23290=CARTESIAN_POINT ( 'NONE',  ( -0.7739934281325309140, -8.972773999336983053, -4.522129901861164925 ) ) ;
#23291=CARTESIAN_POINT ( 'NONE',  ( 7.686969782318655575, -9.486238560348441595, 1.000000000000000222 ) ) ;
#23292=CARTESIAN_POINT ( 'NONE',  ( 107.9883904550100482, -17.90218755680270846, 5.108687026697555922 ) ) ;
#23304=CARTESIAN_POINT ( 'NONE',  ( 1.278428506419904798, -2.392608122357158251, 1.500000000000000000 ) ) ;
#23307=CARTESIAN_POINT ( 'NONE',  ( 21.03177542174473658, -17.18603084754145982, -1.753176640694677380 ) ) ;
#23310=DIRECTION ( 'NONE',  ( -0.4851627901281745370, -0.000000000000000000, -0.8744238486426618717 ) ) ;
#23311=CARTESIAN_POINT ( 'NONE',  ( 107.9171431298509987, -16.87624379866894841, 2.462434481765830796 ) ) ;
#23312=CARTESIAN_POINT ( 'NONE',  ( 107.5617870618796701, -18.98359792747699970, -4.522129903277523510 ) ) ;
#23313=CARTESIAN_POINT ( 'NONE',  ( 0.5491634894704520153, -7.006993281499743098, 1.500000000000000222 ) ) ;
#23324=CARTESIAN_POINT ( 'NONE',  ( -31.18783180709124636, 0.000000000000000000, 1.000000000000000000 ) ) ;
#23331=CARTESIAN_POINT ( 'NONE',  ( 42.88108885380913193, -22.62752020922543750, -4.522129901861166701 ) ) ;
#23340=CARTESIAN_POINT ( 'NONE',  ( -31.59999999999999787, -25.43932300454937945, 11.00000000000000000 ) ) ;
#23341=CARTESIAN_POINT ( 'NONE',  ( -50.60000000000000142, -21.93932300454937945, 1.500000000000000000 ) ) ;
#23345=CARTESIAN_POINT ( 'NONE',  ( 13.13178786249840435, -17.31629153505178920, -4.522129901861164925 ) ) ;
#23351=DIRECTION ( 'NONE',  ( 0.000000000000000000, -1.000000000000000000, 0.000000000000000000 ) ) ;
#23358=CARTESIAN_POINT ( 'NONE',  ( 25.61042644977005622, -17.59778802277103082, 1.000000000000000000 ) ) ;
#23374=CARTESIAN_POINT ( 'NONE',  ( 21.08401840680261330, -16.78474387324011374, 1.949999999999999956 ) ) ;
#23375=CARTESIAN_POINT ( 'NONE',  ( 9.266707753004494563, -0.05004968855533439842, 1.221243012139963779 ) ) ;
#23383=CARTESIAN_POINT ( 'NONE',  ( 23.26681913457865392, -17.19558280316121568, -1.454198315410691000 ) ) ;
#23384=CARTESIAN_POINT ( 'NONE',  ( -32.07659242536668387, -21.93932300455396245, -1.000000000000000000 ) ) ;
#23391=VERTEX_POINT ( 'NONE', #9774 ) ;
#23395=ORIENTED_EDGE ( 'NONE', *, *, #18545, .T. ) ;
#23399=CARTESIAN_POINT ( 'NONE',  ( 16.02446143562542602, -14.75799222003427857, -0.9999999999999997780 ) ) ;
#23405=CARTESIAN_POINT ( 'NONE',  ( -15.51216819290874227, -21.43932300455805873, 1.500000000000000000 ) ) ;
#23410=ORIENTED_EDGE ( 'NONE', *, *, #20919, .F. ) ;
#23413=CARTESIAN_POINT ( 'NONE',  ( -3.910407125125240579, -9.341411376702357217, 1.499999999999999778 ) ) ;
#23424=CARTESIAN_POINT ( 'NONE',  ( -2.972652642344704166, -0.1886749676220912386, -1.397177942464456812 ) ) ;
#23428=LINE ( 'NONE', #5580, #9754 ) ;
#23436=CARTESIAN_POINT ( 'NONE',  ( 107.5356071280131118, -18.60369656572296293, 5.016949557071701093 ) ) ;
#23440=CARTESIAN_POINT ( 'NONE',  ( 107.5354615446400857, -18.60157483985592108, 5.015849210584171658 ) ) ;
#23443=ADVANCED_FACE ( 'NONE', ( #5105 ), #20305, .F. ) ;
#23450=CARTESIAN_POINT ( 'NONE',  ( 19.71936553561526395, -17.01520723777865740, -1.753252447592055896 ) ) ;
#23451=LINE ( 'NONE', #74, #15024 ) ;
#23454=CARTESIAN_POINT ( 'NONE',  ( 107.9076248307730594, -16.73918265980126918, 2.181394474119346505 ) ) ;
#23458=CARTESIAN_POINT ( 'NONE',  ( 18.52596969037426078, -16.42883989518809074, 1.500000000000000444 ) ) ;
#23461=CARTESIAN_POINT ( 'NONE',  ( 3.090086839179210454, 0.04810462266694562339, 0.6765469099963639099 ) ) ;
#23464=SPHERICAL_SURFACE ( 'NONE', #22036, 0.5000000000000000000 ) ;
#23468=ADVANCED_FACE ( 'NONE', ( #24825 ), #31194, .T. ) ;
#23473=CYLINDRICAL_SURFACE ( 'NONE', #24751, 0.5000000000000000000 ) ;
#23478=VECTOR ( 'NONE', #18760, 1000.000000000000000 ) ;
#23485=CARTESIAN_POINT ( 'NONE',  ( -29.85000000000000497, -10.96966150227469505, -11.50000000000000000 ) ) ;
#23493=CARTESIAN_POINT ( 'NONE',  ( 108.0518026804759018, -18.81530782858648720, 3.657879498689815545 ) ) ;
#23498=CARTESIAN_POINT ( 'NONE',  ( -2.715578036410642326, -0.5452877988936790654, -1.748464050203881737 ) ) ;
#23500=CARTESIAN_POINT ( 'NONE',  ( -0.9232102171129827894, 0.000000000000000000, -4.522129901861166701 ) ) ;
#23505=CARTESIAN_POINT ( 'NONE',  ( 21.70556107702209303, -21.76510136446067278, 1.556570398778031716 ) ) ;
#23507=EDGE_CURVE ( 'NONE', #7400, #140, #30007, .T. ) ;
#23509=ORIENTED_EDGE ( 'NONE', *, *, #20060, .T. ) ;
#23514=CARTESIAN_POINT ( 'NONE',  ( 10.90710808013595923, -12.60204455941995150, 1.000000000000000000 ) ) ;
#23546=CARTESIAN_POINT ( 'NONE',  ( 25.38252866315519896, -17.53427985683313040, 1.078182501543538230 ) ) ;
#23551=CARTESIAN_POINT ( 'NONE',  ( 3.744708216408842549, 0.000000000000000000, -1.000000000000000000 ) ) ;
#23555=CIRCLE ( 'NONE', #4364, 0.5000000000000004441 ) ;
#23569=CARTESIAN_POINT ( 'NONE',  ( 8.045354371110260416, -1.465502149859543524, 1.500000000000000000 ) ) ;
#23574=CARTESIAN_POINT ( 'NONE',  ( 107.5894750467910228, -19.38218566293085843, 3.705121501346941404 ) ) ;
#23577=CARTESIAN_POINT ( 'NONE',  ( 6.168724859680794204, -18.37409005221297775, 1.500000000000238032 ) ) ;
#23592=CARTESIAN_POINT ( 'NONE',  ( -3.038890739117042994, -0.3712649131886756049, -1.487764840819184142 ) ) ;
#23596=AXIS2_PLACEMENT_3D ( 'NONE', #8496, #21861, #18544 ) ;
#23601=CARTESIAN_POINT ( 'NONE',  ( 18.06874303396712023, -21.14907373873896645, 1.751201621425063193 ) ) ;
#23604=CONICAL_SURFACE ( 'NONE', #19877, 2.524999999999999467, 0.7853981633974472798 ) ;
#23606=CARTESIAN_POINT ( 'NONE',  ( 107.9965106981324681, -18.01911703775898488, 5.137942289311619781 ) ) ;
#23611=CYLINDRICAL_SURFACE ( 'NONE', #11875, 0.5000000000000008882 ) ;
#23621=ORIENTED_EDGE ( 'NONE', *, *, #7007, .T. ) ;
#23626=CARTESIAN_POINT ( 'NONE',  ( 24.38441422956697124, -17.22282062799600766, -1.000000000000000000 ) ) ;
#23627=CARTESIAN_POINT ( 'NONE',  ( 107.9481247343239687, -17.32237119582743290, -4.511855742419091264 ) ) ;
#23632=CARTESIAN_POINT ( 'NONE',  ( 0.5291895307230495282, -6.519846571640815824, 1.500000000000000444 ) ) ;
#23633=CARTESIAN_POINT ( 'NONE',  ( 8.528645601772334217, -0.5000000000000011102, 1.500000000000000000 ) ) ;
#23635=AXIS2_PLACEMENT_3D ( 'NONE', #17411, #30144, #21918 ) ;
#23637=CARTESIAN_POINT ( 'NONE',  ( 2.802272078496832464, -0.3634031030573117715, 1.485394228827260577 ) ) ;
#23650=AXIS2_PLACEMENT_3D ( 'NONE', #15443, #25653, #2773 ) ;
#23651=ORIENTED_EDGE ( 'NONE', *, *, #27552, .T. ) ;
#23652=CARTESIAN_POINT ( 'NONE',  ( 0.8612084954131845604, -8.440632053510048749, -1.499999999999999556 ) ) ;
#23661=EDGE_LOOP ( 'NONE', ( #22251, #11564, #25045 ) ) ;
#23681=VECTOR ( 'NONE', #27016, 1000.000000000000000 ) ;
#23683=CIRCLE ( 'NONE', #3933, 0.4499999999999992339 ) ;
#23694=CARTESIAN_POINT ( 'NONE',  ( 107.9802527803230419, -17.78500706576073753, 4.325704939602341703 ) ) ;
#23696=CARTESIAN_POINT ( 'NONE',  ( 10.90710808056855363, -12.60204455863645201, 1.499999999999860112 ) ) ;
#23702=CARTESIAN_POINT ( 'NONE',  ( -3.222375984151267581, 0.000000000000000000, -1.000000000000000000 ) ) ;
#23709=ORIENTED_EDGE ( 'NONE', *, *, #3223, .T. ) ;
#23712=DIRECTION ( 'NONE',  ( 0.000000000000000000, -0.000000000000000000, -1.000000000000000000 ) ) ;
#23722=VERTEX_POINT ( 'NONE', #17425 ) ;
#23726=CARTESIAN_POINT ( 'NONE',  ( -2.408800074497548849, -5.498703686517900202, 5.485967528433935314 ) ) ;
#23742=VECTOR ( 'NONE', #4687, 1000.000000000000000 ) ;
#23743=CARTESIAN_POINT ( 'NONE',  ( 8.896977825536888318, -11.14034974407042711, -0.9999999999999997780 ) ) ;
#23748=CARTESIAN_POINT ( 'NONE',  ( -15.06907680150157702, -21.88241439596534121, 1.340913934978399613 ) ) ;
#23751=CARTESIAN_POINT ( 'NONE',  ( 1.073830709372254999, -2.621082672957672166, -1.760914646145874674 ) ) ;
#23768=CARTESIAN_POINT ( 'NONE',  ( -18.35000000000000142, -10.96966150227469505, -1.500000000000000000 ) ) ;
#23771=CARTESIAN_POINT ( 'NONE',  ( 19.72213158284570156, -21.49998897973738821, 1.523512165873458279 ) ) ;
#23775=CARTESIAN_POINT ( 'NONE',  ( 107.4499334670178143, -17.35837986862966176, 4.517176980674937781 ) ) ;
#23781=DIRECTION ( 'NONE',  ( 1.000000000000000000, 0.000000000000000000, 0.000000000000000000 ) ) ;
#23787=DIRECTION ( 'NONE',  ( -0.000000000000000000, -0.000000000000000000, -1.000000000000000000 ) ) ;
#23788=DIRECTION ( 'NONE',  ( -1.000000000000000000, 0.000000000000000000, 0.000000000000000000 ) ) ;
#23791=CARTESIAN_POINT ( 'NONE',  ( 6.353342831038617078, -18.33846711552379816, -1.748782834083794313 ) ) ;
#23793=CARTESIAN_POINT ( 'NONE',  ( 19.46384663048900876, -15.80031286559519010, -1.499999999999722444 ) ) ;
#23794=CARTESIAN_POINT ( 'NONE',  ( 107.9809260575503629, -17.79470209034395012, -4.352197235538400655 ) ) ;
#23799=CARTESIAN_POINT ( 'NONE',  ( -3.889464452585704723, -3.181828567483031112, 1.500000000000000000 ) ) ;
#23803=CARTESIAN_POINT ( 'NONE',  ( 107.3882468701019661, -16.47045351801639512, -2.697862662383026855 ) ) ;
#23809=CARTESIAN_POINT ( 'NONE',  ( 21.04494988260847776, -21.68420912488515739, 1.499840339240483766 ) ) ;
#23811=CARTESIAN_POINT ( 'NONE',  ( 0.6737277144758835323, -5.221526237309871199, -1.499999999999999556 ) ) ;
#23818=CARTESIAN_POINT ( 'NONE',  ( -4.575445569750785424, -7.851872718547149965, -0.9788672205760856615 ) ) ;
#23821=CARTESIAN_POINT ( 'NONE',  ( -23.35000000000000142, -10.96966150227469505, 4.500000000000000888 ) ) ;
#23828=CARTESIAN_POINT ( 'NONE',  ( -50.60000000000000142, -10.96966150227468972, 7.500000000000000000 ) ) ;
#23830=CARTESIAN_POINT ( 'NONE',  ( 107.5615483389071301, -18.98034905113282278, 4.530923109470624155 ) ) ;
#23832=CARTESIAN_POINT ( 'NONE',  ( -23.35000000000000142, -10.96966150227469505, 4.500000000000000888 ) ) ;
#23835=CARTESIAN_POINT ( 'NONE',  ( -23.35000000000000142, -10.96966150227469505, -1.500000000000000000 ) ) ;
#23849=CARTESIAN_POINT ( 'NONE',  ( 9.437548970008970528, 0.1642588933130853801, 1.000000000000000000 ) ) ;
#23853=CARTESIAN_POINT ( 'NONE',  ( 1.138639876302608878, -9.033957850008556889, 1.500000000000000000 ) ) ;
#23859=CARTESIAN_POINT ( 'NONE',  ( 22.16261821944717170, -17.22505787983993741, -1.541391846742717231 ) ) ;
#23865=EDGE_CURVE ( 'NONE', #3159, #22549, #19211, .T. ) ;
#23866=DIRECTION ( 'NONE',  ( 0.000000000000000000, 0.000000000000000000, -1.000000000000000000 ) ) ;
#23875=CARTESIAN_POINT ( 'NONE',  ( 108.1641292914955130, -20.43278308392451947, -1.481931422884068761 ) ) ;
#23877=CARTESIAN_POINT ( 'NONE',  ( 25.25168948427242199, -17.50930648703901582, 1.141351624973356849 ) ) ;
#23882=CARTESIAN_POINT ( 'NONE',  ( 107.4500593345376558, -17.36019228850485163, -4.522129901861164925 ) ) ;
#23895=VERTEX_POINT ( 'NONE', #31148 ) ;
#23896=CARTESIAN_POINT ( 'NONE',  ( -1.033057378353439804, -8.048844657541355474, -4.522129901861164925 ) ) ;
#23921=CARTESIAN_POINT ( 'NONE',  ( 18.74274612900821779, -21.25842652921702935, 1.734019191250946168 ) ) ;
#23940=CARTESIAN_POINT ( 'NONE',  ( 108.0410785058465279, -18.66088238176251224, -3.974415582670320912 ) ) ;
#23941=CARTESIAN_POINT ( 'NONE',  ( 8.486535498532354893, -10.66169397763258253, -1.499999999999820366 ) ) ;
#23942=CARTESIAN_POINT ( 'NONE',  ( 107.9486069274682336, -17.32931465714983688, -4.530749433310830909 ) ) ;
#23946=EDGE_CURVE ( 'NONE', #24299, #2424, #2568, .T. ) ;
#23947=CARTESIAN_POINT ( 'NONE',  ( 3.554613218822866294, -15.76807188677689631, 4.522129901861158707 ) ) ;
#23948=CARTESIAN_POINT ( 'NONE',  ( 3.086618293031886395, -0.003885106576433895991, 0.6225218429476599979 ) ) ;
#23956=CARTESIAN_POINT ( 'NONE',  ( 20.71913853892345614, -21.61372392228095407, 1.559032431776717020 ) ) ;
#23969=CARTESIAN_POINT ( 'NONE',  ( 23.22564588060107482, -21.93932300456764040, 1.000000000000000000 ) ) ;
#23977=CARTESIAN_POINT ( 'NONE',  ( 108.0608891800116709, -18.94615116146357536, 4.531103216122085442 ) ) ;
#23979=CARTESIAN_POINT ( 'NONE',  ( 72.52374898135332160, -19.78015497550546442, -4.522129901861164925 ) ) ;
#23981=EDGE_CURVE ( 'NONE', #17584, #27584, #11313, .T. ) ;
#23990=CIRCLE ( 'NONE', #28275, 0.4500000000000001776 ) ;
#23994=CARTESIAN_POINT ( 'NONE',  ( 7.158832484464911161, -3.801775501249473610, 1.500000000000000000 ) ) ;
#23996=CARTESIAN_POINT ( 'NONE',  ( 7.429379966294620274, -10.00822258298124190, -1.499999999999999778 ) ) ;
#23999=CARTESIAN_POINT ( 'NONE',  ( 0.4715469964658544066, -8.230657990693778459, 1.499999999999999556 ) ) ;
#24018=VECTOR ( 'NONE', #27799, 1000.000000000000000 ) ;
#24022=FACE_OUTER_BOUND ( 'NONE', #27213, .T. ) ;
#24024=CARTESIAN_POINT ( 'NONE',  ( -50.60000000000000142, -10.96966150227468972, 6.999999999999999112 ) ) ;
#24041=VECTOR ( 'NONE', #20339, 1000.000000000000000 ) ;
#24052=CARTESIAN_POINT ( 'NONE',  ( 0.1142986632944693048, -6.518936808292961516, -1.773886185393975135 ) ) ;
#24054=EDGE_LOOP ( 'NONE', ( #1393, #21563, #15857, #26165 ) ) ;
#24057=AXIS2_PLACEMENT_3D ( 'NONE', #2165, #12836, #30607 ) ;
#24070=CARTESIAN_POINT ( 'NONE',  ( -4.499068592350032425, -5.402544097203555218, -1.500000000000000444 ) ) ;
#24077=CARTESIAN_POINT ( 'NONE',  ( 20.55936702064834165, -21.63501724500275714, 1.474765012620294025 ) ) ;
#24078=VECTOR ( 'NONE', #21503, 1000.000000000000000 ) ;
#24080=CARTESIAN_POINT ( 'NONE',  ( -15.02135460118491217, 0.000000000000000000, 1.095404497688272638 ) ) ;
#24082=EDGE_LOOP ( 'NONE', ( #2237, #19853, #1652, #16436 ) ) ;
#24087=AXIS2_PLACEMENT_3D ( 'NONE', #24430, #28795, #31822 ) ;
#24089=CARTESIAN_POINT ( 'NONE',  ( 107.5617723795404999, -18.98359893170737323, 4.522129901861158707 ) ) ;
#24091=VERTEX_POINT ( 'NONE', #12800 ) ;
#24105=CARTESIAN_POINT ( 'NONE',  ( 6.666829201526672577, -7.372062170296981520, -1.500000000000000000 ) ) ;
#24106=CARTESIAN_POINT ( 'NONE',  ( 107.9587511384790872, -17.47538877214310915, -3.690911647522888916 ) ) ;
#24107=EDGE_CURVE ( 'NONE', #2628, #7539, #21487, .T. ) ;
#24109=AXIS2_PLACEMENT_3D ( 'NONE', #6202, #1024, #31623 ) ;
#24114=CARTESIAN_POINT ( 'NONE',  ( -0.5616989984783457013, -12.44624546261724163, 4.522129901861158707 ) ) ;
#24118=LINE ( 'NONE', #16587, #20971 ) ;
#24129=CARTESIAN_POINT ( 'NONE',  ( 21.02910828058320902, -21.78322936331055359, -1.363801422436344613 ) ) ;
#24131=CARTESIAN_POINT ( 'NONE',  ( 8.520101525921534247, -14.04815114857715841, -1.500000000000000222 ) ) ;
#24135=CARTESIAN_POINT ( 'NONE',  ( 25.20116447083585953, -17.53130488828775313, -1.247823832777839703 ) ) ;
#24139=EDGE_LOOP ( 'NONE', ( #28641, #21102, #31545, #17911, #17680, #3585, #1700, #16714, #20762, #27751, #6365, #11437, #31326, #15418, #5092, #26503 ) ) ;
#24140=EDGE_LOOP ( 'NONE', ( #26428, #31246, #14442, #28270, #6909 ) ) ;
#24146=CARTESIAN_POINT ( 'NONE',  ( 13.65718777918027271, -19.09288791508984673, 4.522129901861158707 ) ) ;
#24150=VECTOR ( 'NONE', #9820, 999.9999999999998863 ) ;
#24158=CARTESIAN_POINT ( 'NONE',  ( 108.0286932287532409, -18.48253747268860536, 4.344751374527882959 ) ) ;
#24159=CARTESIAN_POINT ( 'NONE',  ( 6.399351475474185591, -16.64279405588517946, -5.485967528433938867 ) ) ;
#24163=CARTESIAN_POINT ( 'NONE',  ( -31.57659242536668032, -27.93932300454937590, -1.000000000000000000 ) ) ;
#24168=CIRCLE ( 'NONE', #28460, 8.000000000000000000 ) ;
#24176=CARTESIAN_POINT ( 'NONE',  ( 8.706508905304414014, -1.271749511658974319, 1.000000000000000000 ) ) ;
#24181=CARTESIAN_POINT ( 'NONE',  ( 0.8806224662995314478, -9.175208741423659831, 1.499999999999824363 ) ) ;
#24190=CARTESIAN_POINT ( 'NONE',  ( 23.03249562537437711, -17.15537757201811786, -1.465178982930819052 ) ) ;
#24192=ADVANCED_FACE ( 'NONE', ( #28202 ), #26486, .F. ) ;
#24203=DIRECTION ( 'NONE',  ( -0.000000000000000000, -0.000000000000000000, -1.000000000000000000 ) ) ;
#24211=CARTESIAN_POINT ( 'NONE',  ( -1.694237876703142742, -1.500727999663424184, 4.522129901861159595 ) ) ;
#24218=VECTOR ( 'NONE', #303, 1000.000000000000000 ) ;
#24231=CARTESIAN_POINT ( 'NONE',  ( 7.603296595623502796, -4.061113686736324446, -1.000000000000000222 ) ) ;
#24239=CARTESIAN_POINT ( 'NONE',  ( 0.8184811075176973150, -4.596091560410645371, -1.500000000000000000 ) ) ;
#24248=FACE_OUTER_BOUND ( 'NONE', #1596, .T. ) ;
#24272=DIRECTION ( 'NONE',  ( -0.1908089953765452484, 0.000000000000000000, 0.9816271834476638647 ) ) ;
#24277=FACE_OUTER_BOUND ( 'NONE', #13238, .T. ) ;
#24278=CARTESIAN_POINT ( 'NONE',  ( 107.3891785634640570, -16.48386933944874855, 2.725368464337420527 ) ) ;
#24281=CARTESIAN_POINT ( 'NONE',  ( 2.655375060943963472, -12.56041828387959747, 1.000000000000000000 ) ) ;
#24283=CARTESIAN_POINT ( 'NONE',  ( 8.690654616497502261, -10.89241706857619540, -1.500000000000000000 ) ) ;
#24284=CARTESIAN_POINT ( 'NONE',  ( 107.9691564671736188, -17.62522291648321371, -4.956268131904038476 ) ) ;
#24287=EDGE_CURVE ( 'NONE', #1302, #11856, #24665, .T. ) ;
#24291=CARTESIAN_POINT ( 'NONE',  ( 0.3285611067768013926, -13.34342412962908497, 4.522129901861158707 ) ) ;
#24299=VERTEX_POINT ( 'NONE', #458 ) ;
#24304=CARTESIAN_POINT ( 'NONE',  ( 7.308590057547465157, -13.58425266979916124, -1.500000000000000444 ) ) ;
#24308=CARTESIAN_POINT ( 'NONE',  ( 24.83519197235521148, -17.49564329958954545, -1.498842795365640690 ) ) ;
#24312=VERTEX_POINT ( 'NONE', #8459 ) ;
#24338=CARTESIAN_POINT ( 'NONE',  ( 22.93781385240136572, -21.92295985586710572, -1.128554941024477953 ) ) ;
#24339=CYLINDRICAL_SURFACE ( 'NONE', #8195, 10.96966150227469328 ) ;
#24340=CARTESIAN_POINT ( 'NONE',  ( 6.653983693896913465, -6.711078333449102651, 1.500000000000000000 ) ) ;
#24344=CARTESIAN_POINT ( 'NONE',  ( 0.3598463914740824832, -8.266277061147796701, 1.772553072661675166 ) ) ;
#24351=CARTESIAN_POINT ( 'NONE',  ( 24.14342515507837561, -17.38895391569489135, -1.425886477553355736 ) ) ;
#24354=CYLINDRICAL_SURFACE ( 'NONE', #4506, 0.5000000000000000000 ) ;
#24360=CARTESIAN_POINT ( 'NONE',  ( 42.35322304602171783, -22.56891886512033096, -4.522129901861166701 ) ) ;
#24381=CARTESIAN_POINT ( 'NONE',  ( 7.215348531073052740, -5.907639145588611029, -0.9999999999999997780 ) ) ;
#24385=EDGE_LOOP ( 'NONE', ( #13033, #20916, #13571, #19547, #13066 ) ) ;
#24389=CARTESIAN_POINT ( 'NONE',  ( 1.058453267035363021, -9.473955959261930460, -1.500000000000000222 ) ) ;
#24401=EDGE_CURVE ( 'NONE', #14502, #24299, #11971, .T. ) ;
#24405=CARTESIAN_POINT ( 'NONE',  ( -4.458024584373125876, -5.037940649430906248, -1.499999999999999112 ) ) ;
#24426=CARTESIAN_POINT ( 'NONE',  ( -1.924618011135691642, -13.55759823803114550, -1.499999999999999556 ) ) ;
#24430=CARTESIAN_POINT ( 'NONE',  ( -31.10918640827616244, -27.93932300454937590, 1.404595502311727362 ) ) ;
#24431=CARTESIAN_POINT ( 'NONE',  ( 7.193574579131897906, -9.614801642833084472, -1.500000000000000000 ) ) ;
#24432=CARTESIAN_POINT ( 'NONE',  ( 107.9509692546103139, -17.36333158048723035, -4.612881207896696090 ) ) ;
#24451=ORIENTED_EDGE ( 'NONE', *, *, #17083, .F. ) ;
#24453=CARTESIAN_POINT ( 'NONE',  ( 25.29940076078040434, -17.51841556854384052, -1.122629911123405488 ) ) ;
#24468=CARTESIAN_POINT ( 'NONE',  ( 3.544356706773102328, -14.29624599654279393, -5.485967528433937979 ) ) ;
#24483=CARTESIAN_POINT ( 'NONE',  ( 7.230698036208883295, -5.790874022015763067, 1.000000000000000000 ) ) ;
#24489=CARTESIAN_POINT ( 'NONE',  ( 5.359215096090147235, -13.14304817624114285, 1.756412860341782789 ) ) ;
#24493=CARTESIAN_POINT ( 'NONE',  ( 8.694260012178464336, -0.3977034846782427358, -1.500000000000002442 ) ) ;
#24497=CARTESIAN_POINT ( 'NONE',  ( 23.74728587540558422, -17.43182369245569063, -1.598909884665929315 ) ) ;
#24502=CARTESIAN_POINT ( 'NONE',  ( 23.13226153066252522, -21.93404782914821993, -1.074068642721640376 ) ) ;
#24509=CARTESIAN_POINT ( 'NONE',  ( -23.35000000000000142, -10.96966150227469505, 4.000000000000000000 ) ) ;
#24512=CARTESIAN_POINT ( 'NONE',  ( 24.35832023931450507, -17.33818253687174860, -1.317734466820339900 ) ) ;
#24531=ORIENTED_EDGE ( 'NONE', *, *, #18433, .F. ) ;
#24539=ORIENTED_EDGE ( 'NONE', *, *, #6392, .F. ) ;
#24544=CARTESIAN_POINT ( 'NONE',  ( 3.074330700587167620, -11.22349925427311312, -1.500000000000000000 ) ) ;
#24563=CARTESIAN_POINT ( 'NONE',  ( -4.548089889563796007, -6.140210766943967613, -1.500000000000000444 ) ) ;
#24574=CARTESIAN_POINT ( 'NONE',  ( 24.29160796521804144, -17.33532173511319385, 1.337584091083817928 ) ) ;
#24576=CARTESIAN_POINT ( 'NONE',  ( 20.00016891673595154, -21.67414139014260144, 1.443203664631087069 ) ) ;
#24580=VERTEX_POINT ( 'NONE', #7422 ) ;
#24588=CARTESIAN_POINT ( 'NONE',  ( 14.44929100883576822, -20.94157545051515967, -1.499999999999999334 ) ) ;
#24592=CARTESIAN_POINT ( 'NONE',  ( -3.910108620251236289, -3.305117197436432619, 1.500000000000158096 ) ) ;
#24593=CARTESIAN_POINT ( 'NONE',  ( 7.230698036208976553, -5.790874022015092493, -1.000000000000000000 ) ) ;
#24594=CARTESIAN_POINT ( 'NONE',  ( 108.0271645861481602, -18.46052539945377902, -4.398898937011770371 ) ) ;
#24595=ORIENTED_EDGE ( 'NONE', *, *, #13334, .F. ) ;
#24606=CARTESIAN_POINT ( 'NONE',  ( 107.3477315916820913, -15.88627780335592732, -1.500000000000000000 ) ) ;
#24611=CARTESIAN_POINT ( 'NONE',  ( 2.281627749324421028, -0.2935656086769635187, -1.757435426329174710 ) ) ;
#24618=ADVANCED_FACE ( 'NONE', ( #18470 ), #23464, .T. ) ;
#24622=CARTESIAN_POINT ( 'NONE',  ( 20.55463713078643195, -21.58103817311708283, -1.582345582279491847 ) ) ;
#24630=DIRECTION ( 'NONE',  ( 0.000000000000000000, -0.000000000000000000, -1.000000000000000000 ) ) ;
#24631=ORIENTED_EDGE ( 'NONE', *, *, #30019, .F. ) ;
#24632=DIRECTION ( 'NONE',  ( -0.000000000000000000, 0.000000000000000000, 1.000000000000000000 ) ) ;
#24634=AXIS2_PLACEMENT_3D ( 'NONE', #25795, #12408, #7892 ) ;
#24641=CARTESIAN_POINT ( 'NONE',  ( -2.223027892448373510, -2.927336879246196677, -4.522129901861166701 ) ) ;
#24645=AXIS2_PLACEMENT_3D ( 'NONE', #26773, #13572, #3567 ) ;
#24647=CARTESIAN_POINT ( 'NONE',  ( -23.35000000000000142, -10.96966150227469505, 1.500000000000000000 ) ) ;
#24665=CIRCLE ( 'NONE', #30575, 0.5000000000000000000 ) ;
#24668=CARTESIAN_POINT ( 'NONE',  ( 14.73511782699088357, -15.74768507728505362, 1.499999999999998668 ) ) ;
#24675=ADVANCED_FACE ( 'NONE', ( #10763 ), #27382, .F. ) ;
#24681=ORIENTED_EDGE ( 'NONE', *, *, #14276, .T. ) ;
#24684=CARTESIAN_POINT ( 'NONE',  ( 23.22564502775743378, -21.93932300456764040, -1.023882905581262825 ) ) ;
#24687=ORIENTED_EDGE ( 'NONE', *, *, #3062, .T. ) ;
#24709=DIRECTION ( 'NONE',  ( -1.000000000000000000, 0.000000000000000000, -0.000000000000000000 ) ) ;
#24713=DIRECTION ( 'NONE',  ( -0.000000000000000000, -0.000000000000000000, 1.000000000000000000 ) ) ;
#24721=AXIS2_PLACEMENT_3D ( 'NONE', #1560, #1248, #11743 ) ;
#24727=ORIENTED_EDGE ( 'NONE', *, *, #20160, .T. ) ;
#24733=CARTESIAN_POINT ( 'NONE',  ( 10.91170924523349584, -15.11896097446722464, -1.500000000000279110 ) ) ;
#24734=CARTESIAN_POINT ( 'NONE',  ( -61.56966150227469114, -10.96966150227468972, -1.000000000000000000 ) ) ;
#24739=CARTESIAN_POINT ( 'NONE',  ( 108.0285590637735851, -18.48060553035694653, -4.343942861249384002 ) ) ;
#24751=AXIS2_PLACEMENT_3D ( 'NONE', #23324, #428, #5766 ) ;
#24755=CARTESIAN_POINT ( 'NONE',  ( -2.574540400785382044, -12.71128672357123968, -1.499999999999999556 ) ) ;
#24764=CARTESIAN_POINT ( 'NONE',  ( 21.21813830868136463, -21.75718202030616055, 1.395944860341482796 ) ) ;
#24767=CARTESIAN_POINT ( 'NONE',  ( -18.06457975862740284, -25.93932300454937945, 14.13101917082694392 ) ) ;
#24781=CARTESIAN_POINT ( 'NONE',  ( -15.60935834747760609, -25.43932300454937945, 1.500000000000000000 ) ) ;
#24785=CARTESIAN_POINT ( 'NONE',  ( 107.9564799961608941, -17.44268488772687675, -4.756047278368655817 ) ) ;
#24797=DIRECTION ( 'NONE',  ( 0.000000000000000000, 0.000000000000000000, -1.000000000000000000 ) ) ;
#24802=EDGE_CURVE ( 'NONE', #7955, #2302, #24118, .T. ) ;
#24804=CARTESIAN_POINT ( 'NONE',  ( 71.53201042710830393, -18.09776336787419382, -0.9788672205888330202 ) ) ;
#24806=CARTESIAN_POINT ( 'NONE',  ( 7.300970717157576395, -8.296229357995484222, 1.000000000000000000 ) ) ;
#24815=CARTESIAN_POINT ( 'NONE',  ( 108.1300413742128228, -19.95926608421481063, -1.392287898180229133 ) ) ;
#24824=CARTESIAN_POINT ( 'NONE',  ( -2.461002521556598488, -6.738986457086101112, -5.485967528433938867 ) ) ;
#24825=FACE_OUTER_BOUND ( 'NONE', #1212, .T. ) ;
#24829=CARTESIAN_POINT ( 'NONE',  ( 73.25280475360474952, -21.01694209586349515, 5.485967528433935314 ) ) ;
#24839=VERTEX_POINT ( 'NONE', #16276 ) ;
#24849=CARTESIAN_POINT ( 'NONE',  ( 108.0281772836523544, -18.47510799158657591, -4.365046262023239976 ) ) ;
#24854=CARTESIAN_POINT ( 'NONE',  ( 23.27353278736382691, -21.94187821002792660, -1.030224486531079453 ) ) ;
#24855=CARTESIAN_POINT ( 'NONE',  ( 22.95054569172171099, -21.90694603883951785, -1.257390168162247246 ) ) ;
#24861=FACE_OUTER_BOUND ( 'NONE', #13973, .T. ) ;
#24862=CARTESIAN_POINT ( 'NONE',  ( -1.694237876702965329, -1.500727999663087564, -4.522129901861166701 ) ) ;
#24869=CARTESIAN_POINT ( 'NONE',  ( -31.57659242536668742, -27.93932300454937590, -1.000000000000000000 ) ) ;
#24872=VERTEX_POINT ( 'NONE', #11583 ) ;
#24882=CARTESIAN_POINT ( 'NONE',  ( 2.482257818914018532, 0.000000000000000000, 1.712210361609934672 ) ) ;
#24892=ORIENTED_EDGE ( 'NONE', *, *, #31237, .F. ) ;
#24896=CARTESIAN_POINT ( 'NONE',  ( 0.3144672950280170687, -7.550758264647147833, -1.499999999999964251 ) ) ;
#24897=CARTESIAN_POINT ( 'NONE',  ( 3.529609406779910419, -12.17998485103522199, 1.500000000000000444 ) ) ;
#24898=ORIENTED_EDGE ( 'NONE', *, *, #21117, .T. ) ;
#24912=CARTESIAN_POINT ( 'NONE',  ( -2.829285547032501125, -11.58124708880041176, -1.743702903532054371 ) ) ;
#24918=CARTESIAN_POINT ( 'NONE',  ( -14.63259398290947289, -21.93932300455827544, -0.9045955023117271399 ) ) ;
#24931=B_SPLINE_CURVE_WITH_KNOTS ( 'NONE', 3,
 ( #13038, #28584, #23240, #10175, #10518, #25917, #20399, #23383, #5677, #15858, #30615, #7698 ),
 .UNSPECIFIED., .F., .F.,
 ( 4, 2, 2, 2, 2, 4 ),
 ( 3.529906531158615134E-18, 0.0002088350746644245339, 0.0004176701493288455442, 0.0008353402986576876190, 0.001670680597315359192, 0.003341361194630703205 ),
 .UNSPECIFIED. ) ;
#24933=CARTESIAN_POINT ( 'NONE',  ( -4.181737789223789470, -9.389646197556098528, -1.500000000000000888 ) ) ;
#24936=CARTESIAN_POINT ( 'NONE',  ( 9.350000000000028066, 5.584097191983464876E-14, 1.000000000000000000 ) ) ;
#24940=CARTESIAN_POINT ( 'NONE',  ( 107.9828938048920435, -17.82303716254959980, -4.417089530202084724 ) ) ;
#24945=EDGE_CURVE ( 'NONE', #28748, #12752, #12731, .T. ) ;
#24956=CARTESIAN_POINT ( 'NONE',  ( 2.770684449829447615, 0.02953710645924999961, -1.228046178477606443 ) ) ;
#24972=DIRECTION ( 'NONE',  ( -1.000000000000000000, 0.000000000000000000, 0.000000000000000000 ) ) ;
#24980=CARTESIAN_POINT ( 'NONE',  ( -23.35000000000000142, -10.96966150227469505, 1.500000000000000000 ) ) ;
#24989=CARTESIAN_POINT ( 'NONE',  ( -50.60000000000000142, -21.93932300454937945, 1.000000000000000000 ) ) ;
#25000=ORIENTED_EDGE ( 'NONE', *, *, #6609, .F. ) ;
#25005=ORIENTED_EDGE ( 'NONE', *, *, #21394, .F. ) ;
#25008=DIRECTION ( 'NONE',  ( 1.000000000000000000, 0.000000000000000000, 0.000000000000000000 ) ) ;
#25016=DIRECTION ( 'NONE',  ( 0.1908089953765452762, 0.000000000000000000, -0.9816271834476639757 ) ) ;
#25029=ORIENTED_EDGE ( 'NONE', *, *, #9536, .T. ) ;
#25043=CARTESIAN_POINT ( 'NONE',  ( 9.054745842343928430, -14.53181015844465129, -1.499999999999859668 ) ) ;
#25044=CARTESIAN_POINT ( 'NONE',  ( 108.4615897723380868, -15.55450498649102720, 0.9788672205888330202 ) ) ;
#25045=ORIENTED_EDGE ( 'NONE', *, *, #25772, .T. ) ;
#25053=ORIENTED_EDGE ( 'NONE', *, *, #23066, .F. ) ;
#25059=APPLICATION_CONTEXT ( 'configuration controlled 3d designs of mechanical parts and assemblies' ) ;
#25062=CARTESIAN_POINT ( 'NONE',  ( -1.691706751995829539, -13.40606180584711993, -1.500000000000239364 ) ) ;
#25064=EDGE_CURVE ( 'NONE', #23391, #2520, #18583, .T. ) ;
#25069=ORIENTED_EDGE ( 'NONE', *, *, #12328, .F. ) ;
#25075=DIRECTION ( 'NONE',  ( -0.000000000000000000, -0.000000000000000000, -1.000000000000000000 ) ) ;
#25083=ORIENTED_EDGE ( 'NONE', *, *, #22766, .F. ) ;
#25093=CARTESIAN_POINT ( 'NONE',  ( 7.845473912039718556, -1.949903631126105097, -1.500000000000000000 ) ) ;
#25094=CARTESIAN_POINT ( 'NONE',  ( 107.5618622547647334, -18.98489936157325175, -4.518577578190647870 ) ) ;
#25098=VECTOR ( 'NONE', #4597, 1000.000000000000000 ) ;
#25104=CARTESIAN_POINT ( 'NONE',  ( 20.66542725970890260, -21.74162791314452647, -1.399019267719719295 ) ) ;
#25111=CARTESIAN_POINT ( 'NONE',  ( -50.60000000000000142, -10.96966150227468972, 1.500000000000000000 ) ) ;
#25115=CARTESIAN_POINT ( 'NONE',  ( 2.363212477606322359, -0.1552069907123501680, -1.757289734063390396 ) ) ;
#25116=ORIENTED_EDGE ( 'NONE', *, *, #8833, .T. ) ;
#25117=CARTESIAN_POINT ( 'NONE',  ( 9.350000000000001421, 0.000000000000000000, 1.000000000000000000 ) ) ;
#25122=AXIS2_PLACEMENT_3D ( 'NONE', #13360, #10699, #20754 ) ;
#25125=CARTESIAN_POINT ( 'NONE',  ( -2.984394142476101575, -0.2504768897242942161, 1.438806226522167497 ) ) ;
#25127=ORIENTED_EDGE ( 'NONE', *, *, #161, .T. ) ;
#25129=EDGE_CURVE ( 'NONE', #5578, #8757, #31893, .T. ) ;
#25130=EDGE_CURVE ( 'NONE', #4070, #23722, #3591, .T. ) ;
#25131=ORIENTED_EDGE ( 'NONE', *, *, #32787, .F. ) ;
#25134=CARTESIAN_POINT ( 'NONE',  ( 21.33742408005302593, -21.80181733053987614, 1.346293739633778852 ) ) ;
#25138=CARTESIAN_POINT ( 'NONE',  ( 108.0285590637734430, -18.48060553035487530, 4.343942861253616172 ) ) ;
#25141=CARTESIAN_POINT ( 'NONE',  ( 107.4514419172549680, -17.38041855283392678, -4.563595182958755991 ) ) ;
#25142=CARTESIAN_POINT ( 'NONE',  ( 25.42756288599179726, -17.55292975162311464, 1.197473197312291404 ) ) ;
#25155=VERTEX_POINT ( 'NONE', #8387 ) ;
#25164=CARTESIAN_POINT ( 'NONE',  ( 108.0213121623446000, -18.37625195254145893, 5.107626725122443645 ) ) ;
#25166=CARTESIAN_POINT ( 'NONE',  ( 8.438303502872338768, -14.31955465834176522, 1.499999999999858780 ) ) ;
#25171=CARTESIAN_POINT ( 'NONE',  ( -1.427519812010940470, -14.09177734493767531, 1.500000000000000222 ) ) ;
#25175=CARTESIAN_POINT ( 'NONE',  ( 108.1300413742128228, -19.95926608421463300, 1.392287898181946426 ) ) ;
#25178=CARTESIAN_POINT ( 'NONE',  ( 24.37505892579753208, -17.33881490880284204, -1.312584468236271062 ) ) ;
#25181=CARTESIAN_POINT ( 'NONE',  ( 21.51848342574702500, -21.75572564449080559, -1.472637297274180357 ) ) ;
#25186=CARTESIAN_POINT ( 'NONE',  ( 2.632061376486628301, -0.4999999999999981681, 1.949999999999999956 ) ) ;
#25194=CARTESIAN_POINT ( 'NONE',  ( 22.95054569172093650, -21.90694603883944325, 1.257390168162776378 ) ) ;
#25206=CARTESIAN_POINT ( 'NONE',  ( 108.1300413742128228, -19.95926608421463300, 1.392287898181946426 ) ) ;
#25207=CARTESIAN_POINT ( 'NONE',  ( 2.542833796814050640, -3.270102266984055818E-17, -1.603032409779283407 ) ) ;
#25210=VERTEX_POINT ( 'NONE', #26938 ) ;
#25232=CARTESIAN_POINT ( 'NONE',  ( 18.46868857681155163, -16.82956153233909546, -1.753327331145430934 ) ) ;
#25233=CARTESIAN_POINT ( 'NONE',  ( 6.220890055307039646, -15.20372210278347680, 4.522129901861157819 ) ) ;
#25242=CARTESIAN_POINT ( 'NONE',  ( 21.60307794872815279, -17.26039173292174311, 1.753143643191834355 ) ) ;
#25249=CARTESIAN_POINT ( 'NONE',  ( -0.3078811530705855004, -15.09896951176102498, -1.499999999999999556 ) ) ;
#25251=AXIS2_PLACEMENT_3D ( 'NONE', #27370, #17159, #19849 ) ;
#25254=VECTOR ( 'NONE', #25299, 999.9999999999998863 ) ;
#25271=CARTESIAN_POINT ( 'NONE',  ( -2.962992063741595405, -11.77309494928644185, 1.500000000000000000 ) ) ;
#25276=ORIENTED_EDGE ( 'NONE', *, *, #10611, .T. ) ;
#25278=CARTESIAN_POINT ( 'NONE',  ( -1.170068671574867158, -6.059534462705557623, 4.522129901861156931 ) ) ;
#25287=AXIS2_PLACEMENT_3D ( 'NONE', #6354, #27089, #6534 ) ;
#25295=CYLINDRICAL_SURFACE ( 'NONE', #18843, 0.5000000000000004441 ) ;
#25299=DIRECTION ( 'NONE',  ( 0.7071067811865467956, 0.000000000000000000, 0.7071067811865483499 ) ) ;
#25307=CARTESIAN_POINT ( 'NONE',  ( 17.36028307726380504, -18.11957666779667875, -4.522129901861164925 ) ) ;
#25314=ORIENTED_EDGE ( 'NONE', *, *, #30826, .F. ) ;
#25318=ORIENTED_EDGE ( 'NONE', *, *, #25949, .T. ) ;
#25326=CARTESIAN_POINT ( 'NONE',  ( 2.602069235114819801, -11.36561507724872833, -1.760364443161137826 ) ) ;
#25330=CARTESIAN_POINT ( 'NONE',  ( -29.24402871571406237, -27.93932300454937590, 11.00000000000000000 ) ) ;
#25332=CARTESIAN_POINT ( 'NONE',  ( 25.38393466668192744, -17.54878733605304220, 1.232996826557162251 ) ) ;
#25333=CARTESIAN_POINT ( 'NONE',  ( 3.568565220189130027, -17.77020640688392916, 0.9788672205877712029 ) ) ;
#25342=ORIENTED_EDGE ( 'NONE', *, *, #9393, .F. ) ;
#25351=ORIENTED_EDGE ( 'NONE', *, *, #32513, .F. ) ;
#25357=CARTESIAN_POINT ( 'NONE',  ( -1.487372016167590738, -13.44698662728717764, 1.744337752715020340 ) ) ;
#25366=CARTESIAN_POINT ( 'NONE',  ( 21.36297440260807790, -21.76512774916147208, -1.415548493914890793 ) ) ;
#25373=CARTESIAN_POINT ( 'NONE',  ( 24.39840143146020068, -17.41297703074901193, 1.421218545007173040 ) ) ;
#25376=CARTESIAN_POINT ( 'NONE',  ( 23.27353278736381981, -21.94187821002792660, 1.000000000000000000 ) ) ;
#25380=ORIENTED_EDGE ( 'NONE', *, *, #25903, .T. ) ;
#25384=CARTESIAN_POINT ( 'NONE',  ( 19.72181367955163012, -17.01552588882587713, 1.753252306182963238 ) ) ;
#25402=CARTESIAN_POINT ( 'NONE',  ( -0.3880080537174173672, -2.647099810594272906, 4.522129901861157819 ) ) ;
#25406=CARTESIAN_POINT ( 'NONE',  ( -23.35000000000000142, -10.96966150227469505, -11.09540449768827308 ) ) ;
#25409=CARTESIAN_POINT ( 'NONE',  ( 24.34295195636289222, -17.38504247894183408, 1.375705049360312460 ) ) ;
#25412=( BOUNDED_SURFACE ( )  B_SPLINE_SURFACE ( 3, 2, ( 
 ( #23358, #20706, #5158 ),
 ( #13005, #10492, #3310 ),
 ( #26045, #28560, #31063 ),
 ( #25705, #15835, #8154 ),
 ( #5655, #28209, #2832 ),
 ( #28376, #5801, #20853 ),
 ( #23025, #5493, #7977 ),
 ( #18171, #5311, #3005 ),
 ( #18361, #147, #10333 ),
 ( #3147, #31245, #15490 ),
 ( #8318, #13306, #15333 ),
 ( #23514, #23696, #626 ),
 ( #13158, #2644, #466 ),
 ( #10821, #23216, #25892 ),
 ( #20548, #13482, #10645 ),
 ( #30756, #21036, #18515 ),
 ( #15683, #28708, #15979 ),
 ( #26202, #320, #814 ),
 ( #10991, #21192, #31390 ),
 ( #30906, #8465, #18662 ),
 ( #25538, #12811, #7829 ),
 ( #18022, #26853, #29539 ),
 ( #6140, #5961, #11480 ),
 ( #16468, #11792, #21996 ),
 ( #6437, #31730, #13790 ),
 ( #1452, #29050, #24340 ),
 ( #19156, #21674, #16324 ),
 ( #24483, #3970, #32224 ),
 ( #9290, #18849, #26532 ),
 ( #11310, #28861, #3633 ),
 ( #1115, #27018, #23994 ),
 ( #21518, #16641, #14288 ),
 ( #8806, #4121, #16159 ),
 ( #24176, #6626, #19010 ),
 ( #13956, #26387, #3489 ),
 ( #11629, #8628, #1603 ),
 ( #13645, #31544, #31881 ),
 ( #23849, #14140, #958 ) ),
 .UNSPECIFIED., .F., .F., .F. ) 
 B_SPLINE_SURFACE_WITH_KNOTS ( ( 4, 2, 2, 2, 2, 2, 2, 2, 2, 2, 2, 2, 2, 2, 2, 2, 2, 2, 4 ),
 ( 3, 3 ),
 ( 0.01025725344258522978, 0.01409333659602417070, 0.01792941974946311162, 0.02176550290290205428, 0.02368354447962152387, 0.02560158605634099693, 0.02656060684470073346, 0.02751962763306047000, 0.02847864842142020653, 0.02943766920977993959, 0.03135571078649940918, 0.03231473157485914571, 0.03327375236321888224, 0.03423277315157861878, 0.03519179393993834837, 0.03710983551665782143, 0.03902787709337729449, 0.03998689788173703102, 0.04094591867009676756 ),
 ( 0.000000000000000000, 1.000000000000000000 ),
 .UNSPECIFIED. ) 
 GEOMETRIC_REPRESENTATION_ITEM ( )  RATIONAL_B_SPLINE_SURFACE ( (
 ( 1.000000000000000000, 0.7071067811865475727, 1.000000000000000000),
 ( 1.000000000000000000, 0.7071067811865475727, 1.000000000000000000),
 ( 1.000000000000000000, 0.7071067811865475727, 1.000000000000000000),
 ( 1.000000000000000000, 0.7071067811865475727, 1.000000000000000000),
 ( 1.000000000000000000, 0.7071067811865475727, 1.000000000000000000),
 ( 1.000000000000000000, 0.7071067811865475727, 1.000000000000000000),
 ( 1.000000000000000000, 0.7071067811865475727, 1.000000000000000000),
 ( 1.000000000000000000, 0.7071067811865475727, 1.000000000000000000),
 ( 1.000000000000000000, 0.7071067811865471286, 1.000000000000000000),
 ( 1.000000000000000000, 0.7071067811865471286, 1.000000000000000000),
 ( 1.000000000000000000, 0.7071067811865475727, 1.000000000000000000),
 ( 1.000000000000000000, 0.7071067811865475727, 1.000000000000000000),
 ( 1.000000000000000000, 0.7071067811865465735, 1.000000000000000000),
 ( 1.000000000000000000, 0.7071067811865465735, 1.000000000000000000),
 ( 1.000000000000000000, 0.7071067811865475727, 1.000000000000000000),
 ( 1.000000000000000000, 0.7071067811865475727, 1.000000000000000000),
 ( 1.000000000000000000, 0.7071067811865483499, 1.000000000000000000),
 ( 1.000000000000000000, 0.7071067811865483499, 1.000000000000000000),
 ( 1.000000000000000000, 0.7071067811865475727, 1.000000000000000000),
 ( 1.000000000000000000, 0.7071067811865475727, 1.000000000000000000),
 ( 1.000000000000000000, 0.7071067811865475727, 1.000000000000000000),
 ( 1.000000000000000000, 0.7071067811865475727, 1.000000000000000000),
 ( 1.000000000000000000, 0.7071067811865475727, 1.000000000000000000),
 ( 1.000000000000000000, 0.7071067811865475727, 1.000000000000000000),
 ( 1.000000000000000000, 0.7071067811865481278, 1.000000000000000000),
 ( 1.000000000000000000, 0.7071067811865481278, 1.000000000000000000),
 ( 1.000000000000000000, 0.7071067811865476838, 1.000000000000000000),
 ( 1.000000000000000000, 0.7071067811865476838, 1.000000000000000000),
 ( 1.000000000000000000, 0.7071067811865475727, 1.000000000000000000),
 ( 1.000000000000000000, 0.7071067811865475727, 1.000000000000000000),
 ( 1.000000000000000000, 0.7071067811865476838, 1.000000000000000000),
 ( 1.000000000000000000, 0.7071067811865476838, 1.000000000000000000),
 ( 1.000000000000000000, 0.7071067811865476838, 1.000000000000000000),
 ( 1.000000000000000000, 0.7071067811865476838, 1.000000000000000000),
 ( 1.000000000000000000, 0.7071067811865475727, 1.000000000000000000),
 ( 1.000000000000000000, 0.7071067811865475727, 1.000000000000000000),
 ( 1.000000000000000000, 0.7071067811865475727, 1.000000000000000000),
 ( 1.000000000000000000, 0.7071067811865475727, 1.000000000000000000) ) ) 
 REPRESENTATION_ITEM ( '' )  SURFACE ( )  );
#25418=CARTESIAN_POINT ( 'NONE',  ( -2.249829636652692866, -12.47730163696535932, -1.743879033398587408 ) ) ;
#25429=ORIENTED_EDGE ( 'NONE', *, *, #19148, .T. ) ;
#25434=CARTESIAN_POINT ( 'NONE',  ( 43.74661801760413482, -24.08792321988613594, -1.500000000000000000 ) ) ;
#25442=CARTESIAN_POINT ( 'NONE',  ( 5.539187815124529735, -17.99452416398525045, 1.748481376116554742 ) ) ;
#25444=CARTESIAN_POINT ( 'NONE',  ( 9.437548970008963423, 0.1642588933130686435, -1.500000000000000000 ) ) ;
#25460=CARTESIAN_POINT ( 'NONE',  ( -23.35000000000000142, -10.96966150227469505, -11.00000000000000000 ) ) ;
#25462=CARTESIAN_POINT ( 'NONE',  ( 0.1610798642962581184, -10.72944008624797974, -4.522129901861164925 ) ) ;
#25464=CARTESIAN_POINT ( 'NONE',  ( 11.02666429642763646, -12.67048613693261672, 1.000000000000000222 ) ) ;
#25469=CARTESIAN_POINT ( 'NONE',  ( 108.1288400433390393, -19.92462668933126579, 3.636029349014985090 ) ) ;
#25476=CARTESIAN_POINT ( 'NONE',  ( 0.2678094507063553675, -7.640026513854723866, -1.500000000000000000 ) ) ;
#25478=CARTESIAN_POINT ( 'NONE',  ( 0.1161733546981892212, -6.474819093472221176, -1.773743352647767502 ) ) ;
#25486=CARTESIAN_POINT ( 'NONE',  ( 25.43628628520003687, -17.54453570558172260, 1.030327512441693516 ) ) ;
#25487=CARTESIAN_POINT ( 'NONE',  ( 6.655951778521610684, -18.71196003547629516, 1.500000000000000000 ) ) ;
#25488=CARTESIAN_POINT ( 'NONE',  ( 13.13178786250159469, -17.31629153505179275, 4.522129901861156931 ) ) ;
#25498=CARTESIAN_POINT ( 'NONE',  ( 18.02407935480697532, -21.25192265502663247, -1.530583967965385650 ) ) ;
#25499=ORIENTED_EDGE ( 'NONE', *, *, #29625, .T. ) ;
#25501=DIRECTION ( 'NONE',  ( 0.000000000000000000, 0.000000000000000000, 1.000000000000000000 ) ) ;
#25506=CARTESIAN_POINT ( 'NONE',  ( 18.53175858344379634, -21.44524224917989130, -1.499999999999999556 ) ) ;
#25509=CARTESIAN_POINT ( 'NONE',  ( -3.657583913946364174, -9.739478672526409753, 1.743552423778348182 ) ) ;
#25511=CARTESIAN_POINT ( 'NONE',  ( 108.0291781248180598, -18.48951985539477505, -4.325670280508457921 ) ) ;
#25513=EDGE_LOOP ( 'NONE', ( #33025, #3646, #7585, #841 ) ) ;
#25515=CARTESIAN_POINT ( 'NONE',  ( 108.0980302657043239, -19.48097355589947810, 2.293520641443586250 ) ) ;
#25517=CARTESIAN_POINT ( 'NONE',  ( 107.6641948605100083, -20.45809826282308208, 1.500000000000000000 ) ) ;
#25528=CARTESIAN_POINT ( 'NONE',  ( -23.35000000000000142, -10.96966150227469505, -11.50000000000000000 ) ) ;
#25537=CARTESIAN_POINT ( 'NONE',  ( 8.808801416188583033, -14.57828162013994344, 1.754901028757273496 ) ) ;
#25538=CARTESIAN_POINT ( 'NONE',  ( 7.650166299107816315, -9.403575859904028889, 1.000000000000000000 ) ) ;
#25539=ORIENTED_EDGE ( 'NONE', *, *, #854, .T. ) ;
#25562=DIRECTION ( 'NONE',  ( -0.000000000000000000, -1.000000000000000000, 0.000000000000000000 ) ) ;
#25564=CARTESIAN_POINT ( 'NONE',  ( 23.03249562537846984, -17.15537757201845181, 1.465178982930523066 ) ) ;
#25587=VERTEX_POINT ( 'NONE', #5190 ) ;
#25588=CARTESIAN_POINT ( 'NONE',  ( -0.1366093623685602776, -14.96249823008941604, -1.500000000000000000 ) ) ;
#25596=CARTESIAN_POINT ( 'NONE',  ( 23.22564588060107482, -21.93932300456764040, 1.500000000000000000 ) ) ;
#25597=CARTESIAN_POINT ( 'NONE',  ( 0.9232102171129904500, 0.000000000000000000, 4.522129901861156931 ) ) ;
#25598=CARTESIAN_POINT ( 'NONE',  ( -0.3253503806707769841, -14.55949634428441009, 1.745204865412639306 ) ) ;
#25600=CARTESIAN_POINT ( 'NONE',  ( 24.80306213860341558, -17.49230408913766865, 1.499999999999999778 ) ) ;
#25602=EDGE_LOOP ( 'NONE', ( #20519, #20103, #31314, #14683 ) ) ;
#25611=CARTESIAN_POINT ( 'NONE',  ( 23.04481819307356005, -21.91824019632980836, 1.500000000000000000 ) ) ;
#25619=CARTESIAN_POINT ( 'NONE',  ( -0.3880080537174158128, -2.647099810593990465, -4.522129901861164925 ) ) ;
#25634=CARTESIAN_POINT ( 'NONE',  ( 16.80274661516410006, -16.53680364986711737, 1.500000000000000000 ) ) ;
#25637=CIRCLE ( 'NONE', #14971, 10.96966150227469328 ) ;
#25638=CARTESIAN_POINT ( 'NONE',  ( 0.3941402309825520200, -8.465515007537584680, -1.772213618796667722 ) ) ;
#25640=CARTESIAN_POINT ( 'NONE',  ( 17.02282544784375418, -15.06900748075850416, -1.000000000000138556 ) ) ;
#25647=CARTESIAN_POINT ( 'NONE',  ( 43.89586892125095119, -24.33975351994666525, 0.9788672205877712029 ) ) ;
#25648=CARTESIAN_POINT ( 'NONE',  ( -1.047937531484013585, -4.989690239015236450, 4.522129901861156931 ) ) ;
#25653=DIRECTION ( 'NONE',  ( -0.000000000000000000, -1.000000000000000000, -0.000000000000000000 ) ) ;
#25663=AXIS2_PLACEMENT_3D ( 'NONE', #7962, #20531, #2476 ) ;
#25677=B_SPLINE_CURVE_WITH_KNOTS ( 'NONE', 3,
 ( #3728, #29144, #13894, #18775, #24106, #5895, #11084, #31664, #21620, #5750, #752, #8895, #29293 ),
 .UNSPECIFIED., .F., .F.,
 ( 4, 3, 3, 3, 4 ),
 ( 8.673617379884035472E-19, 0.0002329468921300049229, 0.001653916346091481061, 0.002601229312345668468, 0.003274063357856006780 ),
 .UNSPECIFIED. ) ;
#25683=EDGE_LOOP ( 'NONE', ( #21760, #6474, #19777, #16508, #12688, #26880 ) ) ;
#25686=CARTESIAN_POINT ( 'NONE',  ( -14.47914180357919989, -28.43932300454937590, -4.314460059828594041 ) ) ;
#25691=CARTESIAN_POINT ( 'NONE',  ( 23.05582684282763495, -21.92970410991115671, 1.098153529935464778 ) ) ;
#25692=B_SPLINE_CURVE_WITH_KNOTS ( 'NONE', 3,
 ( #15612, #18113, #28309, #31000, #26316, #411 ),
 .UNSPECIFIED., .F., .F.,
 ( 4, 2, 4 ),
 ( 2.872315617932023530E-05, 0.0004097954672333709329, 0.0007908677782874217084 ),
 .UNSPECIFIED. ) ;
#25704=CARTESIAN_POINT ( 'NONE',  ( 6.944655341030708584, -13.87327314716643833, 1.755631441884608623 ) ) ;
#25705=CARTESIAN_POINT ( 'NONE',  ( 20.69346795569472164, -16.15118080712967696, 0.9999999999998612221 ) ) ;
#25725=EDGE_CURVE ( 'NONE', #9323, #29074, #3418, .T. ) ;
#25726=CARTESIAN_POINT ( 'NONE',  ( 14.65314785874341119, -16.14430731538131170, -1.753659771011512269 ) ) ;
#25727=FACE_OUTER_BOUND ( 'NONE', #5052, .T. ) ;
#25731=CIRCLE ( 'NONE', #24109, 2.099999999999997868 ) ;
#25769=CARTESIAN_POINT ( 'NONE',  ( 8.528645601772334217, -0.5000000000000000000, -1.500000000000000000 ) ) ;
#25770=CARTESIAN_POINT ( 'NONE',  ( 7.611844841314693078, -2.453950335954177220, 1.500000000000000000 ) ) ;
#25772=EDGE_CURVE ( 'NONE', #25587, #14095, #22539, .T. ) ;
#25773=CARTESIAN_POINT ( 'NONE',  ( 107.6365100547759397, -20.05945961560171753, -2.316983664052866043 ) ) ;
#25779=CARTESIAN_POINT ( 'NONE',  ( -2.249933675096747354, -12.47715805579040982, 1.743879002063110528 ) ) ;
#25782=DIRECTION ( 'NONE',  ( -0.000000000000000000, 0.000000000000000000, 1.000000000000000000 ) ) ;
#25793=DIRECTION ( 'NONE',  ( 0.000000000000000000, 0.000000000000000000, -1.000000000000000000 ) ) ;
#25795=CARTESIAN_POINT ( 'NONE',  ( -55.09999999999999432, -10.96966150227468972, 6.999999999999999112 ) ) ;
#25801=ORIENTED_EDGE ( 'NONE', *, *, #2251, .T. ) ;
#25805=CARTESIAN_POINT ( 'NONE',  ( 0.1517578099452217555, -1.375880305419572514, -4.522129901861164925 ) ) ;
#25807=CARTESIAN_POINT ( 'NONE',  ( 107.9482911536555605, -17.32476759280069700, 4.518410020412943595 ) ) ;
#25812=CARTESIAN_POINT ( 'NONE',  ( -3.226940125355896249, -1.840961574400530945E-05, 0.9957093966831336296 ) ) ;
#25823=CARTESIAN_POINT ( 'NONE',  ( 6.013832568680315127, -13.53405802968792848, 1.500000000000000000 ) ) ;
#25826=LINE ( 'NONE', #18284, #7981 ) ;
#25833=CARTESIAN_POINT ( 'NONE',  ( 3.857446109187582017, -11.79189269903710624, 1.500000000000000222 ) ) ;
#25838=CARTESIAN_POINT ( 'NONE',  ( 3.583596913636438064, -0.01388667853607550469, 1.134179515492628632 ) ) ;
#25840=CARTESIAN_POINT ( 'NONE',  ( -50.60000000000000142, -10.96966150227468972, 0.9999999999999991118 ) ) ;
#25857=CARTESIAN_POINT ( 'NONE',  ( 3.554613218822866738, -15.76807188677470073, -4.522129901861166701 ) ) ;
#25863=CONICAL_SURFACE ( 'NONE', #21580, 9.500000000000003553, 0.1919862177193767117 ) ;
#25867=CARTESIAN_POINT ( 'NONE',  ( 108.0291781248179177, -18.48951985539285658, 4.325670280512381005 ) ) ;
#25879=CARTESIAN_POINT ( 'NONE',  ( -15.60935834747760609, -25.43932300454937945, 1.500000000000000000 ) ) ;
#25883=CARTESIAN_POINT ( 'NONE',  ( 22.54151439274395585, -21.86162235810803267, 1.385141676429126001 ) ) ;
#25887=VERTEX_POINT ( 'NONE', #10893 ) ;
#25892=CARTESIAN_POINT ( 'NONE',  ( 9.827398781245818782, -12.51289689083618129, 1.500000000000000000 ) ) ;
#25896=ORIENTED_EDGE ( 'NONE', *, *, #20448, .T. ) ;
#25900=CARTESIAN_POINT ( 'NONE',  ( 2.281627749324420140, -0.2935656086769634077, -1.757435426329174710 ) ) ;
#25903=EDGE_CURVE ( 'NONE', #24091, #7488, #16380, .T. ) ;
#25917=CARTESIAN_POINT ( 'NONE',  ( 23.81423349025420322, -17.27971345279105719, -1.410233427488536417 ) ) ;
#25924=B_SPLINE_CURVE_WITH_KNOTS ( 'NONE', 3,
 ( #11350, #16685, #4004, #11835, #21553, #31763, #8836, #32073 ),
 .UNSPECIFIED., .F., .F.,
 ( 4, 2, 2, 4 ),
 ( -5.999999999462396917E-08, 0.0004626438357226977461, 0.0006939957535840434594, 0.0009253476714453893895 ),
 .UNSPECIFIED. ) ;
#25927=ORIENTED_EDGE ( 'NONE', *, *, #15920, .F. ) ;
#25933=CARTESIAN_POINT ( 'NONE',  ( 14.29295439700192993, -14.14386588685529489, -1.000000000000000000 ) ) ;
#25934=VERTEX_POINT ( 'NONE', #13365 ) ;
#25947=CARTESIAN_POINT ( 'NONE',  ( -4.154891947659814733, -6.512605193776770385, 1.745058689288190523 ) ) ;
#25949=EDGE_CURVE ( 'NONE', #31647, #25934, #23683, .T. ) ;
#25951=DIRECTION ( 'NONE',  ( 0.000000000000000000, 0.000000000000000000, 1.000000000000000000 ) ) ;
#25965=ORIENTED_EDGE ( 'NONE', *, *, #26107, .T. ) ;
#25971=CARTESIAN_POINT ( 'NONE',  ( 20.66455810932185955, -16.14294586248262320, 1.000000000000000000 ) ) ;
#25972=CARTESIAN_POINT ( 'NONE',  ( 107.9565509429370849, -17.44370650368591313, 4.757555836516734082 ) ) ;
#25977=LINE ( 'NONE', #3569, #23478 ) ;
#25992=CARTESIAN_POINT ( 'NONE',  ( 107.8981067246555625, -16.60212429951632629, 1.900353104894979772 ) ) ;
#25994=CARTESIAN_POINT ( 'NONE',  ( 1.449903671498899538, -2.780906680908541873, 1.499999999999999112 ) ) ;
#25996=EDGE_CURVE ( 'NONE', #12596, #7729, #18755, .T. ) ;
#25998=CARTESIAN_POINT ( 'NONE',  ( 2.692942092879393456, -0.02443046219423304979, 1.307625729273631077 ) ) ;
#26008=CARTESIAN_POINT ( 'NONE',  ( 18.70218739254009677, -21.34730519116027025, -1.543632415226145804 ) ) ;
#26009=ORIENTED_EDGE ( 'NONE', *, *, #22639, .T. ) ;
#26034=CARTESIAN_POINT ( 'NONE',  ( -15.51216819290874227, -25.44850941282521006, 1.500000000000000000 ) ) ;
#26035=CARTESIAN_POINT ( 'NONE',  ( 23.22234548918896380, -21.93639154399404489, 1.104776513122921022 ) ) ;
#26038=B_SPLINE_CURVE_WITH_KNOTS ( 'NONE', 3,
 ( #28392, #2344, #7989, #15695 ),
 .UNSPECIFIED., .F., .F.,
 ( 4, 4 ),
 ( 0.005732069968871193570, 0.4737525964755946450 ),
 .UNSPECIFIED. ) ;
#26045=CARTESIAN_POINT ( 'NONE',  ( 23.15368348421776901, -16.86203458153667256, 1.000000000000138778 ) ) ;
#26074=CARTESIAN_POINT ( 'NONE',  ( 3.381541507458994289, -0.06919447570412250170, -1.261810069052565986 ) ) ;
#26075=DIRECTION ( 'NONE',  ( 1.000000000000000000, 0.000000000000000000, 0.000000000000000000 ) ) ;
#26077=DIRECTION ( 'NONE',  ( 1.000000000000000000, 0.000000000000000000, 0.000000000000000000 ) ) ;
#26088=ADVANCED_FACE ( 'NONE', ( #4030 ), #1305, .T. ) ;
#26092=CARTESIAN_POINT ( 'NONE',  ( 7.189332377417184006, -9.531173777829009097, 1.500000000000000000 ) ) ;
#26094=CARTESIAN_POINT ( 'NONE',  ( -15.12340757463330476, -27.93932300454937590, -0.9999999999999997780 ) ) ;
#26099=CARTESIAN_POINT ( 'NONE',  ( -0.1325319112326446558, -14.88632472074928081, 1.499999999999681366 ) ) ;
#26100=CARTESIAN_POINT ( 'NONE',  ( -29.24402871571405882, 0.000000000000000000, 11.50000000000000000 ) ) ;
#26101=CARTESIAN_POINT ( 'NONE',  ( 3.569153896158649530, -0.01695480042954938815, 1.144240241240434663 ) ) ;
#26102=CARTESIAN_POINT ( 'NONE',  ( 23.85324836636559453, -17.43424264171722982, 1.580747861890658745 ) ) ;
#26105=CARTESIAN_POINT ( 'NONE',  ( -31.15578486440642436, -25.44239456788696785, 1.499999999999999778 ) ) ;
#26107=EDGE_CURVE ( 'NONE', #32817, #25210, #28413, .T. ) ;
#26110=DIRECTION ( 'NONE',  ( 0.9816271834476637537, 0.000000000000000000, 0.1908089953765453872 ) ) ;
#26111=CARTESIAN_POINT ( 'NONE',  ( 108.0291781248179177, -18.48951985539285658, 4.325670280512381005 ) ) ;
#26112=AXIS2_PLACEMENT_3D ( 'NONE', #23828, #940, #10627 ) ;
#26113=EDGE_CURVE ( 'NONE', #15269, #1202, #9482, .T. ) ;
#26114=CARTESIAN_POINT ( 'NONE',  ( -23.35000000000000142, -10.96966150227469505, -11.09540449768827308 ) ) ;
#26121=CARTESIAN_POINT ( 'NONE',  ( 108.0076953296759683, -18.18017294959541630, 4.637765880993337753 ) ) ;
#26138=FACE_OUTER_BOUND ( 'NONE', #33043, .T. ) ;
#26139=CARTESIAN_POINT ( 'NONE',  ( 107.4495515710665359, -17.35288078708288140, -4.502149265236362830 ) ) ;
#26142=AXIS2_PLACEMENT_3D ( 'NONE', #17598, #15415, #22949 ) ;
#26143=CARTESIAN_POINT ( 'NONE',  ( 107.5617723795401872, -18.98359893170738744, -4.522129901861166701 ) ) ;
#26144=CARTESIAN_POINT ( 'NONE',  ( 4.959216681210401489, -12.47312135805140088, 1.500000000000000666 ) ) ;
#26153=EDGE_CURVE ( 'NONE', #1139, #12534, #11532, .T. ) ;
#26159=CARTESIAN_POINT ( 'NONE',  ( 18.74274612900900294, -21.25842652921760489, -1.734019191250015357 ) ) ;
#26165=ORIENTED_EDGE ( 'NONE', *, *, #30556, .F. ) ;
#26166=DIRECTION ( 'NONE',  ( 0.000000000000000000, 0.000000000000000000, 1.000000000000000000 ) ) ;
#26168=CARTESIAN_POINT ( 'NONE',  ( -4.176822952888146645, -3.225712836239801096, -0.9788672205760856615 ) ) ;
#26172=ORIENTED_EDGE ( 'NONE', *, *, #9943, .T. ) ;
#26185=CARTESIAN_POINT ( 'NONE',  ( 109.5084093630373729, -17.21855534384546971, -4.522129901861164925 ) ) ;
#26190=CARTESIAN_POINT ( 'NONE',  ( 22.00639167669143603, -21.80013755708273848, 1.500000000000000000 ) ) ;
#26196=ORIENTED_EDGE ( 'NONE', *, *, #27368, .T. ) ;
#26202=CARTESIAN_POINT ( 'NONE',  ( 8.690654615650863946, -10.89241706942921084, 1.000000000000000000 ) ) ;
#26217=ADVANCED_FACE ( 'NONE', ( #11343 ), #28889, .T. ) ;
#26219=CARTESIAN_POINT ( 'NONE',  ( 8.528645601772334217, -0.5000000000000011102, 1.500000000000000000 ) ) ;
#26242=CARTESIAN_POINT ( 'NONE',  ( -30.98484230743790135, -10.96966150227469328, -11.09540449768827308 ) ) ;
#26249=CARTESIAN_POINT ( 'NONE',  ( 19.54632490742270434, -15.82374593131492801, -1.000000000000000000 ) ) ;
#26278=CARTESIAN_POINT ( 'NONE',  ( 107.3818320530746320, -16.38511360653449600, 0.000000000000000000 ) ) ;
#26279=CARTESIAN_POINT ( 'NONE',  ( -2.655659815843975036, 0.1700350810728117334, -1.254089647469598612 ) ) ;
#26282=B_SPLINE_SURFACE_WITH_KNOTS ( 'NONE', 1, 3, ( 
 ( #14599, #24804, #12094, #22292, #32503, #19780, #29988, #7080, #28477, #3078, #18263, #540, #2571, #7756, #55, #20466 ),
 ( #2418, #2929, #15259, #12588, #15765, #15090, #15408, #5398, #30837, #12737, #20629, #10729, #13091, #8249, #5234, #18442 ),
 ( #22943, #249, #30681, #25307, #10242, #17948, #28135, #13234, #25462, #23290, #15590, #7903, #393, #25619, #25805, #18093 ) ),
 .UNSPECIFIED., .F., .F., .F.,
 ( 2, 1, 2 ),
 ( 4, 2, 2, 2, 2, 2, 2, 4 ),
 ( -0.1724389077684020943, 0.000000000000000000, 1.000000000000000000 ),
 ( 0.000000000000000000, 0.5000000000000000000, 0.6250000000000000000, 0.7500000000000000000, 0.8125000000000000000, 0.8750000000000000000, 0.9375000000000000000, 1.000000000000000000 ),
 .UNSPECIFIED. ) ;
#26287=AXIS2_PLACEMENT_3D ( 'NONE', #11780, #21985, #32210 ) ;
#26290=CARTESIAN_POINT ( 'NONE',  ( 17.37538333147191949, -21.16291065652713144, 1.499999999999996891 ) ) ;
#26291=CARTESIAN_POINT ( 'NONE',  ( -2.988195613244121418, -0.2505024616802880577, -1.434921225358063879 ) ) ;
#26295=CARTESIAN_POINT ( 'NONE',  ( 107.9822664857447450, -17.81400392288609780, 4.398951253679784124 ) ) ;
#26300=ORIENTED_EDGE ( 'NONE', *, *, #23981, .T. ) ;
#26306=CARTESIAN_POINT ( 'NONE',  ( 17.39502519979081185, -21.04076415203811479, -1.751145182513948573 ) ) ;
#26311=CARTESIAN_POINT ( 'NONE',  ( -4.155175026768859858, -6.548389795709734784, -1.745040213387592187 ) ) ;
#26314=CARTESIAN_POINT ( 'NONE',  ( 108.1166869805057900, -19.74962560783402310, -1.742921814161544569 ) ) ;
#26316=CARTESIAN_POINT ( 'NONE',  ( 107.7918428252582714, -20.44935860102534519, -1.500028854543400181 ) ) ;
#26317=CARTESIAN_POINT ( 'NONE',  ( 107.9477480374278571, -17.31694685422549540, -4.497032296529938300 ) ) ;
#26339=CARTESIAN_POINT ( 'NONE',  ( -15.26206363037222857, -25.49623161314220710, 1.500000000000013989 ) ) ;
#26342=CARTESIAN_POINT ( 'NONE',  ( 0.5492144360001000036, -7.007719521915549699, -1.500000000000000666 ) ) ;
#26352=CYLINDRICAL_SURFACE ( 'NONE', #32648, 8.500000000000000000 ) ;
#26357=ORIENTED_EDGE ( 'NONE', *, *, #9454, .T. ) ;
#26362=CARTESIAN_POINT ( 'NONE',  ( 107.5579690617258848, -18.92842216329967542, 4.649137216790264482 ) ) ;
#26375=DIRECTION ( 'NONE',  ( -1.000000000000000000, 1.387778780781444256E-14, 0.000000000000000000 ) ) ;
#26378=CARTESIAN_POINT ( 'NONE',  ( 21.99035326629933706, -21.86692099231501984, 1.263015267642078054 ) ) ;
#26385=CYLINDRICAL_SURFACE ( 'NONE', #32769, 0.5000000000000004441 ) ;
#26386=CARTESIAN_POINT ( 'NONE',  ( -23.35000000000000142, -10.96966150227469505, 4.000000000000000000 ) ) ;
#26387=CARTESIAN_POINT ( 'NONE',  ( 8.845957756764844859, -0.9823800963980794387, 1.500000000000000000 ) ) ;
#26388=VERTEX_POINT ( 'NONE', #14486 ) ;
#26390=EDGE_CURVE ( 'NONE', #29074, #9056, #13470, .T. ) ;
#26395=CARTESIAN_POINT ( 'NONE',  ( 1.306406124627619736, -9.317880825549442747, 1.499999999999999556 ) ) ;
#26410=DIRECTION ( 'NONE',  ( -0.000000000000000000, -1.000000000000000000, 0.000000000000000000 ) ) ;
#26411=ADVANCED_FACE ( 'NONE', ( #6659 ), #16848, .T. ) ;
#26418=CARTESIAN_POINT ( 'NONE',  ( -0.4046470899336805926, -12.07320251013792323, 5.485967528433935314 ) ) ;
#26427=EDGE_CURVE ( 'NONE', #12534, #32817, #8143, .T. ) ;
#26428=ORIENTED_EDGE ( 'NONE', *, *, #20793, .F. ) ;
#26435=ORIENTED_EDGE ( 'NONE', *, *, #8507, .F. ) ;
#26439=ADVANCED_FACE ( 'NONE', ( #21702 ), #1332, .F. ) ;
#26440=CARTESIAN_POINT ( 'NONE',  ( 6.682200477904377323, -7.715721153621220019, 1.500000000000000000 ) ) ;
#26441=CARTESIAN_POINT ( 'NONE',  ( 0.6153366188829528793, -5.549022540254107128, -1.499999999999999556 ) ) ;
#26447=CARTESIAN_POINT ( 'NONE',  ( 8.235945875020298956, -19.08855532455987358, 1.500000000000315525 ) ) ;
#26462=DIRECTION ( 'NONE',  ( -0.000000000000000000, -1.000000000000000000, -0.000000000000000000 ) ) ;
#26463=CARTESIAN_POINT ( 'NONE',  ( 24.08745121461140570, -17.31475877198404589, 1.374955925956904412 ) ) ;
#26467=FACE_OUTER_BOUND ( 'NONE', #4116, .T. ) ;
#26473=ADVANCED_FACE ( 'NONE', ( #12652 ), #5147, .T. ) ;
#26476=ORIENTED_EDGE ( 'NONE', *, *, #23865, .F. ) ;
#26478=CARTESIAN_POINT ( 'NONE',  ( -2.160443185886078865, -12.59954908393165240, -1.743857611967832622 ) ) ;
#26480=CARTESIAN_POINT ( 'NONE',  ( 7.154313483739800361, -6.723190066291400591, -1.000000000000000000 ) ) ;
#26481=CARTESIAN_POINT ( 'NONE',  ( 107.4501371742636735, -17.36131785966625785, -4.525205764350905824 ) ) ;
#26484=CARTESIAN_POINT ( 'NONE',  ( -2.223027892448374399, -2.927336879245633572, 4.522129901861158707 ) ) ;
#26485=CARTESIAN_POINT ( 'NONE',  ( 2.995361005316234060, -0.2432974174152501834, 1.434016190628301546 ) ) ;
#26486=( BOUNDED_SURFACE ( )  B_SPLINE_SURFACE ( 3, 2, ( 
 ( #32752, #4989, #25376 ),
 ( #15481, #14979, #22356 ),
 ( #32569, #12503, #9829 ),
 ( #12314, #20045, #20355 ),
 ( #30240, #20192, #30389 ),
 ( #7310, #27697, #4802 ),
 ( #7655, #17854, #25194 ),
 ( #2319, #7462, #17662 ),
 ( #2485, #28052, #25883 ),
 ( #26378, #31383, #31534 ),
 ( #13298, #13468, #23505 ),
 ( #15829, #21329, #10809 ) ),
 .UNSPECIFIED., .F., .F., .F. ) 
 B_SPLINE_SURFACE_WITH_KNOTS ( ( 4, 2, 2, 2, 2, 4 ),
 ( 3, 3 ),
 ( 0.01237460209466365035, 0.01250742172631305257, 0.01264024135796245653, 0.01290588062126126270, 0.01343715914785887505, 0.01449971620105409802 ),
 ( 0.000000000000000000, 1.000000000000000000 ),
 .UNSPECIFIED. ) 
 GEOMETRIC_REPRESENTATION_ITEM ( )  RATIONAL_B_SPLINE_SURFACE ( (
 ( 1.000000000000000000, 0.9985794324048127280, 1.000000000000000000),
 ( 1.000000000000000000, 0.9985649967291867490, 1.000000000000000000),
 ( 1.000000000000000000, 0.9977546568863879806, 1.000000000000000000),
 ( 1.000000000000000000, 0.9959318651690971524, 1.000000000000000000),
 ( 1.000000000000000000, 0.9948682866524912738, 1.000000000000000000),
 ( 1.000000000000000000, 0.9916149370760292125, 1.000000000000000000),
 ( 1.000000000000000000, 0.9892930324833523192, 1.000000000000000000),
 ( 1.000000000000000000, 0.9821212088646815719, 1.000000000000000000),
 ( 1.000000000000000000, 0.9771237707447232301, 1.000000000000000000),
 ( 1.000000000000000000, 0.9616790524998285461, 1.000000000000000000),
 ( 1.000000000000000000, 0.9507373671939208792, 1.000000000000000000),
 ( 1.000000000000000000, 0.9391581256476260187, 1.000000000000000000) ) ) 
 REPRESENTATION_ITEM ( '' )  SURFACE ( )  );
#26499=ORIENTED_EDGE ( 'NONE', *, *, #19243, .T. ) ;
#26500=CARTESIAN_POINT ( 'NONE',  ( 25.14437127914504444, -17.52581659214493115, -1.374992938514766116 ) ) ;
#26503=ORIENTED_EDGE ( 'NONE', *, *, #26835, .T. ) ;
#26510=VERTEX_POINT ( 'NONE', #21184 ) ;
#26522=LINE ( 'NONE', #803, #8632 ) ;
#26525=EDGE_CURVE ( 'NONE', #28440, #2672, #5648, .T. ) ;
#26532=CARTESIAN_POINT ( 'NONE',  ( 6.784984840995086586, -5.399320162307873261, 1.500000000000000000 ) ) ;
#26536=CARTESIAN_POINT ( 'NONE',  ( 0.5636301045504281682, -7.175383382611437710, 1.500000000000000444 ) ) ;
#26558=DIRECTION ( 'NONE',  ( -0.000000000000000000, -1.000000000000000000, 0.000000000000000000 ) ) ;
#26559=CARTESIAN_POINT ( 'NONE',  ( 3.554613218822865850, -15.76807188677689986, 4.522129901861159595 ) ) ;
#26569=DIRECTION ( 'NONE',  ( -3.469446951953614189E-15, 0.000000000000000000, -1.000000000000000000 ) ) ;
#26585=ORIENTED_EDGE ( 'NONE', *, *, #4036, .F. ) ;
#26588=CARTESIAN_POINT ( 'NONE',  ( 14.48597245533614064, -20.94846345271118437, 1.500000000000000444 ) ) ;
#26596=B_SPLINE_CURVE_WITH_KNOTS ( 'NONE', 3,
 ( #16139, #23498, #10976, #944, #8133, #8611, #29181, #3293 ),
 .UNSPECIFIED., .F., .F.,
 ( 4, 2, 2, 4 ),
 ( 0.000000000000000000, 0.0003782825618925954618, 0.0005674238428388933553, 0.0007565651237851912488 ),
 .UNSPECIFIED. ) ;
#26597=DIRECTION ( 'NONE',  ( -1.000000000000000000, 0.000000000000000000, 0.000000000000000000 ) ) ;
#26598=CARTESIAN_POINT ( 'NONE',  ( -2.767073886773233848, -0.6621507858625382825, -1.748408842879326075 ) ) ;
#26601=CARTESIAN_POINT ( 'NONE',  ( 107.8717334959377609, -16.22235636681381621, 1.414040860148557677 ) ) ;
#26604=CARTESIAN_POINT ( 'NONE',  ( 20.75046113880689092, -21.62010873700215541, 1.554218361998283227 ) ) ;
#26608=CARTESIAN_POINT ( 'NONE',  ( 107.9476209416900474, -17.31511670722516882, 4.492030933741832044 ) ) ;
#26610=EDGE_LOOP ( 'NONE', ( #10624, #8943, #16482, #30251 ) ) ;
#26620=CARTESIAN_POINT ( 'NONE',  ( 17.39502519979081185, -21.04076415203811479, -1.751145182513948573 ) ) ;
#26621=CARTESIAN_POINT ( 'NONE',  ( 108.0549841752498565, -18.86112056187526775, -3.563976902055589147 ) ) ;
#26622=CARTESIAN_POINT ( 'NONE',  ( 10.63777812034630976, -12.44241537516159113, -1.000000000000000000 ) ) ;
#26629=ORIENTED_EDGE ( 'NONE', *, *, #12012, .F. ) ;
#26631=CARTESIAN_POINT ( 'NONE',  ( -29.73484230743789070, -25.93932300454937945, 11.09540449768827308 ) ) ;
#26638=CARTESIAN_POINT ( 'NONE',  ( 18.73041676179872184, -21.25644754115793233, 1.734286084696329722 ) ) ;
#26645=EDGE_LOOP ( 'NONE', ( #3054, #26942, #18485, #13189, #6438 ) ) ;
#26646=ORIENTED_EDGE ( 'NONE', *, *, #28160, .F. ) ;
#26648=CARTESIAN_POINT ( 'NONE',  ( -1.921189184902823754, -10.44034746380417467, 4.522129901861158707 ) ) ;
#26658=( BOUNDED_SURFACE ( )  B_SPLINE_SURFACE ( 3, 2, ( 
 ( #13595, #3584, #3105 ),
 ( #3434, #8421, #913 ),
 ( #5614, #11091, #23637 ),
 ( #21290, #25998, #26485 ),
 ( #31491, #7932, #5756 ),
 ( #3254, #16274, #758 ),
 ( #28661, #18614, #2959 ),
 ( #13744, #31193, #25838 ),
 ( #28806, #23461, #13116 ),
 ( #10942, #23948, #28507 ) ),
 .UNSPECIFIED., .F., .F., .F. ) 
 B_SPLINE_SURFACE_WITH_KNOTS ( ( 4, 2, 2, 2, 4 ),
 ( 3, 3 ),
 ( 0.003636727685402258142, 0.004103800047000625076, 0.004570872408598991576, 0.005037944770197358077, 0.005505017131795725445 ),
 ( 0.000000000000000000, 1.000000000000000000 ),
 .UNSPECIFIED. ) 
 GEOMETRIC_REPRESENTATION_ITEM ( )  RATIONAL_B_SPLINE_SURFACE ( (
 ( 1.000000000000000000, 0.8449619147701442623, 1.000000000000000000),
 ( 1.000000000000000000, 0.8255905392900690920, 1.000000000000000000),
 ( 1.000000000000000000, 0.8027571906106222288, 1.000000000000000000),
 ( 1.000000000000000000, 0.7529839109803591057, 1.000000000000000000),
 ( 1.000000000000000000, 0.7260803501547112848, 1.000000000000000000),
 ( 1.000000000000000000, 0.6677408092242498316, 1.000000000000000000),
 ( 1.000000000000000000, 0.6373774895460140311, 1.000000000000000000),
 ( 1.000000000000000000, 0.5732936775527678330, 1.000000000000000000),
 ( 1.000000000000000000, 0.5402556527144246612, 1.000000000000000000),
 ( 1.000000000000000000, 0.5090209295198749873, 1.000000000000000000) ) ) 
 REPRESENTATION_ITEM ( '' )  SURFACE ( )  );
#26659=CARTESIAN_POINT ( 'NONE',  ( 0.8407900506754626413, -11.56055812333295130, -4.522129901861164925 ) ) ;
#26662=EDGE_CURVE ( 'NONE', #27553, #20422, #17861, .T. ) ;
#26674=CARTESIAN_POINT ( 'NONE',  ( -48.07500000000000284, -10.96966150227468972, 7.500000000000000000 ) ) ;
#26680=CARTESIAN_POINT ( 'NONE',  ( 0.4783367452032581402, -8.598034230381170318, 1.771412240841123920 ) ) ;
#26686=CARTESIAN_POINT ( 'NONE',  ( 21.04767255914888580, -17.06392231637762436, -1.500000000000848210 ) ) ;
#26705=CARTESIAN_POINT ( 'NONE',  ( 3.544356706772826993, -14.29624599654059303, 5.485967528433933538 ) ) ;
#26728=CARTESIAN_POINT ( 'NONE',  ( 7.151900074888314585, -6.858124901741749824, -0.9999999999999997780 ) ) ;
#26731=EDGE_LOOP ( 'NONE', ( #3123, #7622, #22836, #29491, #19594, #13535, #50, #10110 ) ) ;
#26740=VECTOR ( 'NONE', #16143, 1000.000000000000000 ) ;
#26750=ADVANCED_FACE ( 'NONE', ( #20270 ), #20966, .T. ) ;
#26752=CARTESIAN_POINT ( 'NONE',  ( 25.36291108019387863, -17.54678858634073890, 1.252583955065272425 ) ) ;
#26754=CARTESIAN_POINT ( 'NONE',  ( -4.555723515433391491, -6.511021237588678012, -1.499999999999999556 ) ) ;
#26770=CARTESIAN_POINT ( 'NONE',  ( 18.66634262892177532, -21.55284492811545860, 1.491166157331047293 ) ) ;
#26773=CARTESIAN_POINT ( 'NONE',  ( -50.60000000000000142, -0.5000000000000000000, 1.000000000000000000 ) ) ;
#26780=CARTESIAN_POINT ( 'NONE',  ( -17.45597128428592981, -25.43932300454937234, 11.50000000000000000 ) ) ;
#26784=CARTESIAN_POINT ( 'NONE',  ( -3.790542665135919531, -3.338451600437029931, -1.747101525495873053 ) ) ;
#26787=CARTESIAN_POINT ( 'NONE',  ( 9.360049167874114673, -11.53021799246534584, -1.000000000000000000 ) ) ;
#26795=CARTESIAN_POINT ( 'NONE',  ( -2.962992063741595405, -11.77309494928644185, 1.500000000000000000 ) ) ;
#26798=DIRECTION ( 'NONE',  ( -0.000000000000000000, -0.000000000000000000, 1.000000000000000000 ) ) ;
#26801=CARTESIAN_POINT ( 'NONE',  ( 107.3578191293706396, -16.03232060375378154, -1.799467592163734642 ) ) ;
#26805=B_SPLINE_CURVE_WITH_KNOTS ( 'NONE', 3,
 ( #1811, #3805, #8820, #6955, #14470, #1469 ),
 .UNSPECIFIED., .F., .F.,
 ( 4, 2, 4 ),
 ( -5.641427396388729422E-06, 0.0003847768015433646440, 0.0007751950304831179903 ),
 .UNSPECIFIED. ) ;
#26813=CARTESIAN_POINT ( 'NONE',  ( 25.38273381070351320, -17.54867692718865868, -1.149837904939237321 ) ) ;
#26817=ORIENTED_EDGE ( 'NONE', *, *, #9776, .F. ) ;
#26827=AXIS2_PLACEMENT_3D ( 'NONE', #14886, #27765, #4879 ) ;
#26834=CARTESIAN_POINT ( 'NONE',  ( 107.5605484478042655, -18.96584416766395620, 4.567556099746715503 ) ) ;
#26835=EDGE_CURVE ( 'NONE', #7472, #12927, #21485, .T. ) ;
#26844=CIRCLE ( 'NONE', #23650, 0.5000000000000004441 ) ;
#26853=CARTESIAN_POINT ( 'NONE',  ( 7.362531901230354947, -8.542914936813595261, 1.500000000000000000 ) ) ;
#26858=CARTESIAN_POINT ( 'NONE',  ( 3.163725240263005389, -11.65225984964322947, 1.500000000000000888 ) ) ;
#26859=MECHANICAL_CONTEXT ( 'NONE', #25059, 'mechanical' ) ;
#26870=TOROIDAL_SURFACE ( 'NONE', #21021, 7.144028715714068056, 0.5000000000000000000 ) ;
#26880=ORIENTED_EDGE ( 'NONE', *, *, #22237, .F. ) ;
#26883=CARTESIAN_POINT ( 'NONE',  ( 71.84273455771214856, -21.42499078636276622, -4.522129901861166701 ) ) ;
#26888=CARTESIAN_POINT ( 'NONE',  ( 25.43628654896339114, -17.54453578616444887, -1.025162786324184117 ) ) ;
#26905=ORIENTED_EDGE ( 'NONE', *, *, #27156, .F. ) ;
#26911=CARTESIAN_POINT ( 'NONE',  ( 9.052197806735183150, -0.5587348279125937678, -0.9999999999999997780 ) ) ;
#26919=CARTESIAN_POINT ( 'NONE',  ( 2.281627749324421472, -0.2935656086769634077, -1.757435426329174044 ) ) ;
#26937=CARTESIAN_POINT ( 'NONE',  ( -2.880987360464339009, -0.6119841066606575009, -1.500000000000000222 ) ) ;
#26938=CARTESIAN_POINT ( 'NONE',  ( -32.06740601709051930, -27.93932300454937590, -0.9045955023117255855 ) ) ;
#26942=ORIENTED_EDGE ( 'NONE', *, *, #28056, .T. ) ;
#26944=CARTESIAN_POINT ( 'NONE',  ( 107.4500373638804120, -17.36019379023677089, -4.522129901861164036 ) ) ;
#26951=ORIENTED_EDGE ( 'NONE', *, *, #1091, .F. ) ;
#26964=CARTESIAN_POINT ( 'NONE',  ( -15.09999999999999609, -21.93932300455815820, 1.000000000000000000 ) ) ;
#26965=CARTESIAN_POINT ( 'NONE',  ( 12.29359089006071137, -13.32350401976880327, -1.500000000000554889 ) ) ;
#26967=CARTESIAN_POINT ( 'NONE',  ( 107.5410504431967240, -18.68278515834781928, -4.957602148651905516 ) ) ;
#26972=EDGE_CURVE ( 'NONE', #12444, #12204, #7072, .T. ) ;
#26979=ORIENTED_EDGE ( 'NONE', *, *, #28693, .T. ) ;
#26997=DIRECTION ( 'NONE',  ( -0.000000000000000000, -0.000000000000000000, 1.000000000000000000 ) ) ;
#27010=PLANE ( 'NONE',  #26287 ) ;
#27016=DIRECTION ( 'NONE',  ( -1.000000000000000000, 2.473959037481237219E-13, -0.000000000000000000 ) ) ;
#27018=CARTESIAN_POINT ( 'NONE',  ( 7.637044425071358944, -3.948987408480924888, 1.500000000000286215 ) ) ;
#27020=CARTESIAN_POINT ( 'NONE',  ( 20.07596637266122386, -16.49406355791761314, -1.500000000000000444 ) ) ;
#27023=CARTESIAN_POINT ( 'NONE',  ( 2.040131092124688017, -10.88355153714070944, 1.762033267153191529 ) ) ;
#27028=CARTESIAN_POINT ( 'NONE',  ( 9.172108879787137070, -0.1070445578126106301, -1.318121098349317233 ) ) ;
#27030=CARTESIAN_POINT ( 'NONE',  ( -2.609496843286264411, -0.08904926966055601301, 1.559466048951597905 ) ) ;
#27031=CARTESIAN_POINT ( 'NONE',  ( 24.27681693764188964, -17.38739216501981844, -1.394420419282224710 ) ) ;
#27040=CARTESIAN_POINT ( 'NONE',  ( -2.819379691724354764, -6.927609664243463250, -4.522129901861166701 ) ) ;
#27043=CARTESIAN_POINT ( 'NONE',  ( -31.69096085994287648, -21.93932300455405482, 1.032046942684759827 ) ) ;
#27069=CARTESIAN_POINT ( 'NONE',  ( 3.986046653337826484, -12.21565841940772223, -1.500000000000423217 ) ) ;
#27074=CARTESIAN_POINT ( 'NONE',  ( 108.1288400433390393, -19.92462668933127290, 1.384270303710046335 ) ) ;
#27076=ORIENTED_EDGE ( 'NONE', *, *, #11544, .T. ) ;
#27085=DIRECTION ( 'NONE',  ( 1.000000000000000000, 0.000000000000000000, 0.000000000000000000 ) ) ;
#27086=ADVANCED_FACE ( 'NONE', ( #11019 ), #10319, .T. ) ;
#27089=DIRECTION ( 'NONE',  ( -0.5075624751249148137, -0.8616149568369101397, 0.000000000000000000 ) ) ;
#27093=CARTESIAN_POINT ( 'NONE',  ( 21.34740231350976458, -21.82855858833835327, 1.313840182778293064 ) ) ;
#27105=CARTESIAN_POINT ( 'NONE',  ( -50.60000000000000142, -10.96966150227468972, 7.500000000000000000 ) ) ;
#27106=CARTESIAN_POINT ( 'NONE',  ( -4.497588124534941834, -5.387736868085173825, -1.500000000000000000 ) ) ;
#27111=CARTESIAN_POINT ( 'NONE',  ( -2.880987360464337677, -0.6119841066606549473, 1.499999999999999112 ) ) ;
#27112=CARTESIAN_POINT ( 'NONE',  ( 7.192400642327426041, -7.644771086453554076, -1.500000000000285549 ) ) ;
#27113=CARTESIAN_POINT ( 'NONE',  ( 108.0492966005174367, -18.77922090048372183, -4.828784975709461413 ) ) ;
#27116=B_SPLINE_CURVE_WITH_KNOTS ( 'NONE', 3,
 ( #5546, #1000, #5836, #8211, #26249, #18710, #23399, #25933, #11181, #503, #3367, #10689, #31122, #21389, #23743, #856, #31430, #31596, #8685, #18410, #17014, #16516, #29244, #26728, #4016, #24381, #22222, #1498, #24231, #21873, #21719, #19551, #26911, #9494 ),
 .UNSPECIFIED., .F., .F.,
 ( 4, 2, 2, 2, 2, 2, 2, 2, 2, 2, 2, 2, 2, 2, 2, 2, 4 ),
 ( 4.567156475735417400E-05, 0.003725671012342181808, 0.007405670459927009286, 0.01108566990751183763, 0.01292566963130425441, 0.01476566935509666771, 0.01660566907888907928, 0.01844566880268149259, 0.01936566866457770444, 0.02028566852647391283, 0.02120566838837012469, 0.02212566825026633308, 0.02304566811216254493, 0.02396566797405875332, 0.02580566769785117356, 0.02764566742164359381, 0.02948566714543601752 ),
 .UNSPECIFIED. ) ;
#27129=CARTESIAN_POINT ( 'NONE',  ( 9.350000000000001421, 0.000000000000000000, 1.000000000000000000 ) ) ;
#27130=CARTESIAN_POINT ( 'NONE',  ( 3.094741023239413469, -0.1906005183311293705, -1.397910568869148440 ) ) ;
#27147=ORIENTED_EDGE ( 'NONE', *, *, #31376, .F. ) ;
#27153=CARTESIAN_POINT ( 'NONE',  ( -1.425727661597341989, -5.130997865967109384, -5.485967528433937979 ) ) ;
#27155=CYLINDRICAL_SURFACE ( 'NONE', #20545, 2.099999999999997868 ) ;
#27156=EDGE_CURVE ( 'NONE', #697, #21586, #17899, .T. ) ;
#27171=CARTESIAN_POINT ( 'NONE',  ( 10.51239158225343751, -12.94889321834390472, -1.500000000000000444 ) ) ;
#27173=CARTESIAN_POINT ( 'NONE',  ( 15.92138669867059342, -16.39214949420826528, 1.753532102563923445 ) ) ;
#27183=CARTESIAN_POINT ( 'NONE',  ( 107.8806307222008627, -16.35047421165092985, -1.384330804613826293 ) ) ;
#27186=CARTESIAN_POINT ( 'NONE',  ( 23.15652614122476649, -21.92931078907647802, -1.107159753869481733 ) ) ;
#27188=LINE ( 'NONE', #29369, #12279 ) ;
#27191=DIRECTION ( 'NONE',  ( 1.000000000000000000, 0.000000000000000000, 0.000000000000000000 ) ) ;
#27211=CARTESIAN_POINT ( 'NONE',  ( -31.67864539881508179, -25.93932300454937945, 1.095404497688271528 ) ) ;
#27213=EDGE_LOOP ( 'NONE', ( #12243, #6879, #25539, #17289, #25069 ) ) ;
#27227=CARTESIAN_POINT ( 'NONE',  ( 3.866957346989826405, -11.79825661644774826, -1.500000000000000444 ) ) ;
#27233=CARTESIAN_POINT ( 'NONE',  ( 108.0945118934858158, -19.43030987198200066, -3.536500079605387814 ) ) ;
#27235=EDGE_CURVE ( 'NONE', #3025, #28448, #7649, .T. ) ;
#27236=CARTESIAN_POINT ( 'NONE',  ( 2.948244102837121794, 0.000000000000000000, 1.325449886338921024 ) ) ;
#27242=AXIS2_PLACEMENT_3D ( 'NONE', #7677, #15192, #15343 ) ;
#27246=CARTESIAN_POINT ( 'NONE',  ( -3.175969065750143816, -11.78108755892028015, -1.500000000000000000 ) ) ;
#27254=EDGE_LOOP ( 'NONE', ( #29441, #31031 ) ) ;
#27258=CYLINDRICAL_SURFACE ( 'NONE', #8589, 0.5000000000000008882 ) ;
#27261=ORIENTED_EDGE ( 'NONE', *, *, #22732, .F. ) ;
#27270=AXIS2_PLACEMENT_3D ( 'NONE', #15566, #25782, #20761 ) ;
#27273=CARTESIAN_POINT ( 'NONE',  ( -4.547423194604015784, -6.123025915217619186, -1.500000000000000222 ) ) ;
#27277=CARTESIAN_POINT ( 'NONE',  ( 9.350000000000028066, 5.584097191983464876E-14, -1.000000000000000000 ) ) ;
#27281=CARTESIAN_POINT ( 'NONE',  ( 108.0243158295136254, -18.41950401259834891, -4.472575114496686766 ) ) ;
#27312=EDGE_LOOP ( 'NONE', ( #27890, #28829, #30695, #12637, #27340 ) ) ;
#27315=CARTESIAN_POINT ( 'NONE',  ( 25.52557118915447987, -17.56218954043521663, -1.000000000000000444 ) ) ;
#27323=ADVANCED_FACE ( 'NONE', ( #6662 ), #16852, .T. ) ;
#27326=AXIS2_PLACEMENT_3D ( 'NONE', #22812, #30346, #30195 ) ;
#27328=CARTESIAN_POINT ( 'NONE',  ( 0.004027955751591347049, -11.10248303872634601, -5.485967528433937979 ) ) ;
#27340=ORIENTED_EDGE ( 'NONE', *, *, #4611, .T. ) ;
#27343=CARTESIAN_POINT ( 'NONE',  ( 23.17076521078841367, -21.93622641188920142, -1.056592731017446996 ) ) ;
#27348=( LENGTH_UNIT ( ) NAMED_UNIT ( * ) SI_UNIT ( .MILLI., .METRE. ) );
#27354=CARTESIAN_POINT ( 'NONE',  ( 21.03177542174607240, -17.18603084754166233, 1.753176640694531052 ) ) ;
#27359=CARTESIAN_POINT ( 'NONE',  ( -3.192893893951263884, -11.75153721369459525, 1.499999999999999556 ) ) ;
#27360=AXIS2_PLACEMENT_3D ( 'NONE', #30939, #18215, #26077 ) ;
#27368=EDGE_CURVE ( 'NONE', #28748, #1705, #26844, .T. ) ;
#27370=CARTESIAN_POINT ( 'NONE',  ( -50.60000000000000142, -10.96966150227468972, -1.000000000000000000 ) ) ;
#27376=CARTESIAN_POINT ( 'NONE',  ( -31.63092319849841871, -21.88241439596123072, 1.340913934978400501 ) ) ;
#27382=CONICAL_SURFACE ( 'NONE', #22564, 2.099999999999997868, 1.029744258676653867 ) ;
#27389=ORIENTED_EDGE ( 'NONE', *, *, #10388, .T. ) ;
#27395=CARTESIAN_POINT ( 'NONE',  ( 107.5574910143032099, -18.92149487875213865, -4.691804453562030908 ) ) ;
#27397=FACE_OUTER_BOUND ( 'NONE', #29197, .T. ) ;
#27400=AXIS2_PLACEMENT_3D ( 'NONE', #7299, #15161, #25008 ) ;
#27417=CARTESIAN_POINT ( 'NONE',  ( 6.718506812351674462, -13.33599551843229669, -1.499999999999999112 ) ) ;
#27418=CARTESIAN_POINT ( 'NONE',  ( 0.8407900506755994208, -11.56055812333295307, 4.522129901861157819 ) ) ;
#27436=CARTESIAN_POINT ( 'NONE',  ( 8.273330302600941266, -18.97014676976608882, -1.749556830060739143 ) ) ;
#27438=CIRCLE ( 'NONE', #21050, 5.000000000000000888 ) ;
#27449=AXIS2_PLACEMENT_3D ( 'NONE', #16921, #9548, #19762 ) ;
#27463=CARTESIAN_POINT ( 'NONE',  ( -4.099820753267308326, -5.441111812974985362, 1.745641719294580563 ) ) ;
#27465=CARTESIAN_POINT ( 'NONE',  ( 8.396671913539110577, -0.7629006742128506824, -1.500000000000000000 ) ) ;
#27466=CARTESIAN_POINT ( 'NONE',  ( 108.0280308400905795, -18.47299924072742527, -4.369739108549834050 ) ) ;
#27468=FACE_OUTER_BOUND ( 'NONE', #57, .T. ) ;
#27477=CARTESIAN_POINT ( 'NONE',  ( 0.000000000000000000, 0.000000000000000000, 7.500000000000000000 ) ) ;
#27484=CARTESIAN_POINT ( 'NONE',  ( 2.303688968543995408, -1.057430054352009208, -1.500000000000000666 ) ) ;
#27497=LINE ( 'NONE', #21968, #25098 ) ;
#27499=CARTESIAN_POINT ( 'NONE',  ( -16.85000000000000142, -10.96966150227469505, -11.00000000000000000 ) ) ;
#27506=EDGE_CURVE ( 'NONE', #10544, #31825, #5909, .T. ) ;
#27523=CARTESIAN_POINT ( 'NONE',  ( 14.67795211623746354, -16.02380094600420790, 1.499999999999579892 ) ) ;
#27543=ADVANCED_FACE ( 'NONE', ( #3588 ), #22136, .F. ) ;
#27552=EDGE_CURVE ( 'NONE', #8122, #23895, #6043, .T. ) ;
#27553=VERTEX_POINT ( 'NONE', #24606 ) ;
#27559=CARTESIAN_POINT ( 'NONE',  ( 4.550593937914527487, -12.71036632817956225, 1.757020553911816885 ) ) ;
#27560=ORIENTED_EDGE ( 'NONE', *, *, #1897, .F. ) ;
#27575=CARTESIAN_POINT ( 'NONE',  ( 6.604716885356828548, -13.59583205938461248, -1.500000000000562661 ) ) ;
#27576=CARTESIAN_POINT ( 'NONE',  ( 0.1517578099453105456, -1.375880305419411309, 4.522129901861157819 ) ) ;
#27583=CARTESIAN_POINT ( 'NONE',  ( 24.16865442153403620, -17.43004354390618005, 1.504494863253181602 ) ) ;
#27584=VERTEX_POINT ( 'NONE', #1064 ) ;
#27587=CARTESIAN_POINT ( 'NONE',  ( -31.59999999999999787, -25.43932300454937945, 1.500000000000000000 ) ) ;
#27591=CARTESIAN_POINT ( 'NONE',  ( -3.353510967526656117, -11.46056164226659924, -1.500000000000000000 ) ) ;
#27610=DIRECTION ( 'NONE',  ( -0.000000000000000000, -0.000000000000000000, 1.000000000000000000 ) ) ;
#27616=CARTESIAN_POINT ( 'NONE',  ( 107.5617870620230860, -18.98359792954988379, 4.522129899028605848 ) ) ;
#27620=CARTESIAN_POINT ( 'NONE',  ( 107.6641581766472768, -20.45810077038816743, -1.499999999999999556 ) ) ;
#27623=B_SPLINE_CURVE_WITH_KNOTS ( 'NONE', 3,
 ( #7096, #7261, #11955, #24815 ),
 .UNSPECIFIED., .F., .F.,
 ( 4, 4 ),
 ( -6.746902117092110274E-06, 2.872315617932023530E-05 ),
 .UNSPECIFIED. ) ;
#27629=CARTESIAN_POINT ( 'NONE',  ( 20.49917871223744470, -21.72428526870506005, -1.411325660096713230 ) ) ;
#27632=B_SPLINE_CURVE_WITH_KNOTS ( 'NONE', 3,
 ( #21927, #11912, #4207, #9040, #27106, #27273, #14736, #6723, #16913, #24933, #11566, #19258, #14377, #14229, #21613, #29463, #16759, #24426, #19753, #21764, #9388, #1544, #19599, #17258, #32148, #9220, #29959, #2045, #8889, #24588, #32479, #19449 ),
 .UNSPECIFIED., .F., .F.,
 ( 4, 2, 2, 2, 2, 2, 2, 2, 2, 2, 2, 2, 2, 2, 2, 4 ),
 ( 0.000000000000000000, 0.004348185525199021496, 0.005435231906498774919, 0.006522278287798528341, 0.008696371050398036054, 0.009783417431697791211, 0.01087046381299754637, 0.01195751019429730153, 0.01304455657559705668, 0.01521864933819656700, 0.01630569571949631869, 0.01739274210079607211, 0.02174092762599509621, 0.02608911315119412030, 0.03043729867639314440, 0.03478548420159216503 ),
 .UNSPECIFIED. ) ;
#27642=CARTESIAN_POINT ( 'NONE',  ( -3.038890739117073636, -0.3712649131886727183, 1.487764840819179257 ) ) ;
#27643=CARTESIAN_POINT ( 'NONE',  ( -3.167352811678424196, 3.267420276671043357E-12, 1.051912341319082511 ) ) ;
#27649=CARTESIAN_POINT ( 'NONE',  ( 1.828104818894226380, -1.262475772535087915, 1.500000000000000000 ) ) ;
#27655=CARTESIAN_POINT ( 'NONE',  ( 107.4168514414812279, -16.88233545631868182, -3.542414872600711195 ) ) ;
#27656=CARTESIAN_POINT ( 'NONE',  ( 25.48003164478615190, -17.55790041459374962, 1.000000000000000888 ) ) ;
#27658=ADVANCED_FACE ( 'NONE', ( #16425 ), #26870, .T. ) ;
#27660=DIRECTION ( 'NONE',  ( 0.000000000000000000, -1.000000000000000000, 0.000000000000000000 ) ) ;
#27672=( NAMED_UNIT ( * ) PLANE_ANGLE_UNIT ( ) SI_UNIT ( $, .RADIAN. ) );
#27673=CARTESIAN_POINT ( 'NONE',  ( 107.4763378844003086, -17.74173259612938480, 5.018187998315496223 ) ) ;
#27675=CARTESIAN_POINT ( 'NONE',  ( 19.76534894311605228, -16.89703626480067555, 1.499999999996504796 ) ) ;
#27677=CARTESIAN_POINT ( 'NONE',  ( -0.1366093623685602776, -14.96249823008941604, -1.499999999999999556 ) ) ;
#27693=DIRECTION ( 'NONE',  ( 1.000000000000000000, -0.000000000000000000, 0.000000000000000000 ) ) ;
#27697=CARTESIAN_POINT ( 'NONE',  ( 23.00622743561894623, -21.91302709721439967, 1.171678142437898584 ) ) ;
#27703=CARTESIAN_POINT ( 'NONE',  ( 107.6641948605100083, -20.45809826282308208, 1.500000000000000000 ) ) ;
#27704=CARTESIAN_POINT ( 'NONE',  ( 21.03177542174608661, -17.18603084754167298, 1.753176640694532162 ) ) ;
#27707=CARTESIAN_POINT ( 'NONE',  ( 21.41577794885431274, -21.75491960302827366, 1.449133755489594000 ) ) ;
#27712=EDGE_CURVE ( 'NONE', #30308, #22652, #32235, .T. ) ;
#27722=CARTESIAN_POINT ( 'NONE',  ( 5.978127801841131017, -13.24614298058319051, 0.9788672205888330202 ) ) ;
#27729=ADVANCED_FACE ( 'NONE', ( #32076, #30087 ), #32421, .T. ) ;
#27731=CARTESIAN_POINT ( 'NONE',  ( 23.72064572293002982, -17.26593119145053734, 1.418862781619489644 ) ) ;
#27741=CARTESIAN_POINT ( 'NONE',  ( -3.423542882029046996, -10.69121096831242390, -1.500000000000000444 ) ) ;
#27745=ORIENTED_EDGE ( 'NONE', *, *, #4119, .F. ) ;
#27751=ORIENTED_EDGE ( 'NONE', *, *, #22437, .T. ) ;
#27752=VECTOR ( 'NONE', #21806, 999.9999999999998863 ) ;
#27759=CARTESIAN_POINT ( 'NONE',  ( -3.370691070153704949, -1.614088942876946264, -1.500000000000000000 ) ) ;
#27765=DIRECTION ( 'NONE',  ( -1.000000000000000000, 6.938893903907221278E-15, -0.000000000000000000 ) ) ;
#27766=CARTESIAN_POINT ( 'NONE',  ( 13.13178786250159469, -17.31629153505179275, 4.522129901861156931 ) ) ;
#27767=FACE_OUTER_BOUND ( 'NONE', #1296, .T. ) ;
#27769=CARTESIAN_POINT ( 'NONE',  ( 9.437548970008961646, 0.1642588933130686712, -1.000000000000000000 ) ) ;
#27775=CIRCLE ( 'NONE', #25122, 0.5000000000000008882 ) ;
#27785=CARTESIAN_POINT ( 'NONE',  ( -50.60000000000000142, -10.96966150227468972, 6.999999999999999112 ) ) ;
#27796=CARTESIAN_POINT ( 'NONE',  ( 23.05362332218847143, -16.83301128369467037, 1.000000000000000000 ) ) ;
#27799=DIRECTION ( 'NONE',  ( 0.000000000000000000, 0.000000000000000000, -1.000000000000000000 ) ) ;
#27812=CARTESIAN_POINT ( 'NONE',  ( 1.404908439943009846, -10.20361334857307511, -1.764679167141864458 ) ) ;
#27813=EDGE_CURVE ( 'NONE', #1202, #24580, #29787, .T. ) ;
#27816=AXIS2_PLACEMENT_3D ( 'NONE', #31718, #21326, #10980 ) ;
#27818=CARTESIAN_POINT ( 'NONE',  ( 107.9462823452559945, -17.29584125157618146, -3.322807143007931785 ) ) ;
#27819=CARTESIAN_POINT ( 'NONE',  ( 25.24493059864584765, -17.53551310887478465, 1.328338028043089203 ) ) ;
#27832=AXIS2_PLACEMENT_3D ( 'NONE', #8921, #11275, #28830 ) ;
#27839=CARTESIAN_POINT ( 'NONE',  ( 10.87895964298158624, -15.23742357220648636, 1.754278677543597231 ) ) ;
#27842=CARTESIAN_POINT ( 'NONE',  ( 43.89586892125429074, -24.33975351995231051, -0.9788672205760856615 ) ) ;
#27845=CARTESIAN_POINT ( 'NONE',  ( -0.9905328349288848866, -13.96290196142417628, 1.744688977348453740 ) ) ;
#27853=CIRCLE ( 'NONE', #1682, 0.5000000000000004441 ) ;
#27858=CARTESIAN_POINT ( 'NONE',  ( 0.000000000000000000, 0.000000000000000000, 1.500000000000000000 ) ) ;
#27865=LINE ( 'NONE', #2127, #16595 ) ;
#27866=DIRECTION ( 'NONE',  ( 0.9816271834476639757, 0.000000000000000000, 0.1908089953765452762 ) ) ;
#27872=ORIENTED_EDGE ( 'NONE', *, *, #16190, .T. ) ;
#27883=CARTESIAN_POINT ( 'NONE',  ( 3.431351535095991334, -11.99437772339920016, 1.758550686115804895 ) ) ;
#27887=CARTESIAN_POINT ( 'NONE',  ( 21.89609018930700302, -21.78725138646900561, 1.499999999999999778 ) ) ;
#27890=ORIENTED_EDGE ( 'NONE', *, *, #28056, .F. ) ;
#27908=CARTESIAN_POINT ( 'NONE',  ( 18.53099130238707559, -16.42958907273965607, -1.499999999999999778 ) ) ;
#27909=CARTESIAN_POINT ( 'NONE',  ( 107.5617944031221640, -18.98359742639815551, 4.522129901861158707 ) ) ;
#27924=CARTESIAN_POINT ( 'NONE',  ( 5.492685119413638795, -18.11000744898911208, -1.500000000000157430 ) ) ;
#27929=VECTOR ( 'NONE', #13423, 999.9999999999998863 ) ;
#27947=CARTESIAN_POINT ( 'NONE',  ( 111.3844470440328251, -20.20075132222358505, 1.500000000000000000 ) ) ;
#27950=CARTESIAN_POINT ( 'NONE',  ( 107.6641948605228123, -20.45809826282219746, -1.499999999999999556 ) ) ;
#27958=CARTESIAN_POINT ( 'NONE',  ( -0.05283608181216257332, -14.78963767087145698, 1.745421384833004019 ) ) ;
#27959=CARTESIAN_POINT ( 'NONE',  ( 6.976285486575450001, -4.435383624113830692, -1.500000000000000000 ) ) ;
#27961=ORIENTED_EDGE ( 'NONE', *, *, #3881, .T. ) ;
#27965=CARTESIAN_POINT ( 'NONE',  ( 107.3476768466457401, -15.88628154573096651, 1.500000000000000000 ) ) ;
#27980=FACE_OUTER_BOUND ( 'NONE', #29169, .T. ) ;
#27985=CARTESIAN_POINT ( 'NONE',  ( 12.41789292056455274, -13.38018177111670504, 1.000000000000000000 ) ) ;
#27986=EDGE_CURVE ( 'NONE', #11874, #5578, #12239, .T. ) ;
#27989=ORIENTED_EDGE ( 'NONE', *, *, #201, .F. ) ;
#27996=ADVANCED_FACE ( 'NONE', ( #13304 ), #26385, .T. ) ;
#28001=CARTESIAN_POINT ( 'NONE',  ( 2.281627749324420140, -0.2935656086769634077, -1.757435426329174710 ) ) ;
#28002=CARTESIAN_POINT ( 'NONE',  ( 21.70556107702375570, -21.76510136446086818, -1.556570398780113829 ) ) ;
#28009=CARTESIAN_POINT ( 'NONE',  ( 25.14437127914493075, -17.52581659214492404, 1.374992938514359997 ) ) ;
#28010=CARTESIAN_POINT ( 'NONE',  ( 18.62789956200952446, -21.71817389963752021, 0.9788672205877712029 ) ) ;
#28011=CARTESIAN_POINT ( 'NONE',  ( 3.541509388326462116, -13.88765124358084968, 4.522129901861156931 ) ) ;
#28012=B_SPLINE_CURVE_WITH_KNOTS ( 'NONE', 3,
 ( #15313, #28190, #20180, #20528, #12300, #10120, #17488, #17649, #7298, #120, #25181, #7639, #12145, #22344, #9814, #2299, #12489, #32901, #22698, #2473, #5292, #28040, #22515, #22845, #20032, #25366, #33047, #7448 ),
 .UNSPECIFIED., .F., .F.,
 ( 4, 3, 3, 3, 3, 3, 3, 3, 3, 4 ),
 ( 3.469446951953614189E-18, 0.0002206598333029125968, 0.0003690260377615042645, 0.0004687386537139015975, 0.0005359204132811800627, 0.0005814601065133845987, 0.0006257480493229339476, 0.0006439039612560342211, 0.0006584914725869980530, 0.0006666056854015675517 ),
 .UNSPECIFIED. ) ;
#28013=CARTESIAN_POINT ( 'NONE',  ( -15.59081359172382975, -25.43932300454937945, 1.404595502311726696 ) ) ;
#28029=CARTESIAN_POINT ( 'NONE',  ( -2.786590204610738031, -5.640011313469492471, -4.522129901861166701 ) ) ;
#28031=ORIENTED_EDGE ( 'NONE', *, *, #27235, .T. ) ;
#28032=CARTESIAN_POINT ( 'NONE',  ( -2.762703010982404006, -11.69547828613897700, 1.743724233132518675 ) ) ;
#28040=CARTESIAN_POINT ( 'NONE',  ( 21.37407243444119942, -21.76038176774102695, -1.427857905595965926 ) ) ;
#28052=CARTESIAN_POINT ( 'NONE',  ( 22.51665287054298403, -21.85882206146554552, 1.289857144952121448 ) ) ;
#28056=EDGE_CURVE ( 'NONE', #4832, #17041, #16817, .T. ) ;
#28061=DIRECTION ( 'NONE',  ( -0.000000000000000000, 1.000000000000000000, -0.000000000000000000 ) ) ;
#28064=CARTESIAN_POINT ( 'NONE',  ( 22.00639167669143603, -21.80013755708273848, 1.500000000000000000 ) ) ;
#28069=CARTESIAN_POINT ( 'NONE',  ( -28.35000000000000497, -10.96966150227469505, -1.500000000000000000 ) ) ;
#28084=CARTESIAN_POINT ( 'NONE',  ( 24.37505892580042755, -17.33881490880317244, 1.312584468235632462 ) ) ;
#28107=CARTESIAN_POINT ( 'NONE',  ( -4.365512850963738423, -6.230587388684557304, -1.500000000000000000 ) ) ;
#28115=CARTESIAN_POINT ( 'NONE',  ( 0.8407900506754618641, -11.56055812333405441, 4.522129901861156931 ) ) ;
#28116=CARTESIAN_POINT ( 'NONE',  ( -0.3079966392002160824, -15.09887389677487057, 1.500000000000000444 ) ) ;
#28119=CARTESIAN_POINT ( 'NONE',  ( 108.0284341522745137, -18.47880683584480366, -4.354933216522902661 ) ) ;
#28129=CARTESIAN_POINT ( 'NONE',  ( 107.9823351630856934, -17.81499285951132094, 4.403864951703802433 ) ) ;
#28135=CARTESIAN_POINT ( 'NONE',  ( 3.541509388326463004, -13.88765124358303993, -4.522129901861164925 ) ) ;
#28139=ORIENTED_EDGE ( 'NONE', *, *, #16016, .T. ) ;
#28140=CARTESIAN_POINT ( 'NONE',  ( -2.863349216192397240, 0.2791979387067812235, 0.7890172491793814302 ) ) ;
#28144=EDGE_LOOP ( 'NONE', ( #33038, #20176, #2866, #29966 ) ) ;
#28150=CARTESIAN_POINT ( 'NONE',  ( 0.2695511591073790347, -5.141785308971643431, -1.768807166514833051 ) ) ;
#28152=CARTESIAN_POINT ( 'NONE',  ( 22.51665287054355957, -21.85882206146509432, -1.289857144951130907 ) ) ;
#28153=CARTESIAN_POINT ( 'NONE',  ( 17.02282544802299213, -15.06900748016021652, -1.500000000000277334 ) ) ;
#28157=CARTESIAN_POINT ( 'NONE',  ( 0.8195958019639205672, -4.591973786415240788, 1.500000000000000000 ) ) ;
#28160=EDGE_CURVE ( 'NONE', #18680, #6546, #1058, .T. ) ;
#28163=DIRECTION ( 'NONE',  ( 1.000000000000000000, 0.000000000000000000, 0.000000000000000000 ) ) ;
#28170=LINE ( 'NONE', #22978, #15692 ) ;
#28182=CARTESIAN_POINT ( 'NONE',  ( 0.9573829800795973233, -15.55580343830457579, 1.746220095277639661 ) ) ;
#28190=CARTESIAN_POINT ( 'NONE',  ( 21.93333526462830108, -21.79160260970720131, -1.500000000000028644 ) ) ;
#28199=CARTESIAN_POINT ( 'NONE',  ( 23.21956321516963229, -21.93898040685625972, 1.019910856439967706 ) ) ;
#28202=FACE_OUTER_BOUND ( 'NONE', #8727, .T. ) ;
#28208=CARTESIAN_POINT ( 'NONE',  ( 107.9802527803231129, -17.78500706576168611, -4.325704939595124365 ) ) ;
#28209=CARTESIAN_POINT ( 'NONE',  ( 19.46384663048941377, -15.80031286559597703, 1.500000000000000000 ) ) ;
#28214=VERTEX_POINT ( 'NONE', #9948 ) ;
#28215=CARTESIAN_POINT ( 'NONE',  ( 1.997966851997896143, -1.624780761253489691, 1.499999999999999556 ) ) ;
#28221=ORIENTED_EDGE ( 'NONE', *, *, #16236, .T. ) ;
#28226=CARTESIAN_POINT ( 'NONE',  ( 19.74803318911342487, -17.01893862700759641, -1.753250791794231933 ) ) ;
#28256=DIRECTION ( 'NONE',  ( 1.000000000000000000, 0.000000000000000000, 0.000000000000000000 ) ) ;
#28263=EDGE_LOOP ( 'NONE', ( #1931, #25276, #22945, #24595, #21306, #30927 ) ) ;
#28265=CARTESIAN_POINT ( 'NONE',  ( 0.1517578099452172036, -1.375880305419571625, 4.522129901861156931 ) ) ;
#28267=CARTESIAN_POINT ( 'NONE',  ( -4.499052284343287411, -5.402383032670722507, 1.499999999999999556 ) ) ;
#28270=ORIENTED_EDGE ( 'NONE', *, *, #327, .F. ) ;
#28271=CARTESIAN_POINT ( 'NONE',  ( 25.52557118915447987, -17.56218954043521663, 1.000000000000000000 ) ) ;
#28275=AXIS2_PLACEMENT_3D ( 'NONE', #8912, #1257, #16600 ) ;
#28279=CARTESIAN_POINT ( 'NONE',  ( -52.69999999999999574, -10.96966150227468972, 0.9999999999999991118 ) ) ;
#28284=CARTESIAN_POINT ( 'NONE',  ( -53.12500000000000000, -10.96966150227468972, 7.500000000000000000 ) ) ;
#28287=CARTESIAN_POINT ( 'NONE',  ( 13.56547938923340624, -13.86701005029668288, 1.000000000000000222 ) ) ;
#28288=CARTESIAN_POINT ( 'NONE',  ( 107.9692545707511471, -17.62663558376400985, 4.957402666611876008 ) ) ;
#28290=EDGE_CURVE ( 'NONE', #28620, #17825, #28170, .T. ) ;
#28303=CARTESIAN_POINT ( 'NONE',  ( 16.80274661516410006, -16.53680364986711737, -1.500000000000000000 ) ) ;
#28308=CARTESIAN_POINT ( 'NONE',  ( 22.04243029793069297, -21.80478118307112823, -1.499729010652245620 ) ) ;
#28309=CARTESIAN_POINT ( 'NONE',  ( 108.0821972398987327, -20.20655521172199798, -1.448620529800456191 ) ) ;
#28311=CARTESIAN_POINT ( 'NONE',  ( 107.9766672148941495, -17.73337581556108233, 4.219849370640194053 ) ) ;
#28314=CARTESIAN_POINT ( 'NONE',  ( 3.065837323883517929, -11.21675834388424065, 1.499999999999999778 ) ) ;
#28335=CARTESIAN_POINT ( 'NONE',  ( -15.10000000000019327, -21.93932300455815820, 1.500000000001016520 ) ) ;
#28337=CARTESIAN_POINT ( 'NONE',  ( -3.370691070153704949, -1.614088942876946264, -1.499999999999999556 ) ) ;
#28340=EDGE_CURVE ( 'NONE', #21513, #18408, #17482, .T. ) ;
#28341=CARTESIAN_POINT ( 'NONE',  ( 17.39502519978889694, -21.04076415203780925, 1.751145182513948351 ) ) ;
#28342=ORIENTED_EDGE ( 'NONE', *, *, #14349, .F. ) ;
#28356=( BOUNDED_SURFACE ( )  B_SPLINE_SURFACE ( 3, 2, ( 
 ( #14929, #32371, #25138 ),
 ( #9430, #30344, #19647 ),
 ( #29841, #14621, #1941 ),
 ( #12114, #19804, #15115 ) ),
 .UNSPECIFIED., .F., .F., .F. ) 
 B_SPLINE_SURFACE_WITH_KNOTS ( ( 4, 4 ),
 ( 3, 3 ),
 ( 0.003792662576232288477, 0.007223425640200679260 ),
 ( 0.000000000000000000, 1.000000000000000000 ),
 .UNSPECIFIED. ) 
 GEOMETRIC_REPRESENTATION_ITEM ( )  RATIONAL_B_SPLINE_SURFACE ( (
 ( 1.000000000000000000, 0.7067603058644416070, 1.000000000000000000),
 ( 1.000000000000000000, 0.7067606020011355517, 1.000000000000000000),
 ( 1.000000000000000000, 0.7067612639882813186, 1.000000000000000000),
 ( 1.000000000000000000, 0.7067623105831687402, 1.000000000000000000) ) ) 
 REPRESENTATION_ITEM ( '' )  SURFACE ( )  );
#28360=CARTESIAN_POINT ( 'NONE',  ( -14.85000000000000142, -10.96966150227469328, 4.500000000000000888 ) ) ;
#28364=CARTESIAN_POINT ( 'NONE',  ( 24.40261005161485386, -17.41690598104249688, 1.428369430449265787 ) ) ;
#28376=CARTESIAN_POINT ( 'NONE',  ( 17.02282544784813112, -15.06900748075983998, 1.000000000000000000 ) ) ;
#28392=CARTESIAN_POINT ( 'NONE',  ( 107.3476768466458253, -15.88628154573095586, -1.500000000000000000 ) ) ;
#28400=CARTESIAN_POINT ( 'NONE',  ( 0.8032528114568877609, -4.297275870435987244, 0.9788672205888330202 ) ) ;
#28413=LINE ( 'NONE', #8663, #30665 ) ;
#28416=AXIS2_PLACEMENT_3D ( 'NONE', #20996, #26166, #3119 ) ;
#28435=ORIENTED_EDGE ( 'NONE', *, *, #7132, .T. ) ;
#28440=VERTEX_POINT ( 'NONE', #27129 ) ;
#28442=CYLINDRICAL_SURFACE ( 'NONE', #17647, 10.96966150227469328 ) ;
#28444=CARTESIAN_POINT ( 'NONE',  ( 8.571721676197487483, -11.50721971753373118, 1.500000000000000222 ) ) ;
#28448=VERTEX_POINT ( 'NONE', #1740 ) ;
#28451=CARTESIAN_POINT ( 'NONE',  ( 0.2699473030965058307, -15.55366081788063681, 1.500000000000000444 ) ) ;
#28460=AXIS2_PLACEMENT_3D ( 'NONE', #20582, #13045, #3032 ) ;
#28468=CARTESIAN_POINT ( 'NONE',  ( -2.745055912661924058, -0.1926413909297530480, -1.404235515124709455 ) ) ;
#28469=ORIENTED_EDGE ( 'NONE', *, *, #10496, .F. ) ;
#28471=CARTESIAN_POINT ( 'NONE',  ( -48.07500000000000284, -10.96966150227468972, 7.500000000000000000 ) ) ;
#28476=CYLINDRICAL_SURFACE ( 'NONE', #11733, 0.5000000000000004441 ) ;
#28477=CARTESIAN_POINT ( 'NONE',  ( 0.9306419922191571104, -8.901511148765195003, -0.9788672205888330202 ) ) ;
#28479=CARTESIAN_POINT ( 'NONE',  ( 107.4707837513502255, -17.66103516835562459, 4.957671652933026252 ) ) ;
#28480=VERTEX_POINT ( 'NONE', #13911 ) ;
#28483=ORIENTED_EDGE ( 'NONE', *, *, #3504, .F. ) ;
#28484=FACE_OUTER_BOUND ( 'NONE', #27312, .T. ) ;
#28507=CARTESIAN_POINT ( 'NONE',  ( 3.750263394063812150, -2.684783474401000736E-05, 0.9948185799301203502 ) ) ;
#28519=ADVANCED_FACE ( 'NONE', ( #27980 ), #22942, .T. ) ;
#28521=CARTESIAN_POINT ( 'NONE',  ( 17.39502519979085449, -21.04076415203812189, -1.751145182513949239 ) ) ;
#28532=CARTESIAN_POINT ( 'NONE',  ( -2.373270979209490594, -12.30283429957249552, 1.743844681977045452 ) ) ;
#28533=ORIENTED_EDGE ( 'NONE', *, *, #7015, .F. ) ;
#28556=AXIS2_PLACEMENT_3D ( 'NONE', #11466, #14275, #4259 ) ;
#28558=CARTESIAN_POINT ( 'NONE',  ( 107.9095624609269777, -17.54879161072074112, 4.428303208956443804 ) ) ;
#28560=CARTESIAN_POINT ( 'NONE',  ( 23.15368348411500676, -16.86203458189232762, 1.500000000000277778 ) ) ;
#28574=DIRECTION ( 'NONE',  ( 0.000000000000000000, -0.000000000000000000, -1.000000000000000000 ) ) ;
#28582=ORIENTED_EDGE ( 'NONE', *, *, #20160, .F. ) ;
#28584=CARTESIAN_POINT ( 'NONE',  ( 24.29160796521618337, -17.33532173511207830, -1.337584091082468118 ) ) ;
#28586=CLOSED_SHELL ( 'NONE', ( #18220, #22225, #26750, #21740, #21666, #30072, #13222, #32112, #13140, #24675, #18166, #30590, #8028, #4637, #9796, #13288, #20909, #1707, #19477, #16059, #19951, #7418, #19784, #21623, #30512, #3551, #27543, #26439, #1, #7253, #1685, #3531, #6269, #2444, #30644, #16014, #985, #31795, #8554, #20194, #28519, #12819, #2218, #17373, #27729, #12231, #23443, #13857, #20737, #31827, #30683, #6720, #15258, #8944, #11463, #30429, #4156, #19205, #26473, #9920, #17987, #9889, #22367, #15089, #19430, #884, #31028, #30482, #27323, #24618, #16335, #14905, #33052, #26411, #26217, #27996, #32543, #1869, #11937, #6881, #28770, #18634, #26088, #7856, #22128, #23468, #32013, #27658, #18998, #2328, #20994, #3068, #18671, #3445, #27086, #30357, #15149, #10159, #24192, #9688, #14715, #19284, #18179, #17995, #17648, #29928, #22444, #13237, #6611, #30156, #13834, #32019, #19438 ) ) ;
#28592=CARTESIAN_POINT ( 'NONE',  ( 2.632061376486628301, -0.5000000000000000000, -1.500000000000000000 ) ) ;
#28606=ORIENTED_EDGE ( 'NONE', *, *, #6127, .T. ) ;
#28607=CARTESIAN_POINT ( 'NONE',  ( -15.02135460118491217, -21.93013659628234890, 1.095404497688272638 ) ) ;
#28609=CARTESIAN_POINT ( 'NONE',  ( 6.910673634762098061, -8.774004714863517407, 1.499999999999999778 ) ) ;
#28615=CARTESIAN_POINT ( 'NONE',  ( -1.201782691452277785, -13.92888619398943639, 1.500000000000158984 ) ) ;
#28620=VERTEX_POINT ( 'NONE', #2416 ) ;
#28622=CARTESIAN_POINT ( 'NONE',  ( 107.3477133433398336, -15.88627905081428615, 1.500000000000000000 ) ) ;
#28628=CARTESIAN_POINT ( 'NONE',  ( -2.626726202933311161, 0.09953226261466606439, -1.366272513173331982 ) ) ;
#28630=CARTESIAN_POINT ( 'NONE',  ( -28.85000000000000497, -10.96966150227469505, 4.500000000000000888 ) ) ;
#28636=CARTESIAN_POINT ( 'NONE',  ( 107.9805524956831846, -17.78932289238704811, 4.337499095951103278 ) ) ;
#28640=DIRECTION ( 'NONE',  ( -0.000000000000000000, -0.000000000000000000, -1.000000000000000000 ) ) ;
#28641=ORIENTED_EDGE ( 'NONE', *, *, #9776, .T. ) ;
#28642=CYLINDRICAL_SURFACE ( 'NONE', #19347, 0.5000000000000004441 ) ;
#28648=FACE_OUTER_BOUND ( 'NONE', #31297, .T. ) ;
#28652=CARTESIAN_POINT ( 'NONE',  ( 21.34414429286656656, -21.72097900651801083, -1.443623072030687515 ) ) ;
#28653=CARTESIAN_POINT ( 'NONE',  ( 23.01404055077311028, -17.34213939868426735, -1.500000000000000666 ) ) ;
#28661=CARTESIAN_POINT ( 'NONE',  ( 3.048228882235579196, 0.5389963249801693612, 1.289664751349846261 ) ) ;
#28678=ORIENTED_EDGE ( 'NONE', *, *, #10582, .F. ) ;
#28689=DIRECTION ( 'NONE',  ( -0.000000000000000000, -0.000000000000000000, 1.000000000000000000 ) ) ;
#28693=EDGE_CURVE ( 'NONE', #29863, #5623, #13036, .T. ) ;
#28698=CARTESIAN_POINT ( 'NONE',  ( 24.39957246288403070, -17.41407024517256730, 1.423208249768635358 ) ) ;
#28708=CARTESIAN_POINT ( 'NONE',  ( 9.126991455998574310, -11.32614230997930882, 1.499999999999998668 ) ) ;
#28712=CARTESIAN_POINT ( 'NONE',  ( 0.8185896255502229657, -4.595692320205778891, 1.500000000000000000 ) ) ;
#28728=ORIENTED_EDGE ( 'NONE', *, *, #1288, .F. ) ;
#28747=DIRECTION ( 'NONE',  ( 0.1908089953765452762, 0.000000000000000000, 0.9816271834476639757 ) ) ;
#28748=VERTEX_POINT ( 'NONE', #18092 ) ;
#28755=CARTESIAN_POINT ( 'NONE',  ( 20.07596637266183848, -16.49406355791779077, 1.500000000000000222 ) ) ;
#28756=FACE_OUTER_BOUND ( 'NONE', #11950, .T. ) ;
#28758=ORIENTED_EDGE ( 'NONE', *, *, #30491, .T. ) ;
#28770=ADVANCED_FACE ( 'NONE', ( #18262 ), #28476, .T. ) ;
#28772=CARTESIAN_POINT ( 'NONE',  ( -2.760161469795139322, -0.06813755667441036279, -1.269913365998981192 ) ) ;
#28773=CARTESIAN_POINT ( 'NONE',  ( 72.25703127509153489, -22.87839253411022611, 1.500000000000000000 ) ) ;
#28780=CARTESIAN_POINT ( 'NONE',  ( 107.4581749826926398, -17.47794492952237277, 4.757811978365556804 ) ) ;
#28787=ORIENTED_EDGE ( 'NONE', *, *, #22706, .F. ) ;
#28793=CARTESIAN_POINT ( 'NONE',  ( -5.427698642335591239E-12, -21.93932300456189566, 1.500000000000000000 ) ) ;
#28794=CARTESIAN_POINT ( 'NONE',  ( 11.84010260670268089, -19.96226796878934451, -1.750548469652316586 ) ) ;
#28795=DIRECTION ( 'NONE',  ( 0.1908089953765452484, 0.000000000000000000, 0.9816271834476638647 ) ) ;
#28796=DIRECTION ( 'NONE',  ( -0.000000000000000000, 0.000000000000000000, 1.000000000000000000 ) ) ;
#28805=CARTESIAN_POINT ( 'NONE',  ( -48.50000000000000000, -10.96966150227468972, 0.9999999999999991118 ) ) ;
#28806=CARTESIAN_POINT ( 'NONE',  ( 3.329122376115755344, 0.6654791810447507894, 0.9318852528021189796 ) ) ;
#28808=( BOUNDED_SURFACE ( )  B_SPLINE_SURFACE ( 3, 2, ( 
 ( #28983, #16268, #16576 ),
 ( #16085, #26317, #21283 ),
 ( #31187, #8268, #26139 ),
 ( #6082, #23627, #3428 ),
 ( #21137, #31336, #13588 ),
 ( #23794, #906, #26481 ),
 ( #13740, #23942, #1051 ),
 ( #11243, #21449, #3907 ),
 ( #14085, #1906, #11920 ),
 ( #22429, #9395, #32645 ),
 ( #32486, #14742, #14236 ),
 ( #12079, #24432, #29469 ),
 ( #24940, #7056, #9724 ),
 ( #17423, #24785, #29649 ),
 ( #12225, #21770, #6730 ),
 ( #4567, #24284, #4213 ),
 ( #19606, #1550, #29804 ),
 ( #30160, #22123, #32335 ),
 ( #1399, #32154, #6878 ),
 ( #4398, #17067, #9546 ),
 ( #2052, #4069, #22275 ),
 ( #16919, #1721, #19953 ),
 ( #11730, #21934, #26967 ),
 ( #7233, #27113, #31979 ),
 ( #27281, #9046, #14582 ),
 ( #6568, #11572, #9228 ),
 ( #24594, #19760, #19456 ),
 ( #29965, #14383, #17268 ),
 ( #27466, #19265, #16767 ),
 ( #12722, #17928, #32828 ),
 ( #28119, #20611, #32982 ),
 ( #12572, #18078, #25094 ),
 ( #10218, #13073, #23273 ),
 ( #22924, #4721, #7737 ),
 ( #9901, #20440, #30307 ),
 ( #2711, #14891, #7382 ),
 ( #17570, #5218, #32 ),
 ( #5065, #30463, #22617 ) ),
 .UNSPECIFIED., .F., .F., .F. ) 
 B_SPLINE_SURFACE_WITH_KNOTS ( ( 4, 2, 2, 2, 2, 2, 2, 2, 2, 2, 2, 2, 2, 2, 2, 2, 2, 2, 4 ),
 ( 3, 3 ),
 ( 0.007230792593457298703, 0.007246581719258846262, 0.007262370845060393820, 0.007270265407961168033, 0.007278159970861941379, 0.007293949096663488937, 0.007357105599869678304, 0.007483418606282057906, 0.007609731612694438374, 0.007736044619106817975, 0.007862357625519197576, 0.007988670631931578045, 0.008114983638343956779, 0.008178140141550147013, 0.008193929267351695439, 0.008209718393153242130, 0.008217612956054016343, 0.008225507518954788821, 0.008241296644756337247 ),
 ( 0.000000000000000000, 1.000000000000000000 ),
 .UNSPECIFIED. ) 
 GEOMETRIC_REPRESENTATION_ITEM ( )  RATIONAL_B_SPLINE_SURFACE ( (
 ( 1.000000000000000000, 0.7074680672122112268, 1.000000000000000000),
 ( 1.000000000000000000, 0.7074680692382261382, 1.000000000000000000),
 ( 1.000000000000000000, 0.7074680712595373677, 1.000000000000000000),
 ( 1.000000000000000000, 0.7074680752927113847, 1.000000000000000000),
 ( 1.000000000000000000, 0.7074685410474966796, 1.000000000000000000),
 ( 1.000000000000000000, 0.7074678484437120218, 1.000000000000000000),
 ( 1.000000000000000000, 0.7074669202766126208, 1.000000000000000000),
 ( 1.000000000000000000, 0.7074656694464243056, 1.000000000000000000),
 ( 1.000000000000000000, 0.7074650308517693720, 1.000000000000000000),
 ( 1.000000000000000000, 0.7074630745461631953, 1.000000000000000000),
 ( 1.000000000000000000, 0.7074617163714869150, 1.000000000000000000),
 ( 1.000000000000000000, 0.7074546413305010661, 1.000000000000000000),
 ( 1.000000000000000000, 0.7074480833215146536, 1.000000000000000000),
 ( 1.000000000000000000, 0.7074249281477825724, 1.000000000000000000),
 ( 1.000000000000000000, 0.7074047634757077985, 1.000000000000000000),
 ( 1.000000000000000000, 0.7073503653998111096, 1.000000000000000000),
 ( 1.000000000000000000, 0.7073152363876467064, 1.000000000000000000),
 ( 1.000000000000000000, 0.7072250595811295781, 1.000000000000000000),
 ( 1.000000000000000000, 0.7071666794510108600, 1.000000000000000000),
 ( 1.000000000000000000, 0.7070478450249763069, 1.000000000000000000),
 ( 1.000000000000000000, 0.7069901110841356751, 1.000000000000000000),
 ( 1.000000000000000000, 0.7068987577186105487, 1.000000000000000000),
 ( 1.000000000000000000, 0.7068634512106897194, 1.000000000000000000),
 ( 1.000000000000000000, 0.7068087972553998011, 1.000000000000000000),
 ( 1.000000000000000000, 0.7067884384462148617, 1.000000000000000000),
 ( 1.000000000000000000, 0.7067650571034519436, 1.000000000000000000),
 ( 1.000000000000000000, 0.7067584107639131030, 1.000000000000000000),
 ( 1.000000000000000000, 0.7067512283872569023, 1.000000000000000000),
 ( 1.000000000000000000, 0.7067498488587909966, 1.000000000000000000),
 ( 1.000000000000000000, 0.7067471983191341289, 1.000000000000000000),
 ( 1.000000000000000000, 0.7067453388308237994, 1.000000000000000000),
 ( 1.000000000000000000, 0.7067443930682688613, 1.000000000000000000),
 ( 1.000000000000000000, 0.7067447018949120086, 1.000000000000000000),
 ( 1.000000000000000000, 0.7067447029564462024, 1.000000000000000000),
 ( 1.000000000000000000, 0.7067447034884694057, 1.000000000000000000),
 ( 1.000000000000000000, 0.7067447050884115844, 1.000000000000000000),
 ( 1.000000000000000000, 0.7067447061600561353, 1.000000000000000000),
 ( 1.000000000000000000, 0.7067447072368862049, 1.000000000000000000) ) ) 
 REPRESENTATION_ITEM ( '' )  SURFACE ( )  );
#28810=ORIENTED_EDGE ( 'NONE', *, *, #3437, .T. ) ;
#28818=CARTESIAN_POINT ( 'NONE',  ( 20.75046113880788923, -21.62010873700192803, -1.554218361998998210 ) ) ;
#28820=CARTESIAN_POINT ( 'NONE',  ( 0.6071737056423955892, -7.494373765315226699, -1.499999999999999778 ) ) ;
#28825=CARTESIAN_POINT ( 'NONE',  ( 25.10129074173041985, -17.52164282029558962, -1.281897516810667215 ) ) ;
#28829=ORIENTED_EDGE ( 'NONE', *, *, #10388, .F. ) ;
#28830=DIRECTION ( 'NONE',  ( 0.000000000000000000, 0.000000000000000000, -1.000000000000000000 ) ) ;
#28841=CARTESIAN_POINT ( 'NONE',  ( 108.0265366049212332, -18.45148262600833178, 4.417053837905102753 ) ) ;
#28843=CARTESIAN_POINT ( 'NONE',  ( 3.541509388326463004, -13.88765124358303993, -4.522129901861164925 ) ) ;
#28849=LINE ( 'NONE', #5949, #26740 ) ;
#28850=CARTESIAN_POINT ( 'NONE',  ( 23.27353278736381981, -21.94187821002792660, 1.000000000000000000 ) ) ;
#28861=CARTESIAN_POINT ( 'NONE',  ( 7.461135469111389362, -4.560857689425765749, 1.500000000000283995 ) ) ;
#28879=AXIS2_PLACEMENT_3D ( 'NONE', #14564, #11903, #9379 ) ;
#28880=CARTESIAN_POINT ( 'NONE',  ( 24.39659513448100725, -17.41072360183587264, -1.416990234759457401 ) ) ;
#28885=EDGE_LOOP ( 'NONE', ( #24531, #10580, #10823, #14917, #9176 ) ) ;
#28886=VERTEX_POINT ( 'NONE', #7348 ) ;
#28889=CYLINDRICAL_SURFACE ( 'NONE', #4929, 0.5000000000000000000 ) ;
#28890=CARTESIAN_POINT ( 'NONE',  ( 41.92799935459299832, -21.01937708444107855, 4.522129901861156931 ) ) ;
#28916=AXIS2_PLACEMENT_3D ( 'NONE', #26278, #3394, #26597 ) ;
#28921=CARTESIAN_POINT ( 'NONE',  ( 7.085399849431558650, -9.284427924817970634, 1.499999999999999556 ) ) ;
#28923=CARTESIAN_POINT ( 'NONE',  ( 0.3238988396964614935, -5.504238404182476785, -1.499999999999999778 ) ) ;
#28924=CARTESIAN_POINT ( 'NONE',  ( -50.60000000000000142, -10.96966150227468972, 7.500000000000000000 ) ) ;
#28929=DIRECTION ( 'NONE',  ( -1.000000000000000000, 2.473959037481237219E-13, 0.000000000000000000 ) ) ;
#28960=CARTESIAN_POINT ( 'NONE',  ( 107.4494258168277554, -17.35106999866604127, 4.497200797759677293 ) ) ;
#28965=DIRECTION ( 'NONE',  ( -0.000000000000000000, 0.000000000000000000, 1.000000000000000000 ) ) ;
#28977=CARTESIAN_POINT ( 'NONE',  ( -3.348814662102636230, -1.982334143703736062, -1.747785174145542575 ) ) ;
#28982=CARTESIAN_POINT ( 'NONE',  ( 6.653983693897041363, -6.711078333448701194, -1.500000000000000000 ) ) ;
#28983=CARTESIAN_POINT ( 'NONE',  ( 107.9801098452135335, -17.78294883574212548, -4.320080270629262031 ) ) ;
#28985=AXIS2_PLACEMENT_3D ( 'NONE', #10370, #31272, #5825 ) ;
#28990=CARTESIAN_POINT ( 'NONE',  ( -2.819379691724115400, -6.927609664242504017, 4.522129901861158707 ) ) ;
#28995=DIRECTION ( 'NONE',  ( -0.000000000000000000, 0.000000000000000000, 1.000000000000000000 ) ) ;
#28996=EDGE_CURVE ( 'NONE', #23130, #8778, #530, .T. ) ;
#29007=ORIENTED_EDGE ( 'NONE', *, *, #25772, .F. ) ;
#29010=CARTESIAN_POINT ( 'NONE',  ( 24.35085591271539229, -17.33674746172404824, -1.318654801572369584 ) ) ;
#29018=EDGE_LOOP ( 'NONE', ( #2999, #9801 ) ) ;
#29019=LINE ( 'NONE', #14420, #54 ) ;
#29026=FACE_OUTER_BOUND ( 'NONE', #10395, .T. ) ;
#29034=EDGE_CURVE ( 'NONE', #19511, #3232, #21334, .T. ) ;
#29038=CARTESIAN_POINT ( 'NONE',  ( 24.39659513448100725, -17.41072360183587264, -1.416990234759457401 ) ) ;
#29040=CARTESIAN_POINT ( 'NONE',  ( -15.12340757463330654, -27.93932300454937590, -1.000000000000000000 ) ) ;
#29046=EDGE_LOOP ( 'NONE', ( #19746, #2691, #1678, #24631, #17466 ) ) ;
#29050=CARTESIAN_POINT ( 'NONE',  ( 7.154313482939235413, -6.723190066307162205, 1.499999999999999112 ) ) ;
#29056=CARTESIAN_POINT ( 'NONE',  ( 4.773472048928010025, -12.83524871782340959, 1.756822611201597661 ) ) ;
#29074=VERTEX_POINT ( 'NONE', #32227 ) ;
#29077=VECTOR ( 'NONE', #23161, 1000.000000000000000 ) ;
#29094=LINE ( 'NONE', #6181, #1265 ) ;
#29095=ORIENTED_EDGE ( 'NONE', *, *, #3734, .T. ) ;
#29097=EDGE_LOOP ( 'NONE', ( #22413, #16182 ) ) ;
#29099=CARTESIAN_POINT ( 'NONE',  ( 17.36028307726380504, -18.11957666779667875, -4.522129901861164925 ) ) ;
#29107=CARTESIAN_POINT ( 'NONE',  ( 7.580875386713984199, -18.74596882399356446, 1.749278895650158372 ) ) ;
#29111=ORIENTED_EDGE ( 'NONE', *, *, #23019, .F. ) ;
#29116=CARTESIAN_POINT ( 'NONE',  ( 25.52557118915447987, -17.56218954043521663, 1.000000000000000000 ) ) ;
#29118=CARTESIAN_POINT ( 'NONE',  ( -3.686257773765320600, -9.650692365544669471, -1.743566994282037541 ) ) ;
#29123=FACE_OUTER_BOUND ( 'NONE', #257, .T. ) ;
#29129=EDGE_LOOP ( 'NONE', ( #23395, #3705, #4519, #29597 ) ) ;
#29136=CARTESIAN_POINT ( 'NONE',  ( 22.52203367452234062, -21.86037836540921830, -1.499999999999999556 ) ) ;
#29138=CARTESIAN_POINT ( 'NONE',  ( -28.85000000000000497, -10.96966150227469505, 4.000000000000000000 ) ) ;
#29143=CARTESIAN_POINT ( 'NONE',  ( 7.289999265596935452, -8.244573099839797692, -1.499999999999714673 ) ) ;
#29144=CARTESIAN_POINT ( 'NONE',  ( 107.9778899347920600, -17.75098267791648610, -4.255947362158985392 ) ) ;
#29150=ORIENTED_EDGE ( 'NONE', *, *, #25725, .F. ) ;
#29157=VERTEX_POINT ( 'NONE', #5624 ) ;
#29158=CARTESIAN_POINT ( 'NONE',  ( 5.532756613957264591, -12.77534133546009087, -1.500000000000000666 ) ) ;
#29169=EDGE_LOOP ( 'NONE', ( #10929, #1080, #27389, #16789, #25965, #32447, #25029 ) ) ;
#29170=CARTESIAN_POINT ( 'NONE',  ( -2.223027892448374399, -2.927336879245633572, 4.522129901861158707 ) ) ;
#29171=CARTESIAN_POINT ( 'NONE',  ( -5.427698642335591239E-12, -21.93932300456189566, -1.000000000000000000 ) ) ;
#29180=CARTESIAN_POINT ( 'NONE',  ( 108.0285047196611430, -18.47982298865751005, 4.352162063355596189 ) ) ;
#29181=CARTESIAN_POINT ( 'NONE',  ( -2.613459990200682537, -0.04407919770141072169, -1.513648816985697199 ) ) ;
#29186=CARTESIAN_POINT ( 'NONE',  ( 23.25968157276533788, -21.94039639456149970, 1.058068383262721790 ) ) ;
#29191=EDGE_LOOP ( 'NONE', ( #13387, #27961, #705, #7669 ) ) ;
#29194=CARTESIAN_POINT ( 'NONE',  ( 107.7140348563909669, -17.39211855127401307, 4.500745083103332433 ) ) ;
#29197=EDGE_LOOP ( 'NONE', ( #23057, #12734, #5770, #14024, #12095 ) ) ;
#29198=CARTESIAN_POINT ( 'NONE',  ( 6.910673634762011908, -8.774004714863222532, -1.500000000000000444 ) ) ;
#29199=ORIENTED_EDGE ( 'NONE', *, *, #11023, .T. ) ;
#29200=CARTESIAN_POINT ( 'NONE',  ( 0.1308125268056005985, -6.172912210551425360, 1.772480729299952928 ) ) ;
#29206=CARTESIAN_POINT ( 'NONE',  ( 23.30969226767547298, -17.20274083179951674, -1.451821733976820239 ) ) ;
#29208=VERTEX_POINT ( 'NONE', #15140 ) ;
#29216=DIRECTION ( 'NONE',  ( 0.1290991311231024230, 0.9916316928896837801, 0.000000000000000000 ) ) ;
#29224=DIRECTION ( 'NONE',  ( 0.000000000000000000, -1.000000000000000000, 0.000000000000000000 ) ) ;
#29225=CARTESIAN_POINT ( 'NONE',  ( 17.97422212135272801, -19.86246923125032637, 4.522129901861159595 ) ) ;
#29235=CARTESIAN_POINT ( 'NONE',  ( 3.660726896358641902, 3.599890025830775825E-17, -1.077884872112069292 ) ) ;
#29239=ORIENTED_EDGE ( 'NONE', *, *, #8798, .T. ) ;
#29243=EDGE_CURVE ( 'NONE', #29157, #5623, #23990, .T. ) ;
#29244=CARTESIAN_POINT ( 'NONE',  ( 7.177184080414120260, -7.491031434833116620, -1.000000000000000000 ) ) ;
#29254=EDGE_LOOP ( 'NONE', ( #32008, #8762, #29199 ) ) ;
#29265=CARTESIAN_POINT ( 'NONE',  ( -3.910356079379007088, -9.341596471033172477, -1.500000000000000000 ) ) ;
#29270=CARTESIAN_POINT ( 'NONE',  ( 20.53274989849606769, -21.72776571847631999, 1.408906953170992127 ) ) ;
#29277=B_SPLINE_CURVE_WITH_KNOTS ( 'NONE', 3,
 ( #310, #2995, #28199, #10322, #10805, #22855, #5646, #13148, #25691, #29325, #5933, #19134, #4102, #938, #6605, #10968 ),
 .UNSPECIFIED., .F., .F.,
 ( 4, 2, 2, 2, 2, 2, 2, 4 ),
 ( 0.000000000000000000, 3.093269050410396288E-05, 6.186538100820792576E-05, 0.0001237307620164256093, 0.0002474615240328612476, 0.0004949230480657320361, 0.0009898460961314727458, 0.001979692192262965007 ),
 .UNSPECIFIED. ) ;
#29284=EDGE_LOOP ( 'NONE', ( #12513, #18516, #25314, #21426 ) ) ;
#29290=CARTESIAN_POINT ( 'NONE',  ( -4.062288539342293170, -5.105566185483802144, -1.745843300479905436 ) ) ;
#29292=CARTESIAN_POINT ( 'NONE',  ( 13.85437446117461491, -14.51384729145977204, -1.499999999999999334 ) ) ;
#29293=CARTESIAN_POINT ( 'NONE',  ( 107.8806307222008627, -16.35047421165092985, -1.384330804613826293 ) ) ;
#29294=ORIENTED_EDGE ( 'NONE', *, *, #7742, .F. ) ;
#29299=CARTESIAN_POINT ( 'NONE',  ( 6.448894291894883501, -17.04229596238074507, 4.522129901861158707 ) ) ;
#29313=VERTEX_POINT ( 'NONE', #11593 ) ;
#29325=CARTESIAN_POINT ( 'NONE',  ( 22.93781638691914182, -21.92296000134991729, 1.128554389308254136 ) ) ;
#29329=CARTESIAN_POINT ( 'NONE',  ( 108.0605219787248643, -18.94086355428285984, 4.544875792429381889 ) ) ;
#29331=CARTESIAN_POINT ( 'NONE',  ( -0.9232102171129827894, 0.000000000000000000, -4.522129901861166701 ) ) ;
#29337=EDGE_CURVE ( 'NONE', #22172, #25587, #9834, .T. ) ;
#29349=CARTESIAN_POINT ( 'NONE',  ( 7.565496255526688252, -10.23852490753150768, -1.499999999999999778 ) ) ;
#29353=CARTESIAN_POINT ( 'NONE',  ( 0.3239945992768507033, -5.503618096412950855, 1.499999999999858558 ) ) ;
#29364=EDGE_CURVE ( 'NONE', #12752, #24872, #32145, .T. ) ;
#29365=CARTESIAN_POINT ( 'NONE',  ( 23.12748570787497826, -21.92617700502155387, -1.175810055043982061 ) ) ;
#29369=CARTESIAN_POINT ( 'NONE',  ( -14.51685907258683983, -28.43932300454937590, -1.000000000000000000 ) ) ;
#29382=CARTESIAN_POINT ( 'NONE',  ( 42.67399297346871379, -22.27808837059998481, 5.485967528433935314 ) ) ;
#29393=DIRECTION ( 'NONE',  ( 0.9816271834476644198, 0.000000000000000000, 0.1908089953765420288 ) ) ;
#29396=CARTESIAN_POINT ( 'NONE',  ( -31.63092319849839029, -25.68921844201284088, 1.340913934978428035 ) ) ;
#29403=VECTOR ( 'NONE', #28640, 1000.000000000000000 ) ;
#29412=EDGE_CURVE ( 'NONE', #28440, #21586, #16864, .T. ) ;
#29413=CARTESIAN_POINT ( 'NONE',  ( -23.35000000000000142, -10.96966150227469505, -11.00000000000000000 ) ) ;
#29420=DIRECTION ( 'NONE',  ( 0.1587661886298589176, 0.9873162094020071500, 0.000000000000000000 ) ) ;
#29434=CARTESIAN_POINT ( 'NONE',  ( -23.35000000000000142, -10.96966150227469505, -11.50000000000000000 ) ) ;
#29441=ORIENTED_EDGE ( 'NONE', *, *, #19148, .F. ) ;
#29448=CIRCLE ( 'NONE', #629, 6.000000000000001776 ) ;
#29453=CARTESIAN_POINT ( 'NONE',  ( -23.35000000000000142, -10.96966150227469505, -1.499999999999999556 ) ) ;
#29460=CARTESIAN_POINT ( 'NONE',  ( 22.00639167669224960, -21.80013755708282730, -1.499999999999999556 ) ) ;
#29463=CARTESIAN_POINT ( 'NONE',  ( -2.807293726618242946, -12.37543429821833385, -1.499999999999999556 ) ) ;
#29468=CARTESIAN_POINT ( 'NONE',  ( 7.166310627377574072, -7.340520188494797260, -1.499999999999856559 ) ) ;
#29469=CARTESIAN_POINT ( 'NONE',  ( 107.4526306908116879, -17.39749363332668608, -4.613092379735242332 ) ) ;
#29483=CIRCLE ( 'NONE', #5966, 7.634842307437897269 ) ;
#29491=ORIENTED_EDGE ( 'NONE', *, *, #12012, .T. ) ;
#29495=ORIENTED_EDGE ( 'NONE', *, *, #15477, .T. ) ;
#29499=ORIENTED_EDGE ( 'NONE', *, *, #29651, .F. ) ;
#29514=CIRCLE ( 'NONE', #10822, 0.4999999999999978351 ) ;
#29539=CARTESIAN_POINT ( 'NONE',  ( 6.879500825888995585, -8.675028761530525045, 1.500000000000000000 ) ) ;
#29542=CARTESIAN_POINT ( 'NONE',  ( 9.613697478362256632, -12.36077863760288231, -1.500000000000000444 ) ) ;
#29544=CARTESIAN_POINT ( 'NONE',  ( 0.4214208491204014528, -4.489406624787253719, 1.766534570867400955 ) ) ;
#29548=CARTESIAN_POINT ( 'NONE',  ( 11.59711033912294731, -20.31971356584124422, 1.499999999999999334 ) ) ;
#29553=FACE_OUTER_BOUND ( 'NONE', #3604, .T. ) ;
#29555=ORIENTED_EDGE ( 'NONE', *, *, #6127, .F. ) ;
#29561=VECTOR ( 'NONE', #5564, 1000.000000000000000 ) ;
#29571=CARTESIAN_POINT ( 'NONE',  ( 107.9916885326170473, -18.73354948406877440, 4.428418223197585490 ) ) ;
#29580=CIRCLE ( 'NONE', #10365, 6.000000000000001776 ) ;
#29597=ORIENTED_EDGE ( 'NONE', *, *, #3734, .F. ) ;
#29601=CARTESIAN_POINT ( 'NONE',  ( 0.3474085791285200786, -7.723996299823893352, -1.499999999999981570 ) ) ;
#29603=EDGE_LOOP ( 'NONE', ( #548, #27147, #22743, #12897 ) ) ;
#29607=CARTESIAN_POINT ( 'NONE',  ( 107.5603894785018468, -18.96336710931913316, -4.563597971271542875 ) ) ;
#29618=CARTESIAN_POINT ( 'NONE',  ( -3.135269660805079628, -0.5000000000000025535, -1.500000000000000000 ) ) ;
#29625=EDGE_CURVE ( 'NONE', #30338, #21513, #18749, .T. ) ;
#29642=CARTESIAN_POINT ( 'NONE',  ( 2.281627749324420140, -0.2935656086769634077, -1.757435426329174710 ) ) ;
#29648=CARTESIAN_POINT ( 'NONE',  ( 6.800570610007084404, -8.349954097220308569, -1.500000000000000000 ) ) ;
#29649=CARTESIAN_POINT ( 'NONE',  ( 107.4581045272831545, -17.47692235061807864, -4.756303059044163284 ) ) ;
#29651=EDGE_CURVE ( 'NONE', #9004, #19632, #19319, .T. ) ;
#29654=CARTESIAN_POINT ( 'NONE',  ( 9.350000000000001421, 0.000000000000000000, 1.000000000000000000 ) ) ;
#29655=CARTESIAN_POINT ( 'NONE',  ( 24.46547057403054737, -17.44104734125400213, -1.464603527736665134 ) ) ;
#29665=DIRECTION ( 'NONE',  ( 2.473959037481232675E-13, 1.000000000000000000, 0.000000000000000000 ) ) ;
#29704=( BOUNDED_SURFACE ( )  B_SPLINE_SURFACE ( 3, 2, ( 
 ( #20858, #31071, #10996 ),
 ( #21196, #8470, #5659 ),
 ( #28215, #23220, #10498 ),
 ( #5318, #15495, #636 ),
 ( #10827, #21042, #31249 ),
 ( #8323, #18519, #5968 ),
 ( #28712, #19512, #29544 ),
 ( #29706, #21678, #21343 ),
 ( #31886, #29353, #9296 ),
 ( #4125, #16164, #29200 ),
 ( #6288, #1609, #21829 ),
 ( #1119, #11797, #6631 ),
 ( #26536, #8636, #16823 ),
 ( #3791, #13962, #14145 ),
 ( #11315, #16473, #21525 ),
 ( #31735, #23999, #24344 ),
 ( #8810, #19017, #26680 ),
 ( #23853, #24181, #22006 ),
 ( #26395, #11142, #16328 ),
 ( #1308, #19341, #3493 ),
 ( #11484, #8952, #27023 ),
 ( #1456, #19160, #6441 ),
 ( #16648, #26858, #3975 ),
 ( #11634, #31548, #32040 ),
 ( #9109, #32230, #962 ),
 ( #13649, #18854, #29056 ),
 ( #3639, #14291, #24489 ),
 ( #6146, #13794, #14953 ),
 ( #4778, #30366, #6942 ),
 ( #32719, #25166, #17634 ),
 ( #2288, #4280, #2107 ),
 ( #9449, #7134, #27839 ),
 ( #6787, #17476, #1962 ),
 ( #24668, #27523, #19830 ),
 ( #16975, #22500, #27173 ),
 ( #10107, #14453, #1796 ),
 ( #17329, #27675, #19667 ),
 ( #22686, #9798, #27354 ) ),
 .UNSPECIFIED., .F., .F., .F. ) 
 B_SPLINE_SURFACE_WITH_KNOTS ( ( 4, 2, 2, 2, 2, 2, 2, 2, 2, 2, 2, 2, 2, 2, 2, 2, 2, 2, 4 ),
 ( 3, 3 ),
 ( 0.000000000000000000, 0.001917845367245767704, 0.003835690734491535407, 0.004794613418114419476, 0.005753536101737302677, 0.006712458785360186746, 0.007191920127171628346, 0.007671381468983070814, 0.008630304152605954016, 0.009589226836228838952, 0.01150707220347460535, 0.01246599488709749029, 0.01342491757072037349, 0.01534276293796614163, 0.01726060830521190803, 0.01917845367245767790, 0.02301414440694921071, 0.02684983514144074698, 0.03068552587593228326 ),
 ( 0.000000000000000000, 1.000000000000000000 ),
 .UNSPECIFIED. ) 
 GEOMETRIC_REPRESENTATION_ITEM ( )  RATIONAL_B_SPLINE_SURFACE ( (
 ( 1.000000000000000000, 0.8449619147701442623, 1.000000000000000000),
 ( 1.000000000000000000, 0.8445678281941895182, 1.000000000000000000),
 ( 1.000000000000000000, 0.8440735482790849842, 1.000000000000000000),
 ( 1.000000000000000000, 0.8426717852686910204, 1.000000000000000000),
 ( 1.000000000000000000, 0.8417782867635215105, 1.000000000000000000),
 ( 1.000000000000000000, 0.8396989866086126408, 1.000000000000000000),
 ( 1.000000000000000000, 0.8389583138861036460, 1.000000000000000000),
 ( 1.000000000000000000, 0.8374420476517394629, 1.000000000000000000),
 ( 1.000000000000000000, 0.8366705097161594162, 1.000000000000000000),
 ( 1.000000000000000000, 0.8350115697338978960, 1.000000000000000000),
 ( 1.000000000000000000, 0.8340765399395944080, 1.000000000000000000),
 ( 1.000000000000000000, 0.8336680578661073149, 1.000000000000000000),
 ( 1.000000000000000000, 0.8336622264597983722, 1.000000000000000000),
 ( 1.000000000000000000, 0.8338830948382838226, 1.000000000000000000),
 ( 1.000000000000000000, 0.8341112768085173768, 1.000000000000000000),
 ( 1.000000000000000000, 0.8349632181683559473, 1.000000000000000000),
 ( 1.000000000000000000, 0.8357222399959970405, 1.000000000000000000),
 ( 1.000000000000000000, 0.8375330892283537887, 1.000000000000000000),
 ( 1.000000000000000000, 0.8383871522769865692, 1.000000000000000000),
 ( 1.000000000000000000, 0.8406677340059340864, 1.000000000000000000),
 ( 1.000000000000000000, 0.8419340173013039053, 1.000000000000000000),
 ( 1.000000000000000000, 0.8434078201704927613, 1.000000000000000000),
 ( 1.000000000000000000, 0.8438011345265380436, 1.000000000000000000),
 ( 1.000000000000000000, 0.8444525021093555184, 1.000000000000000000),
 ( 1.000000000000000000, 0.8447123061114764075, 1.000000000000000000),
 ( 1.000000000000000000, 0.8453648520239724906, 1.000000000000000000),
 ( 1.000000000000000000, 0.8456340021638725224, 1.000000000000000000),
 ( 1.000000000000000000, 0.8460540157046728682, 1.000000000000000000),
 ( 1.000000000000000000, 0.8462024902987614894, 1.000000000000000000),
 ( 1.000000000000000000, 0.8464941297768426853, 1.000000000000000000),
 ( 1.000000000000000000, 0.8466725100393527326, 1.000000000000000000),
 ( 1.000000000000000000, 0.8470349430677968083, 1.000000000000000000),
 ( 1.000000000000000000, 0.8471950786340051165, 1.000000000000000000),
 ( 1.000000000000000000, 0.8474407600832977172, 1.000000000000000000),
 ( 1.000000000000000000, 0.8475244351830560907, 1.000000000000000000),
 ( 1.000000000000000000, 0.8476586567771616787, 1.000000000000000000),
 ( 1.000000000000000000, 0.8477086664503143965, 1.000000000000000000),
 ( 1.000000000000000000, 0.8477574071929551147, 1.000000000000000000) ) ) 
 REPRESENTATION_ITEM ( '' )  SURFACE ( )  );
#29705=ORIENTED_EDGE ( 'NONE', *, *, #32513, .T. ) ;
#29706=CARTESIAN_POINT ( 'NONE',  ( 0.6729935896713523658, -5.225233662718014038, 1.500000000000000000 ) ) ;
#29710=CARTESIAN_POINT ( 'NONE',  ( 9.337065666035902822, -0.007760238742139066379, -1.098363920870219168 ) ) ;
#29715=FACE_OUTER_BOUND ( 'NONE', #9263, .T. ) ;
#29720=DIRECTION ( 'NONE',  ( 0.000000000000000000, 0.000000000000000000, 1.000000000000000000 ) ) ;
#29726=DIRECTION ( 'NONE',  ( -0.000000000000000000, 0.000000000000000000, 1.000000000000000000 ) ) ;
#29732=DIRECTION ( 'NONE',  ( -1.000000000000000000, 2.498001805406600196E-13, 0.000000000000000000 ) ) ;
#29735=DIRECTION ( 'NONE',  ( 0.000000000000000000, -1.000000000000000000, 0.000000000000000000 ) ) ;
#29750=CYLINDRICAL_SURFACE ( 'NONE', #18298, 0.5000000000000004441 ) ;
#29751=ORIENTED_EDGE ( 'NONE', *, *, #10619, .T. ) ;
#29756=CARTESIAN_POINT ( 'NONE',  ( 9.015861660202212136, -14.64815961618594109, -1.754831069275766042 ) ) ;
#29758=ORIENTED_EDGE ( 'NONE', *, *, #18537, .T. ) ;
#29764=CARTESIAN_POINT ( 'NONE',  ( 3.519702661476644678, 3.984442983884231162E-15, 1.098333652976365871 ) ) ;
#29771=CARTESIAN_POINT ( 'NONE',  ( -3.789183816811442007, -9.307783592219267987, -1.743674011537540203 ) ) ;
#29774=PRODUCT_DEFINITION_SHAPE ( 'NONE', 'NONE',  #32113 ) ;
#29787=B_SPLINE_CURVE_WITH_KNOTS ( 'NONE', 3,
 ( #25206, #4995, #7469, #18169, #30246, #27703 ),
 .UNSPECIFIED., .F., .F.,
 ( 4, 2, 4 ),
 ( 2.872315617951276927E-05, 0.0004097954672334697037, 0.0007908677782874266957 ),
 .UNSPECIFIED. ) ;
#29802=CARTESIAN_POINT ( 'NONE',  ( -4.059984658974702398, -5.088068716088551824, 1.745854725342557812 ) ) ;
#29804=CARTESIAN_POINT ( 'NONE',  ( 107.4762276881066043, -17.74013139905899905, -5.017020369388183632 ) ) ;
#29810=CARTESIAN_POINT ( 'NONE',  ( 107.3477133433398620, -15.88627905081428260, -1.500000000000000000 ) ) ;
#29815=DIRECTION ( 'NONE',  ( 0.000000000000000000, -1.000000000000000000, 0.000000000000000000 ) ) ;
#29820=CARTESIAN_POINT ( 'NONE',  ( 3.086618293031875293, -0.003885106576443817308, -0.6225218429476583326 ) ) ;
#29822=CARTESIAN_POINT ( 'NONE',  ( 7.167277592125206986, -6.432846314878395866, 1.000000000000000666 ) ) ;
#29829=VERTEX_POINT ( 'NONE', #12816 ) ;
#29830=ORIENTED_EDGE ( 'NONE', *, *, #1872, .T. ) ;
#29834=LINE ( 'NONE', #27315, #21437 ) ;
#29841=CARTESIAN_POINT ( 'NONE',  ( 107.6300027436162310, -19.96576125925734502, 2.508990583257467044 ) ) ;
#29845=CARTESIAN_POINT ( 'NONE',  ( 25.52557118915443723, -17.56218954043521308, 1.000000000000000888 ) ) ;
#29853=CARTESIAN_POINT ( 'NONE',  ( 21.64915922382874314, -21.84574418159160203, -1.293067337327047372 ) ) ;
#29858=CARTESIAN_POINT ( 'NONE',  ( 16.05919002109104099, -15.28992581341303136, -1.499999999999999778 ) ) ;
#29863=VERTEX_POINT ( 'NONE', #23702 ) ;
#29864=CARTESIAN_POINT ( 'NONE',  ( 17.33093461831347781, -21.43932300456618378, 1.500000000000000000 ) ) ;
#29865=AXIS2_PLACEMENT_3D ( 'NONE', #27499, #12445, #24972 ) ;
#29868=CARTESIAN_POINT ( 'NONE',  ( 24.40342144122098134, -17.37878489514604041, -1.350270808451339510 ) ) ;
#29884=CARTESIAN_POINT ( 'NONE',  ( -23.35000000000000142, -10.96966150227469505, -11.50000000000000000 ) ) ;
#29885=CARTESIAN_POINT ( 'NONE',  ( 25.41905588447623643, -17.54124894465117279, -1.046314264356064117 ) ) ;
#29887=CARTESIAN_POINT ( 'NONE',  ( 17.33093461831353466, -21.43932300456619089, 1.949999999999999512 ) ) ;
#29890=DIRECTION ( 'NONE',  ( -0.000000000000000000, 0.000000000000000000, 1.000000000000000000 ) ) ;
#29915=CARTESIAN_POINT ( 'NONE',  ( 0.8637286840862898885, -8.447112080008446711, -1.500000000000000444 ) ) ;
#29928=ADVANCED_FACE ( 'NONE', ( #324 ), #29704, .F. ) ;
#29933=CARTESIAN_POINT ( 'NONE',  ( 11.75204077933772417, -19.94170559719522728, -1.750535629482800282 ) ) ;
#29948=CARTESIAN_POINT ( 'NONE',  ( -29.35000000000000853, -10.96966150227469505, -1.500000000000000000 ) ) ;
#29950=ORIENTED_EDGE ( 'NONE', *, *, #8631, .T. ) ;
#29959=CARTESIAN_POINT ( 'NONE',  ( 7.382000898082563545, -19.12189044733477417, -1.499999999999998224 ) ) ;
#29965=CARTESIAN_POINT ( 'NONE',  ( 108.0278902883042633, -18.47097532996942348, -4.374628062554474006 ) ) ;
#29966=ORIENTED_EDGE ( 'NONE', *, *, #4569, .F. ) ;
#29975=DIRECTION ( 'NONE',  ( -1.000000000000000000, 0.000000000000000000, 0.000000000000000000 ) ) ;
#29988=CARTESIAN_POINT ( 'NONE',  ( 3.527557386959558894, -11.88551672347146848, -0.9788672205888330202 ) ) ;
#30007=B_SPLINE_CURVE_WITH_KNOTS ( 'NONE', 3,
 ( #31190, #5900, #13113, #25994, #7927, #20492, #28157, #79, #3101, #13412, #23632, #23313, #20653, #8418, #2760, #755, #16090, #15620, #12758, #5425, #20973, #28314, #13257, #25833, #31339, #26144, #8272, #10442, #5261, #15931, #10938, #5753, #18611, #15433, #2593, #23458, #416, #18464 ),
 .UNSPECIFIED., .F., .F.,
 ( 4, 2, 2, 2, 2, 2, 2, 2, 2, 2, 2, 2, 2, 2, 2, 2, 2, 2, 4 ),
 ( 1.067815302520814551E-18, 0.001916204205297452126, 0.003832408410594902951, 0.004790510513243628581, 0.005748612615892353776, 0.006706714718541078972, 0.007185765769865441570, 0.007664816821189803300, 0.008622918923838523292, 0.009581021026487241549, 0.01149722523178467806, 0.01245532733443339458, 0.01341342943708211284, 0.01532963364237954589, 0.01724583784767698066, 0.01916204205297441718, 0.02299445046356927980, 0.02682685887416414242, 0.03065926728475900503 ),
 .UNSPECIFIED. ) ;
#30015=AXIS2_PLACEMENT_3D ( 'NONE', #31444, #28929, #6034 ) ;
#30016=CARTESIAN_POINT ( 'NONE',  ( 110.2779561444948939, -18.44184597392421665, -5.485967528433938867 ) ) ;
#30017=CARTESIAN_POINT ( 'NONE',  ( 107.9116956367119116, -16.79780125263170376, -2.301619431082305489 ) ) ;
#30019=EDGE_CURVE ( 'NONE', #32242, #28214, #10779, .T. ) ;
#30024=CARTESIAN_POINT ( 'NONE',  ( 6.448894291898077391, -17.04229596238074862, 4.522129901861159595 ) ) ;
#30050=ORIENTED_EDGE ( 'NONE', *, *, #3497, .F. ) ;
#30065=AXIS2_PLACEMENT_3D ( 'NONE', #27785, #5078, #12732 ) ;
#30072=ADVANCED_FACE ( 'NONE', ( #5124 ), #23180, .T. ) ;
#30079=ORIENTED_EDGE ( 'NONE', *, *, #7324, .F. ) ;
#30080=AXIS2_PLACEMENT_3D ( 'NONE', #1140, #19178, #29216 ) ;
#30087=FACE_OUTER_BOUND ( 'NONE', #29018, .T. ) ;
#30103=CYLINDRICAL_SURFACE ( 'NONE', #27242, 0.5000000000000004441 ) ;
#30112=CARTESIAN_POINT ( 'NONE',  ( 0.5496208378618945289, -7.013485574150957191, -1.500000000000000444 ) ) ;
#30113=CARTESIAN_POINT ( 'NONE',  ( 0.3277201397524639459, -5.271209332775584677, 1.500000000000000444 ) ) ;
#30119=ORIENTED_EDGE ( 'NONE', *, *, #17121, .F. ) ;
#30120=CARTESIAN_POINT ( 'NONE',  ( 22.19921710918638880, -17.00655848932612102, 1.494769569001483500 ) ) ;
#30129=CARTESIAN_POINT ( 'NONE',  ( 15.95505886943986518, -20.93460726762247504, -1.499999999986860511 ) ) ;
#30144=DIRECTION ( 'NONE',  ( -0.000000000000000000, 0.000000000000000000, 1.000000000000000000 ) ) ;
#30152=CARTESIAN_POINT ( 'NONE',  ( 107.3615104199937775, -16.08547161712497697, 1.908459023709874636 ) ) ;
#30156=ADVANCED_FACE ( 'NONE', ( #8435 ), #13671, .F. ) ;
#30160=CARTESIAN_POINT ( 'NONE',  ( 107.9987586186765327, -18.05148653437722217, -4.627286608547184876 ) ) ;
#30167=DIRECTION ( 'NONE',  ( -1.000000000000000000, 0.000000000000000000, 0.000000000000000000 ) ) ;
#30175=CARTESIAN_POINT ( 'NONE',  ( 3.048228882235557879, 0.5389963249801591472, -1.289664751349871574 ) ) ;
#30177=CARTESIAN_POINT ( 'NONE',  ( 2.632061376486628301, -0.5000000000000000000, -1.500000000000000000 ) ) ;
#30195=DIRECTION ( 'NONE',  ( 1.000000000000000000, 0.000000000000000000, 0.000000000000000000 ) ) ;
#30196=CARTESIAN_POINT ( 'NONE',  ( 25.52557090713405685, -17.56218951387322491, 1.057622280107608725 ) ) ;
#30197=LINE ( 'NONE', #22315, #13930 ) ;
#30204=VERTEX_POINT ( 'NONE', #9072 ) ;
#30214=CARTESIAN_POINT ( 'NONE',  ( -2.386718424894566315, -9.330009425477193474, -4.522129901861166701 ) ) ;
#30215=VERTEX_POINT ( 'NONE', #31357 ) ;
#30226=DIRECTION ( 'NONE',  ( 1.000000000000000000, 0.000000000000000000, 0.000000000000000000 ) ) ;
#30236=DIRECTION ( 'NONE',  ( 0.000000000000000000, 0.000000000000000000, -1.000000000000000000 ) ) ;
#30237=LINE ( 'NONE', #6658, #20910 ) ;
#30240=CARTESIAN_POINT ( 'NONE',  ( 23.09498300328107590, -21.93193249238093756, 1.086362660086114929 ) ) ;
#30246=CARTESIAN_POINT ( 'NONE',  ( 107.7918428252582146, -20.44935860102534875, 1.500028854543402845 ) ) ;
#30247=CARTESIAN_POINT ( 'NONE',  ( 0.2603629172483717391, -5.188755369436605314, 1.768970845646744561 ) ) ;
#30251=ORIENTED_EDGE ( 'NONE', *, *, #23507, .F. ) ;
#30260=EDGE_LOOP ( 'NONE', ( #10916, #5757, #8476, #2941 ) ) ;
#30265=CARTESIAN_POINT ( 'NONE',  ( 0.5636839040845996740, -7.175910112258415019, -1.499999999999999556 ) ) ;
#30272=EDGE_LOOP ( 'NONE', ( #14737, #26172, #19045, #5469 ) ) ;
#30273=CARTESIAN_POINT ( 'NONE',  ( 22.17497728449718863, -17.32537947343248064, 1.743178009048999444 ) ) ;
#30280=CARTESIAN_POINT ( 'NONE',  ( -3.111251654333415217, -11.33182932643446605, -1.500000000000000222 ) ) ;
#30307=CARTESIAN_POINT ( 'NONE',  ( 107.5620888422228205, -18.98815586165099845, -4.509679481931270217 ) ) ;
#30308=VERTEX_POINT ( 'NONE', #9753 ) ;
#30309=CARTESIAN_POINT ( 'NONE',  ( 107.8806307222008627, -16.35047421165092985, 1.384330804614037236 ) ) ;
#30312=CARTESIAN_POINT ( 'NONE',  ( 107.3476950949991959, -15.88628029827230570, -1.500000000000000000 ) ) ;
#30315=ORIENTED_EDGE ( 'NONE', *, *, #26427, .F. ) ;
#30317=B_SPLINE_CURVE_WITH_KNOTS ( 'NONE', 3,
 ( #25867, #18493, #30737, #12978, #23493, #31223, #23192, #10473, #25515, #15656, #2984, #10626, #15158 ),
 .UNSPECIFIED., .F., .F.,
 ( 4, 3, 3, 3, 4 ),
 ( 8.673617379884035472E-19, 0.0002877298135619251536, 0.001654640778973444316, 0.002565914753109074971, 0.003274339315400769980 ),
 .UNSPECIFIED. ) ;
#30320=ORIENTED_EDGE ( 'NONE', *, *, #31875, .F. ) ;
#30322=( BOUNDED_SURFACE ( )  B_SPLINE_SURFACE ( 3, 2, ( 
 ( #29845, #27656, #10090 ),
 ( #30196, #17458, #25486 ),
 ( #17616, #15119, #12119 ),
 ( #25142, #32525, #15282 ),
 ( #25332, #12268, #33018 ),
 ( #27819, #32376, #4936 ),
 ( #28009, #2442, #2265 ),
 ( #12450, #12612, #7269 ),
 ( #32695, #22666, #4761 ),
 ( #22813, #20306, #9775 ) ),
 .UNSPECIFIED., .F., .F., .F. ) 
 B_SPLINE_SURFACE_WITH_KNOTS ( ( 4, 2, 2, 2, 4 ),
 ( 3, 3 ),
 ( 0.01348603581695214694, 0.01365687529133369216, 0.01382771476571523911, 0.01416939371447832954, 0.01485275161200451215 ),
 ( 0.000000000000000000, 1.000000000000000000 ),
 .UNSPECIFIED. ) 
 GEOMETRIC_REPRESENTATION_ITEM ( )  RATIONAL_B_SPLINE_SURFACE ( (
 ( 1.000000000000000000, 0.9948736491435667961, 1.000000000000000000),
 ( 1.000000000000000000, 0.9948794564610410340, 1.000000000000000000),
 ( 1.000000000000000000, 0.9935082075948730163, 1.000000000000000000),
 ( 1.000000000000000000, 0.9898246045859987463, 1.000000000000000000),
 ( 1.000000000000000000, 0.9875779995959915736, 1.000000000000000000),
 ( 1.000000000000000000, 0.9804235948789852273, 1.000000000000000000),
 ( 1.000000000000000000, 0.9752522326727456337, 1.000000000000000000),
 ( 1.000000000000000000, 0.9593679678194060312, 1.000000000000000000),
 ( 1.000000000000000000, 0.9482314950094890005, 1.000000000000000000),
 ( 1.000000000000000000, 0.9372872368324467462, 1.000000000000000000) ) ) 
 REPRESENTATION_ITEM ( '' )  SURFACE ( )  );
#30325=DIRECTION ( 'NONE',  ( -0.9816271834476639757, 0.000000000000000000, 0.1908089953765452762 ) ) ;
#30326=CARTESIAN_POINT ( 'NONE',  ( 3.750263394063806821, -2.684783475528570995E-05, -0.9948185799301207943 ) ) ;
#30330=LINE ( 'NONE', #17595, #24018 ) ;
#30332=CARTESIAN_POINT ( 'NONE',  ( -2.983877251335061320, -0.2474135948681125963, 1.436677650513773274 ) ) ;
#30338=VERTEX_POINT ( 'NONE', #14765 ) ;
#30344=CARTESIAN_POINT ( 'NONE',  ( 108.0945118936045191, -19.43030987200927839, 3.536500079626898163 ) ) ;
#30345=DIRECTION ( 'NONE',  ( -1.000000000000000000, 0.000000000000000000, -0.000000000000000000 ) ) ;
#30346=DIRECTION ( 'NONE',  ( -0.000000000000000000, -0.000000000000000000, 1.000000000000000000 ) ) ;
#30347=FACE_OUTER_BOUND ( 'NONE', #12055, .T. ) ;
#30357=ADVANCED_FACE ( 'NONE', ( #17444 ), #5390, .F. ) ;
#30364=CARTESIAN_POINT ( 'NONE',  ( 107.4539122023615221, -17.41608652575267158, 4.650537122213327379 ) ) ;
#30366=CARTESIAN_POINT ( 'NONE',  ( 7.214127126792253542, -13.85184692375858617, 1.500000000000140332 ) ) ;
#30370=CARTESIAN_POINT ( 'NONE',  ( -3.790520337094915870, -3.338398410437402042, 1.747101600989292791 ) ) ;
#30374=EDGE_LOOP ( 'NONE', ( #23621, #4200, #29111 ) ) ;
#30380=EDGE_CURVE ( 'NONE', #30476, #11874, #176, .T. ) ;
#30381=FACE_BOUND ( 'NONE', #29097, .T. ) ;
#30389=CARTESIAN_POINT ( 'NONE',  ( 23.14329945973256031, -21.92788238883854390, 1.164089052066326069 ) ) ;
#30397=CARTESIAN_POINT ( 'NONE',  ( 3.744708216408842549, 0.000000000000000000, -1.000000000000000000 ) ) ;
#30414=CARTESIAN_POINT ( 'NONE',  ( -50.60000000000000142, -10.96966150227468972, 7.500000000000000000 ) ) ;
#30415=CARTESIAN_POINT ( 'NONE',  ( 1.278428506419904798, -2.392608122357158251, 1.500000000000000444 ) ) ;
#30429=ADVANCED_FACE ( 'NONE', ( #28484 ), #28642, .T. ) ;
#30433=CARTESIAN_POINT ( 'NONE',  ( -2.938251396093196632, -11.64407820748950861, -1.500000000000079714 ) ) ;
#30436=CARTESIAN_POINT ( 'NONE',  ( 107.4514419172558064, -17.38041855283238135, 4.563595182964964359 ) ) ;
#30452=ORIENTED_EDGE ( 'NONE', *, *, #6966, .F. ) ;
#30453=CARTESIAN_POINT ( 'NONE',  ( 18.53175858344379634, -21.44524224917989130, -1.500000000000000000 ) ) ;
#30456=CARTESIAN_POINT ( 'NONE',  ( 107.5820849072354832, -19.27577136381270151, -3.923241656623378315 ) ) ;
#30458=ORIENTED_EDGE ( 'NONE', *, *, #2458, .F. ) ;
#30461=CARTESIAN_POINT ( 'NONE',  ( -1.397981246020602697, -14.12199645988578212, 1.500000000000000444 ) ) ;
#30463=CARTESIAN_POINT ( 'NONE',  ( 108.0618756673665501, -18.96035633396743592, -4.492382516429220374 ) ) ;
#30473=CARTESIAN_POINT ( 'NONE',  ( -14.62340757463330654, -21.93932300455827900, -1.000000000000000000 ) ) ;
#30476=VERTEX_POINT ( 'NONE', #24089 ) ;
#30481=B_SPLINE_CURVE_WITH_KNOTS ( 'NONE', 3,
 ( #8366, #28755, #1007, #31438, #18418, #13540, #11190, #20911, #10697, #21397, #6189, #13063, #21092, #3539, #28444, #5844, #3374, #13358, #31293, #26092, #28921, #28609, #8693, #26440, #5554, #18562, #11040, #21240, #6026, #25770, #23569, #23264 ),
 .UNSPECIFIED., .F., .F.,
 ( 4, 2, 2, 2, 2, 2, 2, 2, 2, 2, 2, 2, 2, 2, 2, 4 ),
 ( 0.001762511593127062031, 0.004900820851275785282, 0.008039130109424507883, 0.01117743936757322962, 0.01274659399664759482, 0.01353117131118477742, 0.01431574862572196176, 0.01588490325479632870, 0.01666948056933351824, 0.01745405788387070084, 0.01823863519840788344, 0.01902321251294506951, 0.02059236714201943125, 0.02216152177109378951, 0.02373067640016815125, 0.02686898565831688165 ),
 .UNSPECIFIED. ) ;
#30482=ADVANCED_FACE ( 'NONE', ( #18595 ), #23611, .T. ) ;
#30484=AXIS2_PLACEMENT_3D ( 'NONE', #11868, #32102, #16877 ) ;
#30491=EDGE_CURVE ( 'NONE', #13510, #18680, #7311, .T. ) ;
#30494=AXIS2_PLACEMENT_3D ( 'NONE', #12140, #9967, #17644 ) ;
#30495=ORIENTED_EDGE ( 'NONE', *, *, #9566, .T. ) ;
#30496=CARTESIAN_POINT ( 'NONE',  ( 107.4616526958865705, -17.52838469296580826, 4.846942987312949924 ) ) ;
#30497=FACE_OUTER_BOUND ( 'NONE', #4437, .T. ) ;
#30508=CARTESIAN_POINT ( 'NONE',  ( 22.90158751868999332, -21.92087667321502309, -1.135468510342512394 ) ) ;
#30512=ADVANCED_FACE ( 'NONE', ( #16559, #26467 ), #21125, .F. ) ;
#30514=DIRECTION ( 'NONE',  ( -1.000000000000000000, 0.000000000000000000, 6.938893903907221278E-15 ) ) ;
#30519=CARTESIAN_POINT ( 'NONE',  ( -3.659776827757759587, -1.633636780108321807, 0.9788672205877712029 ) ) ;
#30531=CARTESIAN_POINT ( 'NONE',  ( 20.53274989849676757, -21.72776571847661842, -1.408906953170802723 ) ) ;
#30546=CARTESIAN_POINT ( 'NONE',  ( -14.62340757463330654, -27.93932300454937590, -1.000000000000000000 ) ) ;
#30556=EDGE_CURVE ( 'NONE', #21890, #17869, #10274, .T. ) ;
#30562=CARTESIAN_POINT ( 'NONE',  ( -50.60000000000000142, -21.43932300454937945, -1.500000000000000000 ) ) ;
#30564=CARTESIAN_POINT ( 'NONE',  ( 24.41148010920957034, -17.42203112336814996, 1.436991846559697361 ) ) ;
#30565=AXIS2_PLACEMENT_3D ( 'NONE', #9289, #19506, #7395 ) ;
#30573=EDGE_LOOP ( 'NONE', ( #22044, #22806, #9985, #11998 ) ) ;
#30575=AXIS2_PLACEMENT_3D ( 'NONE', #29040, #23351, #6131 ) ;
#30580=CARTESIAN_POINT ( 'NONE',  ( 0.4979849626702088639, -4.221418788689684121, 1.765595572481148512 ) ) ;
#30582=VECTOR ( 'NONE', #24713, 1000.000000000000000 ) ;
#30590=ADVANCED_FACE ( 'NONE', ( #1386 ), #17190, .T. ) ;
#30603=CARTESIAN_POINT ( 'NONE',  ( 12.13203477089214388, -15.56659747185076448, -1.754034475440599872 ) ) ;
#30604=CARTESIAN_POINT ( 'NONE',  ( 71.67787245194618606, -18.34520463695562498, 1.500000000000000444 ) ) ;
#30607=DIRECTION ( 'NONE',  ( 0.000000000000000000, 0.000000000000000000, 1.000000000000000000 ) ) ;
#30609=LINE ( 'NONE', #10360, #10208 ) ;
#30612=CARTESIAN_POINT ( 'NONE',  ( 24.40342144122392298, -17.37878489514629265, 1.350270808450722670 ) ) ;
#30615=CARTESIAN_POINT ( 'NONE',  ( 21.62838417909332733, -16.89547707397426279, -1.499999999999863665 ) ) ;
#30620=CARTESIAN_POINT ( 'NONE',  ( 7.541748857011418394, -18.86390992599486438, -1.499999999999761746 ) ) ;
#30628=CARTESIAN_POINT ( 'NONE',  ( 107.8771114573266630, -16.29979767294548409, 1.280413873165804128 ) ) ;
#30642=ORIENTED_EDGE ( 'NONE', *, *, #8833, .F. ) ;
#30644=ADVANCED_FACE ( 'NONE', ( #11716 ), #19937, .F. ) ;
#30646=FACE_OUTER_BOUND ( 'NONE', #4815, .T. ) ;
#30653=CARTESIAN_POINT ( 'NONE',  ( 107.5756344652065621, -19.18288839493439468, 4.113624156228013362 ) ) ;
#30654=CARTESIAN_POINT ( 'NONE',  ( -1.033057378353323452, -8.048844657540879410, 4.522129901861156931 ) ) ;
#30656=CARTESIAN_POINT ( 'NONE',  ( -2.938323964970641633, -11.64395169159722521, 1.499999999999919620 ) ) ;
#30664=CIRCLE ( 'NONE', #3957, 0.4499999999999990119 ) ;
#30665=VECTOR ( 'NONE', #26558, 1000.000000000000000 ) ;
#30677=CIRCLE ( 'NONE', #22635, 5.000000000000000888 ) ;
#30681=CARTESIAN_POINT ( 'NONE',  ( 41.92799935455844462, -21.01937708447562159, -4.522129901861164925 ) ) ;
#30683=ADVANCED_FACE ( 'NONE', ( #14728 ), #4709, .T. ) ;
#30687=CARTESIAN_POINT ( 'NONE',  ( 107.4934547166204624, -17.99061096458791198, 5.137745733581649432 ) ) ;
#30695=ORIENTED_EDGE ( 'NONE', *, *, #3420, .F. ) ;
#30719=VERTEX_POINT ( 'NONE', #29948 ) ;
#30727=CARTESIAN_POINT ( 'NONE',  ( 6.655951778521610684, -18.71196003547629516, -1.499999999999999556 ) ) ;
#30730=CARTESIAN_POINT ( 'NONE',  ( 7.720912629997967791, -18.80905748744269701, 1.749363945344754478 ) ) ;
#30731=EDGE_LOOP ( 'NONE', ( #27560, #7085, #2249, #4336, #3075 ) ) ;
#30734=ORIENTED_EDGE ( 'NONE', *, *, #25903, .F. ) ;
#30735=DIRECTION ( 'NONE',  ( 0.1908089953765452762, -0.000000000000000000, -0.9816271834476639757 ) ) ;
#30737=CARTESIAN_POINT ( 'NONE',  ( 108.0350161675694238, -18.57358621869218140, 4.153351887601565373 ) ) ;
#30741=CARTESIAN_POINT ( 'NONE',  ( 0.000000000000000000, 0.000000000000000000, 1.500000000000000000 ) ) ;
#30746=CARTESIAN_POINT ( 'NONE',  ( 24.75456913062235031, -17.48748849332650579, 1.499999999999906075 ) ) ;
#30756=CARTESIAN_POINT ( 'NONE',  ( 9.360049167875386544, -11.53021799246641343, 1.000000000000000000 ) ) ;
#30766=CARTESIAN_POINT ( 'NONE',  ( 25.52557118915447987, -17.56218954043521663, -1.000000000000000444 ) ) ;
#30779=CARTESIAN_POINT ( 'NONE',  ( -29.24402871571405882, -25.93932300454937945, 11.00000000000000000 ) ) ;
#30806=CARTESIAN_POINT ( 'NONE',  ( -3.889464452585704723, -3.181828567483031112, -1.500000000000000000 ) ) ;
#30814=CARTESIAN_POINT ( 'NONE',  ( -3.674210872405168082, -10.80251965388255364, 1.499999999999999112 ) ) ;
#30817=CARTESIAN_POINT ( 'NONE',  ( 21.08401840680096129, -16.78474387324269657, -1.500000000000000000 ) ) ;
#30826=EDGE_CURVE ( 'NONE', #18318, #29863, #21639, .T. ) ;
#30832=CARTESIAN_POINT ( 'NONE',  ( 107.5306748766070939, -18.53203061720905254, -5.070947615523107466 ) ) ;
#30837=CARTESIAN_POINT ( 'NONE',  ( 0.8174570305809125692, -9.170357625429589987, -1.500000000000000444 ) ) ;
#30844=ORIENTED_EDGE ( 'NONE', *, *, #18537, .F. ) ;
#30849=CARTESIAN_POINT ( 'NONE',  ( 1.305960519821096844, -9.941484022874826465, 1.500000000000000000 ) ) ;
#30867=ORIENTED_EDGE ( 'NONE', *, *, #20793, .T. ) ;
#30870=FACE_OUTER_BOUND ( 'NONE', #30260, .T. ) ;
#30877=CARTESIAN_POINT ( 'NONE',  ( -4.317168503051449946, -7.715934794172482292, -1.499999999999999556 ) ) ;
#30880=CARTESIAN_POINT ( 'NONE',  ( -2.940647560480709188, -11.38358483011127120, 1.743664474335998582 ) ) ;
#30896=CARTESIAN_POINT ( 'NONE',  ( 21.03177542174473658, -17.18603084754145982, -1.753176640694677380 ) ) ;
#30906=CARTESIAN_POINT ( 'NONE',  ( 7.931701155948623239, -9.929036424222896784, 1.000000000000000000 ) ) ;
#30918=CARTESIAN_POINT ( 'NONE',  ( 107.5617944031221640, -18.98359742639815551, -4.522129901861166701 ) ) ;
#30920=CARTESIAN_POINT ( 'NONE',  ( 9.096376384877638444, -0.1528062924499160868, 1.364612494264895837 ) ) ;
#30922=CARTESIAN_POINT ( 'NONE',  ( 0.5859972064454824769, -5.135271408404158855, 0.9788672205888330202 ) ) ;
#30927=ORIENTED_EDGE ( 'NONE', *, *, #22373, .F. ) ;
#30939=CARTESIAN_POINT ( 'NONE',  ( -50.60000000000000142, -10.96966150227468972, -1.000000000000000000 ) ) ;
#30958=CARTESIAN_POINT ( 'NONE',  ( -3.176043528763360602, -11.78095770713099277, 1.499999999999999556 ) ) ;
#30962=CARTESIAN_POINT ( 'NONE',  ( 107.6641948605228123, -20.45809826282219746, -1.499999999999999556 ) ) ;
#30971=CARTESIAN_POINT ( 'NONE',  ( -3.105859910357408271, -0.009789559233441965172, -1.118159719381818018 ) ) ;
#30973=DIRECTION ( 'NONE',  ( -0.8571673007021120005, 1.049727191138618326E-16, 0.5150380749100547106 ) ) ;
#30982=CARTESIAN_POINT ( 'NONE',  ( 107.9493749606654234, -17.34037414412194877, 4.559070180965012042 ) ) ;
#30983=ORIENTED_EDGE ( 'NONE', *, *, #18889, .F. ) ;
#30987=CARTESIAN_POINT ( 'NONE',  ( 24.38302348701595079, -17.39153354041035726, 1.380603655064675861 ) ) ;
#30998=CARTESIAN_POINT ( 'NONE',  ( 0.6630161036174202493, -9.073167597564687270, -1.769313562487350611 ) ) ;
#30999=CARTESIAN_POINT ( 'NONE',  ( 21.65220420020125758, -21.84595744892894231, -1.292937544721162402 ) ) ;
#31000=CARTESIAN_POINT ( 'NONE',  ( 107.9128139062042919, -20.39012166861468600, -1.488290602270338159 ) ) ;
#31002=CARTESIAN_POINT ( 'NONE',  ( 107.8806307222008627, -16.35047421165092985, 1.384330804614037236 ) ) ;
#31010=EDGE_LOOP ( 'NONE', ( #103, #7006, #13981, #28469 ) ) ;
#31012=CIRCLE ( 'NONE', #7507, 0.5000000000000004441 ) ;
#31025=AXIS2_PLACEMENT_3D ( 'NONE', #9704, #9881, #15041 ) ;
#31028=ADVANCED_FACE ( 'NONE', ( #19552 ), #29750, .T. ) ;
#31031=ORIENTED_EDGE ( 'NONE', *, *, #27235, .F. ) ;
#31039=CIRCLE ( 'NONE', #27816, 4.999999999999997335 ) ;
#31050=CARTESIAN_POINT ( 'NONE',  ( 0.1517578099453120721, -1.375880305419411309, -4.522129901861164925 ) ) ;
#31053=CARTESIAN_POINT ( 'NONE',  ( 24.49428966819754194, -17.44778713273094084, 1.472392441597068613 ) ) ;
#31054=CARTESIAN_POINT ( 'NONE',  ( 22.16007320322699314, -17.32365168620639650, -1.743368838329845572 ) ) ;
#31063=CARTESIAN_POINT ( 'NONE',  ( 23.01404055077173183, -17.34213939868515553, 1.500000000000000000 ) ) ;
#31071=CARTESIAN_POINT ( 'NONE',  ( 2.386646147131364248, -0.3554301312245131683, 1.500000000000000000 ) ) ;
#31074=VECTOR ( 'NONE', #553, 999.9999999999998863 ) ;
#31087=CARTESIAN_POINT ( 'NONE',  ( 2.117172266158205751, -1.242920418748529432, 0.9788672205888330202 ) ) ;
#31088=ORIENTED_EDGE ( 'NONE', *, *, #12794, .T. ) ;
#31102=CARTESIAN_POINT ( 'NONE',  ( 24.35832023931602208, -17.33818253687209676, 1.317734466820223549 ) ) ;
#31115=CIRCLE ( 'NONE', #16668, 0.5000000000000000000 ) ;
#31118=ORIENTED_EDGE ( 'NONE', *, *, #25129, .F. ) ;
#31122=CARTESIAN_POINT ( 'NONE',  ( 10.39650919157949893, -12.30877965038158450, -1.000000000000000000 ) ) ;
#31140=CARTESIAN_POINT ( 'NONE',  ( -4.272725277965156110, -6.149870187536970789, 1.499999999999759304 ) ) ;
#31142=CARTESIAN_POINT ( 'NONE',  ( 44.05836296525849605, -19.40445080606635386, 1.499999999999999778 ) ) ;
#31143=SPHERICAL_SURFACE ( 'NONE', #17094, 0.5000000000000000000 ) ;
#31148=CARTESIAN_POINT ( 'NONE',  ( -13.84999999999999964, -10.96966150227469505, -1.499999999999999556 ) ) ;
#31156=CARTESIAN_POINT ( 'NONE',  ( 107.9988851051869716, -18.05330790866155510, 4.637841734569910557 ) ) ;
#31163=CARTESIAN_POINT ( 'NONE',  ( 107.4499696397440545, -17.35889446679003356, 4.518584177339137753 ) ) ;
#31171=CIRCLE ( 'NONE', #2338, 0.5000000000000005551 ) ;
#31174=EDGE_LOOP ( 'NONE', ( #3922, #579, #9037, #8949, #15046 ) ) ;
#31183=CARTESIAN_POINT ( 'NONE',  ( -2.762625878986976868, -11.69560895226267228, -1.743724257656045662 ) ) ;
#31187=CARTESIAN_POINT ( 'NONE',  ( 107.9803609742689900, -17.78656503166756764, -4.329962501461942281 ) ) ;
#31189=DIRECTION ( 'NONE',  ( -0.000000000000000000, 0.000000000000000000, 1.000000000000000000 ) ) ;
#31190=CARTESIAN_POINT ( 'NONE',  ( 2.632061376486628301, -0.5000000000000000000, 1.500000000000000000 ) ) ;
#31192=CARTESIAN_POINT ( 'NONE',  ( -1.921189184902823754, -10.44034746380417467, 4.522129901861158707 ) ) ;
#31193=CARTESIAN_POINT ( 'NONE',  ( 3.066081126419192504, 0.08824576070981422771, 0.7648597189984532863 ) ) ;
#31194=( BOUNDED_SURFACE ( )  B_SPLINE_SURFACE ( 3, 2, ( 
 ( #25141, #17457, #2090 ),
 ( #27655, #22313, #27818 ),
 ( #32524, #4760, #30017 ),
 ( #9588, #14933, #19807 ) ),
 .UNSPECIFIED., .F., .F., .F. ) 
 B_SPLINE_SURFACE_WITH_KNOTS ( ( 4, 4 ),
 ( 3, 3 ),
 ( 0.004009623062827070289, 0.007419693412580972633 ),
 ( 0.000000000000000000, 1.000000000000000000 ),
 .UNSPECIFIED. ) 
 GEOMETRIC_REPRESENTATION_ITEM ( )  RATIONAL_B_SPLINE_SURFACE ( (
 ( 1.000000000000000000, 0.7074525376967367718, 1.000000000000000000),
 ( 1.000000000000000000, 0.7074519917808602676, 1.000000000000000000),
 ( 1.000000000000000000, 0.7074511013184006103, 1.000000000000000000),
 ( 1.000000000000000000, 0.7074498840443311787, 1.000000000000000000) ) ) 
 REPRESENTATION_ITEM ( '' )  SURFACE ( )  );
#31197=CIRCLE ( 'NONE', #22636, 0.5000000000000004441 ) ;
#31206=CARTESIAN_POINT ( 'NONE',  ( 20.03174988220904496, -21.67712946496369497, -1.441661034764752936 ) ) ;
#31214=ORIENTED_EDGE ( 'NONE', *, *, #28290, .F. ) ;
#31215=ORIENTED_EDGE ( 'NONE', *, *, #14071, .T. ) ;
#31223=CARTESIAN_POINT ( 'NONE',  ( 108.0656705835203297, -19.01500218252613550, 3.248569211028260018 ) ) ;
#31233=CARTESIAN_POINT ( 'NONE',  ( 24.65791283128423927, -17.47550391090821265, 1.495278912112739889 ) ) ;
#31237=EDGE_CURVE ( 'NONE', #20422, #10617, #26038, .T. ) ;
#31245=CARTESIAN_POINT ( 'NONE',  ( 12.29359089006352335, -13.32350401977120313, 1.500000000000832445 ) ) ;
#31246=ORIENTED_EDGE ( 'NONE', *, *, #17976, .T. ) ;
#31249=CARTESIAN_POINT ( 'NONE',  ( 0.8233106589072967108, -3.227070907846791403, 1.762270114843585533 ) ) ;
#31252=EDGE_CURVE ( 'NONE', #30476, #17825, #15245, .T. ) ;
#31264=LINE ( 'NONE', #10514, #11258 ) ;
#31266=ORIENTED_EDGE ( 'NONE', *, *, #31560, .T. ) ;
#31271=CARTESIAN_POINT ( 'NONE',  ( 25.36142496378537814, -17.53025290272828585, 1.090880951025948953 ) ) ;
#31272=DIRECTION ( 'NONE',  ( -0.000000000000000000, 0.000000000000000000, 1.000000000000000000 ) ) ;
#31280=ORIENTED_EDGE ( 'NONE', *, *, #13580, .F. ) ;
#31285=CARTESIAN_POINT ( 'NONE',  ( -13.84999999999999964, -10.96966150227469505, -1.499999999999999556 ) ) ;
#31289=VERTEX_POINT ( 'NONE', #23969 ) ;
#31293=CARTESIAN_POINT ( 'NONE',  ( 7.429379966294792581, -10.00822258298154388, 1.500000000000000000 ) ) ;
#31297=EDGE_LOOP ( 'NONE', ( #29007, #32265, #30452, #22956 ) ) ;
#31302=CARTESIAN_POINT ( 'NONE',  ( 3.660726896358641014, -5.717472393966525748E-18, 1.077884872112069514 ) ) ;
#31308=CARTESIAN_POINT ( 'NONE',  ( 24.95054824997649590, -17.50694965296897365, 1.454185466667848869 ) ) ;
#31309=CARTESIAN_POINT ( 'NONE',  ( -15.12340757463330476, -28.43932300454937590, -1.000000000000000000 ) ) ;
#31310=CARTESIAN_POINT ( 'NONE',  ( -2.785986023666280786, -0.02407431902641572752, -1.185596063490282015 ) ) ;
#31314=ORIENTED_EDGE ( 'NONE', *, *, #18151, .T. ) ;
#31315=CARTESIAN_POINT ( 'NONE',  ( 17.39502519978884010, -21.04076415203780215, 1.751145182513948129 ) ) ;
#31316=CARTESIAN_POINT ( 'NONE',  ( -3.115565086446475895, -0.007767237976396394912, -1.107297703164631608 ) ) ;
#31319=CARTESIAN_POINT ( 'NONE',  ( 107.9496392939063298, -17.34418047704120269, 4.568272308424636385 ) ) ;
#31320=VERTEX_POINT ( 'NONE', #474 ) ;
#31326=ORIENTED_EDGE ( 'NONE', *, *, #6966, .T. ) ;
#31333=CARTESIAN_POINT ( 'NONE',  ( -0.1873139951646253798, -14.67771805109925332, -1.745313736529866100 ) ) ;
#31336=CARTESIAN_POINT ( 'NONE',  ( 107.9482084786819343, -17.32357709375119015, -4.515156556222997608 ) ) ;
#31339=CARTESIAN_POINT ( 'NONE',  ( 4.129189561419488896, -11.96871115988036394, 1.500000000000000888 ) ) ;
#31340=LINE ( 'NONE', #18612, #29077 ) ;
#31342=CARTESIAN_POINT ( 'NONE',  ( -1.218076164763124636, -14.00532792343563848, 1.500000000000000000 ) ) ;
#31343=FACE_OUTER_BOUND ( 'NONE', #20662, .T. ) ;
#31345=CARTESIAN_POINT ( 'NONE',  ( -29.24402871571405882, -27.93932300454937590, 11.00000000000000000 ) ) ;
#31354=CARTESIAN_POINT ( 'NONE',  ( 0.7531256266104227048, -8.135089508258609214, -1.499999999999999778 ) ) ;
#31357=CARTESIAN_POINT ( 'NONE',  ( 107.6641948605228123, -20.45809826282219746, -1.499999999999999556 ) ) ;
#31360=CARTESIAN_POINT ( 'NONE',  ( 14.21659522551972010, -20.98447794504473762, -0.9788672205760856615 ) ) ;
#31364=ORIENTED_EDGE ( 'NONE', *, *, #31252, .T. ) ;
#31371=CARTESIAN_POINT ( 'NONE',  ( 25.56776753627337229, -17.11417227705151589, -0.9999999999999993339 ) ) ;
#31372=CARTESIAN_POINT ( 'NONE',  ( 107.5611841629995098, -18.97506626684318931, 4.544690123031810636 ) ) ;
#31376=EDGE_CURVE ( 'NONE', #15578, #16944, #27623, .T. ) ;
#31383=CARTESIAN_POINT ( 'NONE',  ( 22.01492382911872880, -21.80158502930289544, 1.372788961212862313 ) ) ;
#31384=DIRECTION ( 'NONE',  ( -1.000000000000000000, 0.000000000000000000, 0.000000000000000000 ) ) ;
#31390=CARTESIAN_POINT ( 'NONE',  ( 8.103242287716968306, -10.98376420866808978, 1.500000000000000000 ) ) ;
#31400=CARTESIAN_POINT ( 'NONE',  ( 107.8192447519188306, -18.91582588990454639, -4.500896179815041087 ) ) ;
#31415=CARTESIAN_POINT ( 'NONE',  ( 0.5220033361344494915, 0.000000000000000000, 5.485967528433933538 ) ) ;
#31428=EDGE_CURVE ( 'NONE', #993, #12444, #29834, .T. ) ;
#31430=CARTESIAN_POINT ( 'NONE',  ( 8.099355570077825917, -10.14921976342372467, -1.000000000000000000 ) ) ;
#31431=ORIENTED_EDGE ( 'NONE', *, *, #6609, .T. ) ;
#31438=CARTESIAN_POINT ( 'NONE',  ( 17.05941372759280483, -15.60161612857925739, 1.500000000000000222 ) ) ;
#31439=CARTESIAN_POINT ( 'NONE',  ( 0.3844419896858671248, -5.169620074766034357, -1.500000000000035083 ) ) ;
#31444=CARTESIAN_POINT ( 'NONE',  ( -5.304000690461529555E-12, -21.43932300456189566, 1.000000000000000000 ) ) ;
#31449=EDGE_CURVE ( 'NONE', #26510, #21433, #3834, .T. ) ;
#31461=CARTESIAN_POINT ( 'NONE',  ( 20.05745782660446608, -21.55152848446436309, 1.510982242220422433 ) ) ;
#31465=CARTESIAN_POINT ( 'NONE',  ( 108.0106719622584848, -18.22303571829002422, 4.627257122494635055 ) ) ;
#31466=ORIENTED_EDGE ( 'NONE', *, *, #2443, .F. ) ;
#31479=CARTESIAN_POINT ( 'NONE',  ( -1.487278458322581098, -13.44708787814461637, -1.744337816817864262 ) ) ;
#31482=CARTESIAN_POINT ( 'NONE',  ( 9.851448552575103434, -11.91728849018499581, -1.000000000000000000 ) ) ;
#31487=CIRCLE ( 'NONE', #26142, 0.4499999999999990119 ) ;
#31489=LINE ( 'NONE', #9905, #21622 ) ;
#31491=CARTESIAN_POINT ( 'NONE',  ( 2.748213864407174079, 0.2993382933193597939, 1.561876010259294789 ) ) ;
#31500=CARTESIAN_POINT ( 'NONE',  ( 18.06290729145209184, -21.14813556147793605, 1.751201132231453572 ) ) ;
#31502=CARTESIAN_POINT ( 'NONE',  ( 0.8194515883087264418, -4.592504314968420154, -1.499999999999999334 ) ) ;
#31506=CARTESIAN_POINT ( 'NONE',  ( 25.52557090713695231, -17.56218951387349492, -1.057622280107180845 ) ) ;
#31512=B_SPLINE_CURVE_WITH_KNOTS ( 'NONE', 3,
 ( #28592, #18398, #13339, #8673, #18891, #19043, #26074, #16358, #29235, #23551 ),
 .UNSPECIFIED., .F., .F.,
 ( 4, 2, 2, 2, 4 ),
 ( 0.000000000000000000, 0.0003394344854501923632, 0.0006788689709003847264, 0.001018303456350577035, 0.001357737941800769453 ),
 .UNSPECIFIED. ) ;
#31518=ORIENTED_EDGE ( 'NONE', *, *, #20839, .T. ) ;
#31524=CARTESIAN_POINT ( 'NONE',  ( 108.0618741790777193, -18.96033490297902091, 4.492441070042681339 ) ) ;
#31534=CARTESIAN_POINT ( 'NONE',  ( 22.04243029792654340, -21.80478118307064861, 1.499729010651354777 ) ) ;
#31544=CARTESIAN_POINT ( 'NONE',  ( 9.283830569144180700, -0.1241467202002616427, 1.500000000000000000 ) ) ;
#31545=ORIENTED_EDGE ( 'NONE', *, *, #22732, .T. ) ;
#31548=CARTESIAN_POINT ( 'NONE',  ( 3.708020185722930240, -12.03545600470719279, 1.500000000000000666 ) ) ;
#31558=CARTESIAN_POINT ( 'NONE',  ( 24.16865442153064691, -17.43004354390603083, -1.504494863253570403 ) ) ;
#31560=EDGE_CURVE ( 'NONE', #9323, #8122, #13246, .T. ) ;
#31572=CARTESIAN_POINT ( 'NONE',  ( 108.0291781248179177, -18.48951985539285658, 4.325670280512381005 ) ) ;
#31575=CARTESIAN_POINT ( 'NONE',  ( 3.551765900376501861, -15.35947713381495383, 5.485967528433935314 ) ) ;
#31578=ORIENTED_EDGE ( 'NONE', *, *, #32659, .T. ) ;
#31584=( BOUNDED_SURFACE ( )  B_SPLINE_SURFACE ( 3, 2, ( 
 ( #16831, #26686, #13798 ),
 ( #31740, #21686, #3802 ),
 ( #21531, #23859, #6638 ),
 ( #3984, #13970, #24190 ),
 ( #9303, #8817, #29206 ),
 ( #24497, #11490, #8958 ),
 ( #22017, #13655, #21348 ),
 ( #6452, #16657, #14153 ),
 ( #31558, #24351, #966 ),
 ( #32049, #27031, #4132 ),
 ( #1616, #11147, #11810 ),
 ( #19519, #29868, #25178 ) ),
 .UNSPECIFIED., .F., .F., .F. ) 
 B_SPLINE_SURFACE_WITH_KNOTS ( ( 4, 2, 2, 2, 2, 4 ),
 ( 3, 3 ),
 ( 0.02103335055024949107, 0.02276256425196081928, 0.02362717110281648339, 0.02405947452824431371, 0.02427562624095823060, 0.02449177795367214749 ),
 ( 0.000000000000000000, 1.000000000000000000 ),
 .UNSPECIFIED. ) 
 GEOMETRIC_REPRESENTATION_ITEM ( )  RATIONAL_B_SPLINE_SURFACE ( (
 ( 1.000000000000000000, 0.8477574071936589961, 1.000000000000000000),
 ( 1.000000000000000000, 0.8716452794063324072, 1.000000000000000000),
 ( 1.000000000000000000, 0.8956763213344164365, 1.000000000000000000),
 ( 1.000000000000000000, 0.9319482906208321760, 1.000000000000000000),
 ( 1.000000000000000000, 0.9440737053932664047, 1.000000000000000000),
 ( 1.000000000000000000, 0.9620964665818899642, 1.000000000000000000),
 ( 1.000000000000000000, 0.9681025352174974508, 1.000000000000000000),
 ( 1.000000000000000000, 0.9768916256376188878, 1.000000000000000000),
 ( 1.000000000000000000, 0.9797842808059200603, 1.000000000000000000),
 ( 1.000000000000000000, 0.9854258872291279392, 1.000000000000000000),
 ( 1.000000000000000000, 0.9882007853475626158, 1.000000000000000000),
 ( 1.000000000000000000, 0.9906937806494816590, 1.000000000000000000) ) ) 
 REPRESENTATION_ITEM ( '' )  SURFACE ( )  );
#31586=CARTESIAN_POINT ( 'NONE',  ( 107.9095081641845582, -17.54872683406297540, -4.428332375768106566 ) ) ;
#31596=CARTESIAN_POINT ( 'NONE',  ( 7.778677572338311030, -9.608974357934672028, -1.000000000000000222 ) ) ;
#31608=DIRECTION ( 'NONE',  ( 1.000000000000000000, 0.000000000000000000, 0.000000000000000000 ) ) ;
#31623=DIRECTION ( 'NONE',  ( 1.000000000000000000, 0.000000000000000000, 0.000000000000000000 ) ) ;
#31624=CARTESIAN_POINT ( 'NONE',  ( -4.524729257728259846, -7.612611013041808761, -1.499999999999999556 ) ) ;
#31630=DIRECTION ( 'NONE',  ( -0.000000000000000000, 0.000000000000000000, 1.000000000000000000 ) ) ;
#31636=CARTESIAN_POINT ( 'NONE',  ( 18.70218739253826357, -21.34730519116122949, 1.543632415228167076 ) ) ;
#31641=DIRECTION ( 'NONE',  ( 1.000000000000000000, 0.000000000000000000, 0.000000000000000000 ) ) ;
#31647=VERTEX_POINT ( 'NONE', #26306 ) ;
#31648=CARTESIAN_POINT ( 'NONE',  ( -14.47914180357919989, -27.93932300454937590, -4.314460059828594041 ) ) ;
#31649=CARTESIAN_POINT ( 'NONE',  ( 24.39659513448239991, -17.41072360183627055, 1.416990234759656575 ) ) ;
#31663=CARTESIAN_POINT ( 'NONE',  ( 9.360049168479326553, -11.53021799169701112, -1.500000000000000000 ) ) ;
#31664=CARTESIAN_POINT ( 'NONE',  ( 107.9203180492143588, -16.92196184768069145, -2.556177043345751798 ) ) ;
#31666=AXIS2_PLACEMENT_3D ( 'NONE', #18582, #13559, #26110 ) ;
#31669=( BOUNDED_SURFACE ( )  B_SPLINE_SURFACE ( 3, 2, ( 
 ( #26919, #31783, #6028 ),
 ( #16712, #16526, #21093 ),
 ( #16222, #3376, #11191 ),
 ( #23751, #13844, #3854 ),
 ( #16030, #8367, #3686 ),
 ( #8854, #21727, #10885 ),
 ( #695, #11042, #24239 ),
 ( #21241, #31439, #18718 ),
 ( #16374, #28923, #26441 ),
 ( #13698, #21398, #8695 ),
 ( #24052, #4342, #14844 ),
 ( #32440, #2008, #30112 ),
 ( #14698, #2161, #30265 ),
 ( #22230, #24896, #12035 ),
 ( #32779, #29601, #22381 ),
 ( #7337, #9173, #9857 ),
 ( #14191, #32597, #29915 ),
 ( #19559, #6684, #16873 ),
 ( #20069, #24389, #6836 ),
 ( #1858, #9501, #22072 ),
 ( #17211, #4171, #32098 ),
 ( #1506, #14522, #24544 ),
 ( #9670, #12345, #17527 ),
 ( #11684, #19403, #27227 ),
 ( #1668, #27069, #17381 ),
 ( #19716, #12181, #7188 ),
 ( #19898, #22565, #4024 ),
 ( #6998, #27575, #27417 ),
 ( #21882, #14338, #4674 ),
 ( #11863, #32288, #9349 ),
 ( #29756, #25043, #4523 ),
 ( #17021, #24733, #170 ),
 ( #30603, #2856, #12831 ),
 ( #25726, #33086, #2511 ),
 ( #15010, #4829, #13025 ),
 ( #25232, #20384, #27908 ),
 ( #28226, #10509, #7996 ),
 ( #2352, #12527, #5331 ) ),
 .UNSPECIFIED., .F., .F., .F. ) 
 B_SPLINE_SURFACE_WITH_KNOTS ( ( 4, 2, 2, 2, 2, 2, 2, 2, 2, 2, 2, 2, 2, 2, 2, 2, 2, 2, 4 ),
 ( 3, 3 ),
 ( 0.000000000000000000, 0.001918043520347785828, 0.003836087040695571656, 0.004795108800869464678, 0.005754130561043357267, 0.006713152321217250723, 0.007192663201304197451, 0.007672174081391143312, 0.008631195841565035901, 0.009590217601738929357, 0.01150826112208671453, 0.01246728288226060799, 0.01342630464243450145, 0.01534434816278228662, 0.01726239168313007180, 0.01918043520347785871, 0.02301652224417342907, 0.02685260928486900289, 0.03068869632556457325 ),
 ( 0.000000000000000000, 1.000000000000000000 ),
 .UNSPECIFIED. ) 
 GEOMETRIC_REPRESENTATION_ITEM ( )  RATIONAL_B_SPLINE_SURFACE ( (
 ( 1.000000000000000000, 0.8449619147701439292, 1.000000000000000000),
 ( 1.000000000000000000, 0.8445678029926584340, 1.000000000000000000),
 ( 1.000000000000000000, 0.8440734858009981689, 1.000000000000000000),
 ( 1.000000000000000000, 0.8426715424874036131, 1.000000000000000000),
 ( 1.000000000000000000, 0.8417777985993892820, 1.000000000000000000),
 ( 1.000000000000000000, 0.8396981493403768981, 1.000000000000000000),
 ( 1.000000000000000000, 0.8389573580692519794, 1.000000000000000000),
 ( 1.000000000000000000, 0.8374408369630492732, 1.000000000000000000),
 ( 1.000000000000000000, 0.8366690632723572385, 1.000000000000000000),
 ( 1.000000000000000000, 0.8350101717998674733, 1.000000000000000000),
 ( 1.000000000000000000, 0.8340755910242153570, 1.000000000000000000),
 ( 1.000000000000000000, 0.8336678922694548133, 1.000000000000000000),
 ( 1.000000000000000000, 0.8336623316996139010, 1.000000000000000000),
 ( 1.000000000000000000, 0.8338837348179357623, 1.000000000000000000),
 ( 1.000000000000000000, 0.8341121628413028510, 1.000000000000000000),
 ( 1.000000000000000000, 0.8349642705193365266, 1.000000000000000000),
 ( 1.000000000000000000, 0.8357234841175039675, 1.000000000000000000),
 ( 1.000000000000000000, 0.8375342318403898867, 1.000000000000000000),
 ( 1.000000000000000000, 0.8383883957943909504, 1.000000000000000000),
 ( 1.000000000000000000, 0.8406684190711074534, 1.000000000000000000),
 ( 1.000000000000000000, 0.8419347305613049670, 1.000000000000000000),
 ( 1.000000000000000000, 0.8434083992945078379, 1.000000000000000000),
 ( 1.000000000000000000, 0.8438015669660346996, 1.000000000000000000),
 ( 1.000000000000000000, 0.8444527818707109335, 1.000000000000000000),
 ( 1.000000000000000000, 0.8447125394710991442, 1.000000000000000000),
 ( 1.000000000000000000, 0.8453649836267845830, 1.000000000000000000),
 ( 1.000000000000000000, 0.8456341134025172623, 1.000000000000000000),
 ( 1.000000000000000000, 0.8460541031445641957, 1.000000000000000000),
 ( 1.000000000000000000, 0.8462025651636095880, 1.000000000000000000),
 ( 1.000000000000000000, 0.8464941699322370283, 1.000000000000000000),
 ( 1.000000000000000000, 0.8466725352208778199, 1.000000000000000000),
 ( 1.000000000000000000, 0.8470349366253309142, 1.000000000000000000),
 ( 1.000000000000000000, 0.8471950700188056738, 1.000000000000000000),
 ( 1.000000000000000000, 0.8474407502799835568, 1.000000000000000000),
 ( 1.000000000000000000, 0.8475244277276142713, 1.000000000000000000),
 ( 1.000000000000000000, 0.8476586531197746188, 1.000000000000000000),
 ( 1.000000000000000000, 0.8477086645732269110, 1.000000000000000000),
 ( 1.000000000000000000, 0.8477574071928573041, 1.000000000000000000) ) ) 
 REPRESENTATION_ITEM ( '' )  SURFACE ( )  );
#31672=DIRECTION ( 'NONE',  ( 1.000000000000000000, 0.000000000000000000, 0.000000000000000000 ) ) ;
#31676=VERTEX_POINT ( 'NONE', #11233 ) ;
#31678=B_SPLINE_CURVE_WITH_KNOTS ( 'NONE', 3,
 ( #13551, #5713, #16039, #26102, #13706, #20923, #21585, #18428, #871, #21249 ),
 .UNSPECIFIED., .F., .F.,
 ( 4, 2, 2, 2, 4 ),
 ( -0.0002335416784056200705, 0.0001933787568668222175, 0.0006202991921392645054, 0.001474140062684159598, 0.003181821803773939375 ),
 .UNSPECIFIED. ) ;
#31685=CARTESIAN_POINT ( 'NONE',  ( 21.20754276729287469, -21.72113672149310304, 1.466027919133091384 ) ) ;
#31697=EDGE_LOOP ( 'NONE', ( #2431, #10117, #23176, #15917 ) ) ;
#31701=CARTESIAN_POINT ( 'NONE',  ( -2.386718424894567203, -9.330009425478154483, 4.522129901861158707 ) ) ;
#31709=CARTESIAN_POINT ( 'NONE',  ( 108.0291954987227712, -18.48977003530059804, 4.324986740352072090 ) ) ;
#31710=EDGE_CURVE ( 'NONE', #24312, #22183, #13219, .T. ) ;
#31713=CARTESIAN_POINT ( 'NONE',  ( -0.7739934281325310250, -8.972773999336027373, -4.522129901861164925 ) ) ;
#31718=CARTESIAN_POINT ( 'NONE',  ( -50.60000000000000142, -10.96966150227468972, 6.999999999999999112 ) ) ;
#31723=FACE_OUTER_BOUND ( 'NONE', #7800, .T. ) ;
#31730=CARTESIAN_POINT ( 'NONE',  ( 7.166310627377590059, -7.340520188496220122, 1.499999999999999112 ) ) ;
#31732=CARTESIAN_POINT ( 'NONE',  ( 8.045354371110279956, -1.465502149859512881, -1.500000000000000000 ) ) ;
#31734=ORIENTED_EDGE ( 'NONE', *, *, #16934, .T. ) ;
#31735=CARTESIAN_POINT ( 'NONE',  ( 0.7549893952831980837, -8.141048257043983938, 1.499999999999999556 ) ) ;
#31738=B_SPLINE_CURVE_WITH_KNOTS ( 'NONE', 3,
 ( #3514, #11503, #13670, #29571, #21366, #31572 ),
 .UNSPECIFIED., .F., .F.,
 ( 4, 2, 4 ),
 ( 4.036569264948304377E-14, 0.0003910668831145792121, 0.0007821337661887927100 ),
 .UNSPECIFIED. ) ;
#31740=CARTESIAN_POINT ( 'NONE',  ( 21.60307794872525022, -17.26039173292211970, -1.753143643193426193 ) ) ;
#31746=DIRECTION ( 'NONE',  ( -0.1290991311227714933, -0.9916316928897268568, 0.000000000000000000 ) ) ;
#31756=CARTESIAN_POINT ( 'NONE',  ( 108.1288400433390393, -19.92462668933127290, 1.384270303710046335 ) ) ;
#31757=CARTESIAN_POINT ( 'NONE',  ( -2.461002521556363565, -6.738986457086103776, 5.485967528433935314 ) ) ;
#31759=EDGE_CURVE ( 'NONE', #24872, #1705, #899, .T. ) ;
#31760=CARTESIAN_POINT ( 'NONE',  ( 24.54847674045369743, -17.37474032055271067, 1.294225383761794967 ) ) ;
#31763=CARTESIAN_POINT ( 'NONE',  ( 25.47590240457303423, -17.55751406574353979, -1.147657805880700321 ) ) ;
#31779=ORIENTED_EDGE ( 'NONE', *, *, #25130, .T. ) ;
#31783=CARTESIAN_POINT ( 'NONE',  ( 2.386646147131364692, -0.3554301312245157773, -1.499999999999999112 ) ) ;
#31788=CARTESIAN_POINT ( 'NONE',  ( 7.452958749828057172, -19.12795340808451527, 1.499999999999999112 ) ) ;
#31795=ADVANCED_FACE ( 'NONE', ( #24277 ), #21926, .T. ) ;
#31799=CARTESIAN_POINT ( 'NONE',  ( -4.174600725233243104, -9.415483487261550266, -1.500000000000000000 ) ) ;
#31807=CARTESIAN_POINT ( 'NONE',  ( -31.67864539881508179, -21.93013659627822776, 1.095404497688272194 ) ) ;
#31817=CARTESIAN_POINT ( 'NONE',  ( 107.3993213344157027, -16.62991701035550562, 3.024831839633950636 ) ) ;
#31822=DIRECTION ( 'NONE',  ( 0.9816271834476639757, 0.000000000000000000, -0.1908089953765449709 ) ) ;
#31823=CARTESIAN_POINT ( 'NONE',  ( 13.44509804308993139, -13.81913516398353536, -1.499999999999445111 ) ) ;
#31825=VERTEX_POINT ( 'NONE', #9893 ) ;
#31827=ADVANCED_FACE ( 'NONE', ( #9387 ), #23604, .F. ) ;
#31833=VERTEX_POINT ( 'NONE', #4876 ) ;
#31836=CARTESIAN_POINT ( 'NONE',  ( 107.3679615899517046, -16.17836279666641275, -2.098933649557105596 ) ) ;
#31841=DIRECTION ( 'NONE',  ( 1.000000000000000000, 0.000000000000000000, 0.000000000000000000 ) ) ;
#31843=CARTESIAN_POINT ( 'NONE',  ( 18.52607392133363007, -16.42885517518740457, -1.500000000000000222 ) ) ;
#31859=DIRECTION ( 'NONE',  ( 1.000000000000000000, 0.000000000000000000, 0.000000000000000000 ) ) ;
#31860=CARTESIAN_POINT ( 'NONE',  ( -3.222375984151269357, 0.000000000000000000, 1.000000000000000000 ) ) ;
#31864=CARTESIAN_POINT ( 'NONE',  ( 107.5616947067672129, -18.98247576276246207, 4.525198558126774628 ) ) ;
#31865=CARTESIAN_POINT ( 'NONE',  ( -1.528445841742497535, -6.248157669861958752, -5.485967528433937979 ) ) ;
#31875=EDGE_CURVE ( 'NONE', #11, #30215, #10867, .T. ) ;
#31877=ORIENTED_EDGE ( 'NONE', *, *, #4611, .F. ) ;
#31881=CARTESIAN_POINT ( 'NONE',  ( 8.842484022064880378, 0.1108283380282882452, 1.500000000000000000 ) ) ;
#31883=CARTESIAN_POINT ( 'NONE',  ( 8.970430173840842514, -11.86789775953536363, -1.500000000000000444 ) ) ;
#31886=CARTESIAN_POINT ( 'NONE',  ( 0.6154272894920587156, -5.548424207151230192, 1.500000000000000444 ) ) ;
#31893=B_SPLINE_CURVE_WITH_KNOTS ( 'NONE', 3,
 ( #13227, #5392, #28129, #20933, #15903, #18088, #31156, #18437, #5228, #12898, #5723, #8241, #15579, #26111 ),
 .UNSPECIFIED., .F., .F.,
 ( 4, 2, 2, 2, 2, 2, 4 ),
 ( 8.673617379884035472E-19, 0.0001249476642875234616, 0.0002498953285750460558, 0.0004997906571500799686, 0.0007496859857251137729, 0.0008746336500126335482, 0.0009995813143001532151 ),
 .UNSPECIFIED. ) ;
#31911=CARTESIAN_POINT ( 'NONE',  ( -1.327193056402534710, -8.327227690481549871, 5.485967528433933538 ) ) ;
#31913=B_SPLINE_CURVE_WITH_KNOTS ( 'NONE', 3,
 ( #20178, #2118, #2298, #9304, #9620, #27183 ),
 .UNSPECIFIED., .F., .F.,
 ( 4, 2, 4 ),
 ( 2.626357090645241657E-13, 0.0003954463998646314048, 0.0007908927994666270847 ),
 .UNSPECIFIED. ) ;
#31914=DIRECTION ( 'NONE',  ( 1.000000000000000000, 0.000000000000000000, 0.000000000000000000 ) ) ;
#31924=CARTESIAN_POINT ( 'NONE',  ( -31.18783180709124636, -25.44850941282521006, 1.500000000000000000 ) ) ;
#31942=CARTESIAN_POINT ( 'NONE',  ( 11.75198736701373825, -19.94169323712718978, 1.750535621815488385 ) ) ;
#31945=CARTESIAN_POINT ( 'NONE',  ( 21.64180102898656699, -16.89820628832761784, 1.499999999999856559 ) ) ;
#31947=SPHERICAL_SURFACE ( 'NONE', #16064, 0.5000000000000000000 ) ;
#31952=CARTESIAN_POINT ( 'NONE',  ( -3.729013601334864703, -1.848214304039853095, -1.500000000000000000 ) ) ;
#31961=CARTESIAN_POINT ( 'NONE',  ( 23.81423349025572733, -17.27971345279117088, 1.410233427488315705 ) ) ;
#31963=CARTESIAN_POINT ( 'NONE',  ( 20.99695690729567232, -21.77932090203123749, 1.367431712678154110 ) ) ;
#31978=CARTESIAN_POINT ( 'NONE',  ( 10.65647057407944942, -13.03481288882011491, -1.500000000000000000 ) ) ;
#31979=CARTESIAN_POINT ( 'NONE',  ( 107.5500550589464126, -18.81356462609017655, -4.828513639309408134 ) ) ;
#31984=B_SPLINE_CURVE_WITH_KNOTS ( 'NONE', 3,
 ( #25511, #24849, #17483, #22692, #15307, #32730, #2619, #32895, #10115, #113, #4628, #20174, #15152, #4785 ),
 .UNSPECIFIED., .F., .F.,
 ( 4, 2, 2, 2, 2, 2, 4 ),
 ( 8.673617379884034509E-19, 0.0001249451318035515839, 0.0002498902636071023003, 0.0004997805272141984207, 0.0007496707908212945411, 0.0008746159226248436313, 0.0009995610544283927215 ),
 .UNSPECIFIED. ) ;
#31985=CARTESIAN_POINT ( 'NONE',  ( 24.40244105150047105, -17.41898962163720554, -1.432663565948197437 ) ) ;
#31989=CARTESIAN_POINT ( 'NONE',  ( 107.3781042300268354, -16.32440815734132045, -2.398398155969891032 ) ) ;
#31995=CARTESIAN_POINT ( 'NONE',  ( 3.066471221417552684, -11.21726243446034132, -1.500000000000000222 ) ) ;
#31998=EDGE_LOOP ( 'NONE', ( #10578, #17629, #9867, #17050 ) ) ;
#31999=CARTESIAN_POINT ( 'NONE',  ( 25.16500339546704978, -17.49275296966160198, -1.172809483625713023 ) ) ;
#32001=CARTESIAN_POINT ( 'NONE',  ( 18.73041676179999726, -21.25644754115815260, -1.734286084696279095 ) ) ;
#32005=EDGE_LOOP ( 'NONE', ( #3946, #10690, #11314, #18219 ) ) ;
#32008=ORIENTED_EDGE ( 'NONE', *, *, #3497, .T. ) ;
#32013=ADVANCED_FACE ( 'NONE', ( #28756 ), #1711, .T. ) ;
#32019=ADVANCED_FACE ( 'NONE', ( #1008 ), #31669, .F. ) ;
#32034=CARTESIAN_POINT ( 'NONE',  ( 23.09505198155390460, -21.93193643537372495, -1.086921436894753956 ) ) ;
#32038=CARTESIAN_POINT ( 'NONE',  ( 6.645633185707460200, -7.177124861698851888, -1.500000000000000000 ) ) ;
#32040=CARTESIAN_POINT ( 'NONE',  ( 3.640540270743287898, -12.13672865749711605, 1.758210070446800444 ) ) ;
#32049=CARTESIAN_POINT ( 'NONE',  ( 24.30482536760584367, -17.42173634883301858, -1.458717893414869904 ) ) ;
#32054=CARTESIAN_POINT ( 'NONE',  ( 22.68241379554131854, -21.87740465772118270, -1.258814731508510087 ) ) ;
#32073=CARTESIAN_POINT ( 'NONE',  ( 25.52557118915447987, -17.56218954043521663, -1.000000000000000444 ) ) ;
#32076=FACE_BOUND ( 'NONE', #2098, .T. ) ;
#32077=CIRCLE ( 'NONE', #18203, 0.5000000000000004441 ) ;
#32085=ORIENTED_EDGE ( 'NONE', *, *, #11401, .F. ) ;
#32095=CARTESIAN_POINT ( 'NONE',  ( 107.4500373638809947, -17.36019379023286646, 4.522129901861156931 ) ) ;
#32098=CARTESIAN_POINT ( 'NONE',  ( 2.325338337819572221, -10.58933493131363690, -1.500000000000000000 ) ) ;
#32102=DIRECTION ( 'NONE',  ( 0.000000000000000000, 0.000000000000000000, -1.000000000000000000 ) ) ;
#32106=CIRCLE ( 'NONE', #4321, 8.000000000000000000 ) ;
#32107=ORIENTED_EDGE ( 'NONE', *, *, #17035, .T. ) ;
#32108=CARTESIAN_POINT ( 'NONE',  ( 2.637178239634298205, -1.030952082498953744E-33, 1.518998482601880973 ) ) ;
#32111=CIRCLE ( 'NONE', #21948, 0.5000000000000000000 ) ;
#32112=ADVANCED_FACE ( 'NONE', ( #20219 ), #23065, .F. ) ;
#32113=PRODUCT_DEFINITION ( 'UNKNOWN', '', #1824, #19273 ) ;
#32115=CIRCLE ( 'NONE', #10213, 0.4499999999999996225 ) ;
#32132=CARTESIAN_POINT ( 'NONE',  ( 107.9803621325096685, -17.78658171004472521, 4.330008079635504714 ) ) ;
#32145=CIRCLE ( 'NONE', #96, 0.5000000000000004441 ) ;
#32148=CARTESIAN_POINT ( 'NONE',  ( 3.326404063733029215, -17.46746234660859187, -1.500000000000001776 ) ) ;
#32153=CARTESIAN_POINT ( 'NONE',  ( 6.694810660865504914, -7.699995848971193269, -1.500000000000000000 ) ) ;
#32154=CARTESIAN_POINT ( 'NONE',  ( 107.9963546461726622, -18.01686992834544654, -5.137599899355107524 ) ) ;
#32164=VECTOR ( 'NONE', #21986, 1000.000000000000000 ) ;
#32179=CARTESIAN_POINT ( 'NONE',  ( 2.386646147131364248, -0.3554301312245153333, -1.500000000000000666 ) ) ;
#32182=ORIENTED_EDGE ( 'NONE', *, *, #18889, .T. ) ;
#32204=CARTESIAN_POINT ( 'NONE',  ( -2.786590204610737587, -5.640011313469492471, -4.522129901861166701 ) ) ;
#32210=DIRECTION ( 'NONE',  ( -1.000000000000000000, 0.000000000000000000, -0.000000000000000000 ) ) ;
#32223=CYLINDRICAL_SURFACE ( 'NONE', #30565, 0.5000000000000004441 ) ;
#32224=CARTESIAN_POINT ( 'NONE',  ( 6.734961451239206198, -5.723322302743246937, 1.500000000000000000 ) ) ;
#32227=CARTESIAN_POINT ( 'NONE',  ( -30.49402871571406948, -10.96966150227469505, -11.50000000000000000 ) ) ;
#32230=CARTESIAN_POINT ( 'NONE',  ( 3.985780818972730177, -12.21549014006416733, 1.500000000000104583 ) ) ;
#32233=ORIENTED_EDGE ( 'NONE', *, *, #14071, .F. ) ;
#32234=CARTESIAN_POINT ( 'NONE',  ( -3.368890048313184504, -11.43143575104568832, 1.500000000000000666 ) ) ;
#32235=B_SPLINE_CURVE_WITH_KNOTS ( 'NONE', 3,
 ( #8984, #19195, #15404, #16201, #5827, #2727, #12901, #20624, #30832, #18546, #27395, #4654 ),
 .UNSPECIFIED., .F., .F.,
 ( 4, 2, 2, 2, 2, 4 ),
 ( -5.999999992760755618E-08, 0.0005421413210631730083, 0.0008132419815947244772, 0.001084342642126276055, 0.001626543963189388967, 0.002168745284252502313 ),
 .UNSPECIFIED. ) ;
#32242=VERTEX_POINT ( 'NONE', #24918 ) ;
#32253=CARTESIAN_POINT ( 'NONE',  ( -31.43793636962779203, -21.68942756709066089, 1.500000000000000000 ) ) ;
#32256=DIRECTION ( 'NONE',  ( -0.000000000000000000, 0.000000000000000000, 1.000000000000000000 ) ) ;
#32262=ORIENTED_EDGE ( 'NONE', *, *, #31428, .T. ) ;
#32265=ORIENTED_EDGE ( 'NONE', *, *, #9393, .T. ) ;
#32288=CARTESIAN_POINT ( 'NONE',  ( 8.438478135943391578, -14.31961526477670787, -1.500000000000000444 ) ) ;
#32290=ORIENTED_EDGE ( 'NONE', *, *, #22667, .F. ) ;
#32305=CARTESIAN_POINT ( 'NONE',  ( -17.34999999999999787, -10.96966150227469505, -11.00000000000000000 ) ) ;
#32306=CARTESIAN_POINT ( 'NONE',  ( -4.280320213591900291, -6.512170938462894298, -1.499999999999840128 ) ) ;
#32318=ORIENTED_EDGE ( 'NONE', *, *, #30556, .T. ) ;
#32328=DIRECTION ( 'NONE',  ( -0.000000000000000000, -0.000000000000000000, 1.000000000000000000 ) ) ;
#32335=CARTESIAN_POINT ( 'NONE',  ( 107.4894986256252594, -17.93307083222387632, -5.107540108678854551 ) ) ;
#32337=CARTESIAN_POINT ( 'NONE',  ( -23.35000000000000142, -10.96966150227469505, -1.499999999999999556 ) ) ;
#32343=ORIENTED_EDGE ( 'NONE', *, *, #23865, .T. ) ;
#32344=CARTESIAN_POINT ( 'NONE',  ( -16.96515769256209794, -28.43932300454936879, 11.09540449768827131 ) ) ;
#32349=CARTESIAN_POINT ( 'NONE',  ( 3.583596913636406533, -0.01388667853607431120, -1.134179515492645729 ) ) ;
#32351=CARTESIAN_POINT ( 'NONE',  ( 7.622999046548425639, -3.997048926087008791, 1.000000000000000000 ) ) ;
#32357=CARTESIAN_POINT ( 'NONE',  ( 18.06290729145370477, -21.14813556147819540, -1.751201132231419377 ) ) ;
#32371=CARTESIAN_POINT ( 'NONE',  ( 108.0597073579234149, -18.92913321739387200, 4.563813387248837117 ) ) ;
#32374=CARTESIAN_POINT ( 'NONE',  ( 0.7294883270164040923, -11.94795532514583591, -5.485967528433937979 ) ) ;
#32376=CARTESIAN_POINT ( 'NONE',  ( 25.20116447083525557, -17.53130488828757549, 1.247823832778429898 ) ) ;
#32388=CARTESIAN_POINT ( 'NONE',  ( 7.611844841314722387, -2.453950335954110162, -1.500000000000000222 ) ) ;
#32392=CARTESIAN_POINT ( 'NONE',  ( -50.60000000000000142, -21.43932300454937945, -1.000000000000000000 ) ) ;
#32394=CARTESIAN_POINT ( 'NONE',  ( 8.528645601772334217, -0.5000000000000000000, -1.500000000000000000 ) ) ;
#32399=ORIENTED_EDGE ( 'NONE', *, *, #25996, .T. ) ;
#32401=CARTESIAN_POINT ( 'NONE',  ( 23.27353278736380204, -21.94187821002792660, -1.000000000000000000 ) ) ;
#32421=PLANE ( 'NONE',  #22086 ) ;
#32440=CARTESIAN_POINT ( 'NONE',  ( 0.1361373023263046378, -7.043147518533485751, -1.774498076833521898 ) ) ;
#32441=CARTESIAN_POINT ( 'NONE',  ( -15.02135460118491217, -25.93932300454937945, 1.095404497688272638 ) ) ;
#32445=EDGE_CURVE ( 'NONE', #31825, #25210, #29514, .T. ) ;
#32447=ORIENTED_EDGE ( 'NONE', *, *, #2729, .T. ) ;
#32456=CARTESIAN_POINT ( 'NONE',  ( 8.152039755618655903, -19.35439874310824848, -1.499999999999998668 ) ) ;
#32460=CARTESIAN_POINT ( 'NONE',  ( 107.6149215477164347, -15.92400613423468414, 1.487010776595586670 ) ) ;
#32464=CARTESIAN_POINT ( 'NONE',  ( 21.39621122230731487, -21.77804412735446959, 1.397661460514373122 ) ) ;
#32467=LINE ( 'NONE', #17407, #16579 ) ;
#32479=CARTESIAN_POINT ( 'NONE',  ( 15.88617735125738584, -21.20699763342221900, -1.500000000000000222 ) ) ;
#32484=CARTESIAN_POINT ( 'NONE',  ( 7.461135470892884314, -4.560857689778476498, -1.000000000000000000 ) ) ;
#32486=CARTESIAN_POINT ( 'NONE',  ( 107.9815267783868649, -17.80335232094880382, -4.374195006133829722 ) ) ;
#32493=CARTESIAN_POINT ( 'NONE',  ( -31.85000000000000497, -10.96966150227469505, 4.000000000000000000 ) ) ;
#32499=VERTEX_POINT ( 'NONE', #13524 ) ;
#32501=B_SPLINE_CURVE_WITH_KNOTS ( 'NONE', 3,
 ( #15703, #973, #18381, #28880 ),
 .UNSPECIFIED., .F., .F.,
 ( 4, 4 ),
 ( -7.558714219364254830E-06, 0.0001212692848185989160 ),
 .UNSPECIFIED. ) ;
#32503=CARTESIAN_POINT ( 'NONE',  ( 12.57238041616097313, -15.42470150510370708, -0.9788672205888330202 ) ) ;
#32505=DIRECTION ( 'NONE',  ( 0.000000000000000000, 0.000000000000000000, -1.000000000000000000 ) ) ;
#32509=CARTESIAN_POINT ( 'NONE',  ( 21.20754276729296706, -21.72113672149313857, -1.466027919133052304 ) ) ;
#32513=EDGE_CURVE ( 'NONE', #25887, #7812, #17738, .T. ) ;
#32523=CARTESIAN_POINT ( 'NONE',  ( 13.65718777918027271, -19.09288791508984318, -4.522129901861166701 ) ) ;
#32524=CARTESIAN_POINT ( 'NONE',  ( 107.3822631068044871, -16.38429022892981024, -2.521216264004209506 ) ) ;
#32525=CARTESIAN_POINT ( 'NONE',  ( 25.38273381070388979, -17.54867692718855920, 1.149837904939749800 ) ) ;
#32528=CARTESIAN_POINT ( 'NONE',  ( 17.49368528859141847, -18.49828807951654497, 5.485967528433933538 ) ) ;
#32534=EDGE_LOOP ( 'NONE', ( #8597, #29555, #30844, #22655 ) ) ;
#32543=ADVANCED_FACE ( 'NONE', ( #13828 ), #23092, .T. ) ;
#32555=CARTESIAN_POINT ( 'NONE',  ( 22.46520446472753463, -21.85309543850499736, -1.407654187663929024 ) ) ;
#32559=ORIENTED_EDGE ( 'NONE', *, *, #22373, .T. ) ;
#32565=AXIS2_PLACEMENT_3D ( 'NONE', #32883, #2283, #7130 ) ;
#32567=CARTESIAN_POINT ( 'NONE',  ( 25.25173065115962245, -17.50931434788435936, -1.141336708623620577 ) ) ;
#32569=CARTESIAN_POINT ( 'NONE',  ( 23.19643008672779771, -21.93767770566448050, 1.043375197815962885 ) ) ;
#32597=CARTESIAN_POINT ( 'NONE',  ( 0.5878146867678383236, -8.555166304036935898, -1.500000000000070832 ) ) ;
#32599=CARTESIAN_POINT ( 'NONE',  ( 3.541509388326189001, -13.88765124358304170, 4.522129901861157819 ) ) ;
#32614=CARTESIAN_POINT ( 'NONE',  ( 14.48598712922800225, -20.94846587651628056, -1.499999999999997780 ) ) ;
#32643=CARTESIAN_POINT ( 'NONE',  ( -4.179200081765273467, -3.233695810519997327, 1.500000000000000000 ) ) ;
#32645=CARTESIAN_POINT ( 'NONE',  ( 107.4510233030913611, -17.37417541359246087, -4.558428962808153351 ) ) ;
#32648=AXIS2_PLACEMENT_3D ( 'NONE', #23821, #21646, #21308 ) ;
#32653=DIRECTION ( 'NONE',  ( 1.000000000000000000, 0.000000000000000000, 0.000000000000000000 ) ) ;
#32655=DIRECTION ( 'NONE',  ( -0.000000000000000000, -1.000000000000000000, 0.000000000000000000 ) ) ;
#32659=EDGE_CURVE ( 'NONE', #30204, #3232, #11519, .T. ) ;
#32667=FACE_OUTER_BOUND ( 'NONE', #4595, .T. ) ;
#32671=EDGE_CURVE ( 'NONE', #24299, #3835, #20544, .T. ) ;
#32677=CARTESIAN_POINT ( 'NONE',  ( -3.043410827172835731, -0.3793687891476489882, 1.490164052093359670 ) ) ;
#32688=DIRECTION ( 'NONE',  ( -1.387778780781444413E-14, 0.000000000000000000, -1.000000000000000000 ) ) ;
#32692=AXIS2_PLACEMENT_3D ( 'NONE', #17357, #20539, #5148 ) ;
#32695=CARTESIAN_POINT ( 'NONE',  ( 24.61821134308531356, -17.47399247671398115, 1.556972331816578459 ) ) ;
#32712=AXIS2_PLACEMENT_3D ( 'NONE', #2636, #12799, #23014 ) ;
#32715=CARTESIAN_POINT ( 'NONE',  ( 0.000000000000000000, -27.93932300454937590, -1.000000000000000000 ) ) ;
#32717=VECTOR ( 'NONE', #32655, 1000.000000000000000 ) ;
#32719=CARTESIAN_POINT ( 'NONE',  ( 8.533641835123258801, -14.05299950477806625, 1.499999999999999556 ) ) ;
#32721=AXIS2_PLACEMENT_3D ( 'NONE', #1902, #7051, #22270 ) ;
#32730=CARTESIAN_POINT ( 'NONE',  ( 108.0161426671036082, -18.30181250712185559, -4.596922648963735369 ) ) ;
#32739=CIRCLE ( 'NONE', #25251, 10.96966150227469328 ) ;
#32752=CARTESIAN_POINT ( 'NONE',  ( 23.22564588060109259, -21.93932300456764040, 1.000000000000000000 ) ) ;
#32758=DIRECTION ( 'NONE',  ( 1.000000000000000000, 0.000000000000000000, 0.000000000000000000 ) ) ;
#32763=CARTESIAN_POINT ( 'NONE',  ( 21.37793795825544052, -21.75892242064796278, 1.431755257449183194 ) ) ;
#32769=AXIS2_PLACEMENT_3D ( 'NONE', #6282, #956, #3145 ) ;
#32779=CARTESIAN_POINT ( 'NONE',  ( 0.2332737126359348268, -7.747681480072266424, -1.773831282197832371 ) ) ;
#32780=CARTESIAN_POINT ( 'NONE',  ( 0.1610798642962572302, -10.72944008624798151, 4.522129901861157819 ) ) ;
#32787=EDGE_CURVE ( 'NONE', #1029, #23722, #21176, .T. ) ;
#32788=CARTESIAN_POINT ( 'NONE',  ( 23.02255580927015188, -17.31849206757248183, 1.529834177132855633 ) ) ;
#32794=EDGE_CURVE ( 'NONE', #8502, #3835, #17675, .T. ) ;
#32800=CARTESIAN_POINT ( 'NONE',  ( -2.787158681079298095, -12.40563758779646264, -1.500000000000000000 ) ) ;
#32805=FACE_OUTER_BOUND ( 'NONE', #9598, .T. ) ;
#32811=CIRCLE ( 'NONE', #18389, 0.5000000000000000000 ) ;
#32817=VERTEX_POINT ( 'NONE', #5160 ) ;
#32826=CARTESIAN_POINT ( 'NONE',  ( 8.845957756765750801, -0.9823800963979932854, -1.500000000000000000 ) ) ;
#32828=CARTESIAN_POINT ( 'NONE',  ( 107.5612922043142561, -18.97663357200326217, -4.540760459233397661 ) ) ;
#32837=AXIS2_PLACEMENT_3D ( 'NONE', #16454, #32869, #22314 ) ;
#32846=FACE_OUTER_BOUND ( 'NONE', #10956, .T. ) ;
#32854=PLANE ( 'NONE',  #2667 ) ;
#32861=CARTESIAN_POINT ( 'NONE',  ( 0.1962428234089072521, -6.885380501030516243, -1.500000000000000000 ) ) ;
#32869=DIRECTION ( 'NONE',  ( -0.000000000000000000, 0.000000000000000000, 1.000000000000000000 ) ) ;
#32883=CARTESIAN_POINT ( 'NONE',  ( -50.60000000000000142, -10.96966150227468972, 7.074999999999997513 ) ) ;
#32886=CARTESIAN_POINT ( 'NONE',  ( 107.4513092838961796, -17.37832399921928683, 4.568466631925298671 ) ) ;
#32891=CARTESIAN_POINT ( 'NONE',  ( 111.5384102276657785, -20.44549501351493603, -0.9788672205760856615 ) ) ;
#32895=CARTESIAN_POINT ( 'NONE',  ( 107.9988871568685909, -18.05333745236665166, -4.637859085129263370 ) ) ;
#32901=CARTESIAN_POINT ( 'NONE',  ( 21.40209301355503513, -21.75562217689082800, -1.444354797330493989 ) ) ;
#32930=CARTESIAN_POINT ( 'NONE',  ( 2.482257818914018088, 0.000000000000000000, -1.712210361609936005 ) ) ;
#32935=CARTESIAN_POINT ( 'NONE',  ( 108.0375632182117869, -18.61026311478333994, -4.377304920009720490 ) ) ;
#32946=CARTESIAN_POINT ( 'NONE',  ( 24.09939086539757014, -17.43210107469715098, 1.523452847363739870 ) ) ;
#32954=CARTESIAN_POINT ( 'NONE',  ( 5.388150845455290217, -18.36759383093766118, -1.499999999999999112 ) ) ;
#32972=CARTESIAN_POINT ( 'NONE',  ( -50.60000000000000142, -10.96966150227468972, 1.500000000000000000 ) ) ;
#32980=CARTESIAN_POINT ( 'NONE',  ( -4.147439473165015045, -6.154442848042452674, 1.745243268039455620 ) ) ;
#32982=CARTESIAN_POINT ( 'NONE',  ( 107.5615883074459020, -18.98093538359634636, -4.529405805268299723 ) ) ;
#32988=CARTESIAN_POINT ( 'NONE',  ( -2.837798564937434875, -0.5311976243149594268, -1.513817338014939118 ) ) ;
#32994=DIRECTION ( 'NONE',  ( 0.1908089953765452762, 0.000000000000000000, 0.9816271834476639757 ) ) ;
#32996=VERTEX_POINT ( 'NONE', #1303 ) ;
#32998=EDGE_CURVE ( 'NONE', #14095, #22172, #21523, .T. ) ;
#33003=CARTESIAN_POINT ( 'NONE',  ( -2.742527549463130931, 0.2598362491872778235, 1.021881266978499792 ) ) ;
#33006=EDGE_LOOP ( 'NONE', ( #8485, #6061 ) ) ;
#33012=CARTESIAN_POINT ( 'NONE',  ( 0.1371395441367533607, -7.141515111121043091, -1.774689084756775781 ) ) ;
#33018=CARTESIAN_POINT ( 'NONE',  ( 25.29940076078100475, -17.51841556854394710, 1.122629911123150803 ) ) ;
#33019=CARTESIAN_POINT ( 'NONE',  ( -3.142639414278896925, -12.00291247001455730, 0.9788672205877712029 ) ) ;
#33020=CARTESIAN_POINT ( 'NONE',  ( 0.9232102171129888957, 0.000000000000000000, 4.522129901861156931 ) ) ;
#33025=ORIENTED_EDGE ( 'NONE', *, *, #19243, .F. ) ;
#33029=CARTESIAN_POINT ( 'NONE',  ( 23.22564588060107482, -21.93932300456764040, -1.000000000000000000 ) ) ;
#33038=ORIENTED_EDGE ( 'NONE', *, *, #22795, .T. ) ;
#33043=EDGE_LOOP ( 'NONE', ( #17505, #16601, #33049, #3750, #22269 ) ) ;
#33047=CARTESIAN_POINT ( 'NONE',  ( 21.36179047124926811, -21.76611816616638251, -1.413258355470295102 ) ) ;
#33049=ORIENTED_EDGE ( 'NONE', *, *, #32998, .F. ) ;
#33050=DIRECTION ( 'NONE',  ( -1.000000000000000000, 2.473959037481237219E-13, -0.000000000000000000 ) ) ;
#33052=ADVANCED_FACE ( 'NONE', ( #14641 ), #9952, .T. ) ;
#33056=CARTESIAN_POINT ( 'NONE',  ( 24.26973362692477920, -17.42849669161047288, -1.479847483348366355 ) ) ;
#33067=CARTESIAN_POINT ( 'NONE',  ( 0.1483196811915227509, -7.185865554061074967, 1.774508006492702128 ) ) ;
#33069=EDGE_LOOP ( 'NONE', ( #14114, #5588, #16120, #1179 ) ) ;
#33078=PLANE ( 'NONE',  #5376 ) ;
#33086=CARTESIAN_POINT ( 'NONE',  ( 14.67783075693927408, -16.02377530647586923, -1.500000000000000222 ) ) ;
#33088=CARTESIAN_POINT ( 'NONE',  ( -1.170068671574864494, -6.059534462705076230, 4.522129901861157819 ) ) ;
#33094=DIRECTION ( 'NONE',  ( 0.000000000000000000, 0.000000000000000000, 1.000000000000000000 ) ) ;
#33096=CARTESIAN_POINT ( 'NONE',  ( 23.74728587540910496, -17.43182369245540286, 1.598909884664836856 ) ) ;
#33113=COLOUR_RGB('Light Blue', 0.31764706, 0.68627451, 0.89019608);
#33114=FILL_AREA_STYLE_COLOUR('',#33113);
#33115=FILL_AREA_STYLE('',(#33114));
#33116=SURFACE_STYLE_FILL_AREA(#33115);
#33117=SURFACE_SIDE_STYLE('',(#33116));
#33118=SURFACE_STYLE_USAGE(.BOTH.,#33117);
#33119=PRESENTATION_STYLE_ASSIGNMENT((#33118));
#33156=STYLED_ITEM('',(#33119),#10233);
#33157=MECHANICAL_DESIGN_GEOMETRIC_PRESENTATION_REPRESENTATION('',(#33156),#179);
ENDSEC;
END-ISO-10303-21;
